ISO-10303-21;
HEADER;
FILE_DESCRIPTION (('STEP AP214'),
    '1' );
FILE_NAME ('spur gear_iso_ISO - Spur gear 3M 46T 20PA 20FW ---S46C15H150L8.0S1.step',
    '2026-10-03T12:29:21',
    ( '' ),
    ( '' ),
    'SwSTEP 2.0',
    'SolidWorks 2026',
    '' );
FILE_SCHEMA (( 'AUTOMOTIVE_DESIGN' ));
ENDSEC;

DATA;
#1=CARTESIAN_POINT ( 'NONE',  ( 19.99999999999999645, 0.000000000000000000, 0.000000000000000000 ) ) ;
#10=CYLINDRICAL_SURFACE ( 'NONE', #420, 72.00000000007199219 ) ;
#16=ORIENTED_EDGE ( 'NONE', *, *, #12265, .T. ) ;
#18=EDGE_LOOP ( 'NONE', ( #17253, #7628, #12680, #16637 ) ) ;
#19=DIRECTION ( 'NONE',  ( -1.000000000000000000, 0.000000000000000000, -0.000000000000000000 ) ) ;
#24=DIRECTION ( 'NONE',  ( -1.000000000000000000, -0.000000000000000000, 0.000000000000000000 ) ) ;
#25=CARTESIAN_POINT ( 'NONE',  ( 19.99999999999999645, 0.000000000000000000, 0.000000000000000000 ) ) ;
#27=AXIS2_PLACEMENT_3D ( 'NONE', #16790, #15301, #10014 ) ;
#29=ORIENTED_EDGE ( 'NONE', *, *, #16424, .T. ) ;
#30=ADVANCED_FACE ( 'NONE', ( #14609 ), #17902, .T. ) ;
#39=ORIENTED_EDGE ( 'NONE', *, *, #4985, .T. ) ;
#42=ORIENTED_EDGE ( 'NONE', *, *, #280, .F. ) ;
#45=CARTESIAN_POINT ( 'NONE',  ( 19.99999999999999645, -20.60847369612940128, -61.90898814327737654 ) ) ;
#53=ORIENTED_EDGE ( 'NONE', *, *, #13639, .F. ) ;
#58=CIRCLE ( 'NONE', #5129, 27.60000000002759890 ) ;
#60=VECTOR ( 'NONE', #20579, 1000.000000000000000 ) ;
#63=LINE ( 'NONE', #20325, #13108 ) ;
#64=DIRECTION ( 'NONE',  ( 0.000000000000000000, 0.000000000000000000, 1.000000000000000000 ) ) ;
#70=CARTESIAN_POINT ( 'NONE',  ( 0.000000000000000000, 38.69327817041775575, 52.53819777490647880 ) ) ;
#73=ORIENTED_EDGE ( 'NONE', *, *, #769, .F. ) ;
#75=AXIS2_PLACEMENT_3D ( 'NONE', #412, #6863, #13354 ) ;
#81=ORIENTED_EDGE ( 'NONE', *, *, #16157, .T. ) ;
#82=DIRECTION ( 'NONE',  ( 0.000000000000000000, -0.2697967711570314897, 0.9629172873477973571 ) ) ;
#85=VECTOR ( 'NONE', #11262, 1000.000000000000000 ) ;
#88=EDGE_CURVE ( 'NONE', #14573, #2530, #13132, .T. ) ;
#89=DIRECTION ( 'NONE',  ( -1.000000000000000000, 0.000000000000000000, 0.000000000000000000 ) ) ;
#91=CARTESIAN_POINT ( 'NONE',  ( 150.0000507999999968, 5.400000000000000355, 1.000000000000000000 ) ) ;
#96=CARTESIAN_POINT ( 'NONE',  ( 0.000000000000000000, -3.141410481200616278, -65.17333458706190186 ) ) ;
#98=ORIENTED_EDGE ( 'NONE', *, *, #9726, .F. ) ;
#99=AXIS2_PLACEMENT_3D ( 'NONE', #7590, #19041, #10873 ) ;
#107=CARTESIAN_POINT ( 'NONE',  ( -65.00002539999999840, 3.872983346207417021, 1.000000000000000000 ) ) ;
#109=EDGE_CURVE ( 'NONE', #12091, #18834, #15657, .T. ) ;
#114=CARTESIAN_POINT ( 'NONE',  ( 150.0000507999999968, 0.000000000000000000, 1.000000000000000000 ) ) ;
#116=DIRECTION ( 'NONE',  ( -1.000000000000000000, -0.000000000000000000, 0.000000000000000000 ) ) ;
#117=CIRCLE ( 'NONE', #15334, 27.60000000002759890 ) ;
#119=AXIS2_PLACEMENT_3D ( 'NONE', #12857, #16234, #19212 ) ;
#121=ORIENTED_EDGE ( 'NONE', *, *, #380, .T. ) ;
#125=VERTEX_POINT ( 'NONE', #13749 ) ;
#126=CARTESIAN_POINT ( 'NONE',  ( -10.00000000000000000, 0.000000000000000000, 0.000000000000000000 ) ) ;
#134=CIRCLE ( 'NONE', #11980, 27.60000000002760245 ) ;
#137=DIRECTION ( 'NONE',  ( 1.000000000000000000, -0.000000000000000000, -0.000000000000000000 ) ) ;
#138=DIRECTION ( 'NONE',  ( 0.000000000000000000, 0.000000000000000000, -1.000000000000000000 ) ) ;
#141=VERTEX_POINT ( 'NONE', #18522 ) ;
#144=ORIENTED_EDGE ( 'NONE', *, *, #13905, .F. ) ;
#145=CYLINDRICAL_SURFACE ( 'NONE', #1488, 65.24900000006525147 ) ;
#147=DIRECTION ( 'NONE',  ( 0.000000000000000000, -0.9790840876823206917, -0.2034560130526446298 ) ) ;
#148=ORIENTED_EDGE ( 'NONE', *, *, #3636, .F. ) ;
#150=EDGE_CURVE ( 'NONE', #3064, #8629, #754, .T. ) ;
#153=CARTESIAN_POINT ( 'NONE',  ( 0.000000000000000000, 64.52323195238628273, 6.389157729493382121 ) ) ;
#160=ORIENTED_EDGE ( 'NONE', *, *, #19316, .T. ) ;
#162=STYLED_ITEM ( 'NONE', ( #18380 ), #10511 ) ;
#165=DIRECTION ( 'NONE',  ( -1.000000000000000000, -0.000000000000000000, 0.000000000000000000 ) ) ;
#168=ORIENTED_EDGE ( 'NONE', *, *, #13103, .T. ) ;
#171=ORIENTED_EDGE ( 'NONE', *, *, #11662, .T. ) ;
#175=EDGE_CURVE ( 'NONE', #6580, #16499, #15026, .T. ) ;
#185=DIRECTION ( 'NONE',  ( 1.000000000000000000, 0.000000000000000000, 0.000000000000000000 ) ) ;
#187=AXIS2_PLACEMENT_3D ( 'NONE', #9461, #14239, #12440 ) ;
#198=CARTESIAN_POINT ( 'NONE',  ( 0.000000000000000000, 0.000000000000000000, 0.000000000000000000 ) ) ;
#214=CIRCLE ( 'NONE', #10382, 27.60000000002759535 ) ;
#220=VECTOR ( 'NONE', #17502, 1000.000000000000000 ) ;
#223=ORIENTED_EDGE ( 'NONE', *, *, #11424, .T. ) ;
#224=DIRECTION ( 'NONE',  ( -1.000000000000000000, -0.000000000000000000, -0.000000000000000000 ) ) ;
#227=AXIS2_PLACEMENT_3D ( 'NONE', #13728, #8834, #15310 ) ;
#235=FACE_OUTER_BOUND ( 'NONE', #1622, .T. ) ;
#242=CIRCLE ( 'NONE', #15142, 72.00000000007199219 ) ;
#245=CARTESIAN_POINT ( 'NONE',  ( 19.99999999999999645, 0.000000000000000000, 0.000000000000000000 ) ) ;
#247=ADVANCED_FACE ( 'NONE', ( #7269 ), #15224, .T. ) ;
#250=ORIENTED_EDGE ( 'NONE', *, *, #12738, .T. ) ;
#251=LINE ( 'NONE', #19844, #9700 ) ;
#254=VERTEX_POINT ( 'NONE', #932 ) ;
#255=DIRECTION ( 'NONE',  ( -1.000000000000000000, -0.000000000000000000, -0.000000000000000000 ) ) ;
#256=ORIENTED_EDGE ( 'NONE', *, *, #14101, .F. ) ;
#260=VECTOR ( 'NONE', #15777, 1000.000000000000000 ) ;
#261=LINE ( 'NONE', #14579, #14811 ) ;
#263=AXIS2_PLACEMENT_3D ( 'NONE', #7440, #2362, #13920 ) ;
#267=ADVANCED_FACE ( 'NONE', ( #2088, #12152 ), #10146, .T. ) ;
#268=CIRCLE ( 'NONE', #17552, 27.60000000002759890 ) ;
#272=EDGE_CURVE ( 'NONE', #19715, #5449, #20689, .T. ) ;
#273=VERTEX_POINT ( 'NONE', #11836 ) ;
#276=DIRECTION ( 'NONE',  ( 0.000000000000000000, 0.000000000000000000, 1.000000000000000000 ) ) ;
#277=DIRECTION ( 'NONE',  ( 0.000000000000000000, 0.000000000000000000, 1.000000000000000000 ) ) ;
#280=EDGE_CURVE ( 'NONE', #8357, #19645, #2082, .T. ) ;
#281=VERTEX_POINT ( 'NONE', #13962 ) ;
#283=ORIENTED_EDGE ( 'NONE', *, *, #9192, .T. ) ;
#284=CARTESIAN_POINT ( 'NONE',  ( 0.000000000000000000, 0.000000000000000000, 0.000000000000000000 ) ) ;
#288=EDGE_CURVE ( 'NONE', #12045, #14031, #12238, .T. ) ;
#291=CYLINDRICAL_SURFACE ( 'NONE', #18893, 65.24900000006525147 ) ;
#297=VERTEX_POINT ( 'NONE', #18840 ) ;
#304=FACE_OUTER_BOUND ( 'NONE', #4733, .T. ) ;
#305=DIRECTION ( 'NONE',  ( -1.000000000000000000, 0.000000000000000000, -0.000000000000000000 ) ) ;
#308=CARTESIAN_POINT ( 'NONE',  ( 19.99999999999999645, 3.141410481201988070, -65.17333458706183080 ) ) ;
#309=CARTESIAN_POINT ( 'NONE',  ( -10.00000000000000000, 0.000000000000000000, 0.000000000000000000 ) ) ;
#310=LINE ( 'NONE', #8363, #85 ) ;
#311=CARTESIAN_POINT ( 'NONE',  ( 19.99999999999999645, 0.000000000000000000, 0.000000000000000000 ) ) ;
#320=ORIENTED_EDGE ( 'NONE', *, *, #19952, .T. ) ;
#323=CARTESIAN_POINT ( 'NONE',  ( 0.000000000000000000, -44.69367065308607323, -56.44887778834792869 ) ) ;
#325=DIRECTION ( 'NONE',  ( -1.000000000000000000, -0.000000000000000000, 0.000000000000000000 ) ) ;
#326=AXIS2_PLACEMENT_3D ( 'NONE', #1007, #15102, #2907 ) ;
#328=LINE ( 'NONE', #4786, #20321 ) ;
#337=ORIENTED_EDGE ( 'NONE', *, *, #5451, .T. ) ;
#339=DIRECTION ( 'NONE',  ( 0.000000000000000000, 0.000000000000000000, 1.000000000000000000 ) ) ;
#340=CARTESIAN_POINT ( 'NONE',  ( 19.99999999999999645, -46.17500197033019305, -55.24372537266444283 ) ) ;
#341=DIRECTION ( 'NONE',  ( -1.000000000000000000, -0.000000000000000000, 0.000000000000000000 ) ) ;
#347=CARTESIAN_POINT ( 'NONE',  ( 0.000000000000000000, 68.15657073222436679, 23.20952102120305582 ) ) ;
#348=AXIS2_PLACEMENT_3D ( 'NONE', #20750, #6237, #19174 ) ;
#350=CARTESIAN_POINT ( 'NONE',  ( 19.99999999999999645, 0.000000000000000000, 0.000000000000000000 ) ) ;
#353=DIRECTION ( 'NONE',  ( 0.000000000000000000, 0.000000000000000000, 1.000000000000000000 ) ) ;
#354=DIRECTION ( 'NONE',  ( -1.000000000000000000, 0.000000000000000000, 0.000000000000000000 ) ) ;
#365=ORIENTED_EDGE ( 'NONE', *, *, #15296, .T. ) ;
#367=DIRECTION ( 'NONE',  ( -1.000000000000000000, 0.000000000000000000, 0.000000000000000000 ) ) ;
#372=EDGE_LOOP ( 'NONE', ( #18195, #3696, #3655, #20079 ) ) ;
#373=CYLINDRICAL_SURFACE ( 'NONE', #5994, 27.60000000002760245 ) ;
#374=CIRCLE ( 'NONE', #15611, 72.00000000007199219 ) ;
#377=DIRECTION ( 'NONE',  ( 0.000000000000000000, 0.9422609221188190665, 0.3348796121709901041 ) ) ;
#380=EDGE_CURVE ( 'NONE', #16309, #18776, #7801, .T. ) ;
#381=EDGE_CURVE ( 'NONE', #14573, #1539, #14276, .T. ) ;
#382=CARTESIAN_POINT ( 'NONE',  ( 0.000000000000000000, 0.000000000000000000, 0.000000000000000000 ) ) ;
#386=EDGE_LOOP ( 'NONE', ( #256, #15572, #3501, #7705 ) ) ;
#387=DIRECTION ( 'NONE',  ( 0.000000000000000000, 0.000000000000000000, -1.000000000000000000 ) ) ;
#402=ORIENTED_EDGE ( 'NONE', *, *, #6479, .T. ) ;
#406=AXIS2_PLACEMENT_3D ( 'NONE', #17598, #16302, #3065 ) ;
#407=ORIENTED_EDGE ( 'NONE', *, *, #13428, .F. ) ;
#409=EDGE_CURVE ( 'NONE', #16888, #19366, #720, .T. ) ;
#412=CARTESIAN_POINT ( 'NONE',  ( 0.000000000000000000, -31.98952867950364265, 56.39803944231574206 ) ) ;
#419=AXIS2_PLACEMENT_3D ( 'NONE', #4743, #6227, #16194 ) ;
#420=AXIS2_PLACEMENT_3D ( 'NONE', #16229, #16325, #1815 ) ;
#424=CARTESIAN_POINT ( 'NONE',  ( 19.99999999999999645, 0.000000000000000000, 0.000000000000000000 ) ) ;
#431=ADVANCED_FACE ( 'NONE', ( #19348 ), #12806, .T. ) ;
#434=CARTESIAN_POINT ( 'NONE',  ( 0.000000000000000000, -51.43306257653170377, 40.15061736769546741 ) ) ;
#437=CARTESIAN_POINT ( 'NONE',  ( 0.000000000000000000, -23.08379033237309841, -61.02926039941459635 ) ) ;
#439=EDGE_LOOP ( 'NONE', ( #20238, #7654, #8119, #10471 ) ) ;
#441=CARTESIAN_POINT ( 'NONE',  ( 19.99999999999999645, -14.55863677812166124, 63.60407295269099137 ) ) ;
#443=CIRCLE ( 'NONE', #7543, 27.60000000002760245 ) ;
#450=CIRCLE ( 'NONE', #13996, 27.60000000002760245 ) ;
#453=CYLINDRICAL_SURFACE ( 'NONE', #5418, 27.60000000002759890 ) ;
#454=AXIS2_PLACEMENT_3D ( 'NONE', #4721, #15855, #10975 ) ;
#460=ORIENTED_EDGE ( 'NONE', *, *, #8185, .F. ) ;
#462=DIRECTION ( 'NONE',  ( 0.000000000000000000, -0.1361666490962330500, -0.9906859460363326431 ) ) ;
#467=DIRECTION ( 'NONE',  ( -1.000000000000000000, -0.000000000000000000, -0.000000000000000000 ) ) ;
#470=AXIS2_PLACEMENT_3D ( 'NONE', #11831, #16705, #14913 ) ;
#471=CIRCLE ( 'NONE', #1159, 27.60000000002759535 ) ;
#475=FACE_OUTER_BOUND ( 'NONE', #5629, .T. ) ;
#477=DIRECTION ( 'NONE',  ( -1.000000000000000000, -0.000000000000000000, -0.000000000000000000 ) ) ;
#480=ORIENTED_EDGE ( 'NONE', *, *, #6619, .T. ) ;
#484=ORIENTED_EDGE ( 'NONE', *, *, #9111, .T. ) ;
#485=CIRCLE ( 'NONE', #12331, 27.60000000002759535 ) ;
#486=FACE_OUTER_BOUND ( 'NONE', #14457, .T. ) ;
#491=ORIENTED_EDGE ( 'NONE', *, *, #7031, .F. ) ;
#493=CARTESIAN_POINT ( 'NONE',  ( 19.99999999999999645, 58.44960523466241398, 28.06621538408611016 ) ) ;
#494=ORIENTED_EDGE ( 'NONE', *, *, #12195, .F. ) ;
#496=CIRCLE ( 'NONE', #12347, 72.00000000007199219 ) ;
#497=ORIENTED_EDGE ( 'NONE', *, *, #16576, .F. ) ;
#502=ORIENTED_EDGE ( 'NONE', *, *, #2819, .T. ) ;
#503=CIRCLE ( 'NONE', #7250, 27.60000000002759890 ) ;
#511=LINE ( 'NONE', #16826, #13773 ) ;
#513=EDGE_LOOP ( 'NONE', ( #7968, #13758, #16479, #7513 ) ) ;
#516=CIRCLE ( 'NONE', #19452, 27.60000000002760245 ) ;
#517=DIRECTION ( 'NONE',  ( -1.000000000000000000, -0.000000000000000000, 0.000000000000000000 ) ) ;
#529=VECTOR ( 'NONE', #18916, 1000.000000000000000 ) ;
#533=DIRECTION ( 'NONE',  ( 1.000000000000000000, 0.000000000000000000, -0.000000000000000000 ) ) ;
#535=ORIENTED_EDGE ( 'NONE', *, *, #11183, .F. ) ;
#541=DIRECTION ( 'NONE',  ( 1.000000000000000000, 0.000000000000000000, -0.000000000000000000 ) ) ;
#545=CIRCLE ( 'NONE', #6954, 27.60000000002759890 ) ;
#550=DIRECTION ( 'NONE',  ( -1.000000000000000000, -0.000000000000000000, -0.000000000000000000 ) ) ;
#551=VECTOR ( 'NONE', #6875, 1000.000000000000000 ) ;
#553=DIRECTION ( 'NONE',  ( 0.000000000000000000, 0.000000000000000000, -1.000000000000000000 ) ) ;
#558=LINE ( 'NONE', #11785, #13211 ) ;
#561=CIRCLE ( 'NONE', #8670, 72.00000000007199219 ) ;
#562=CIRCLE ( 'NONE', #15113, 72.00000000007199219 ) ;
#563=ORIENTED_EDGE ( 'NONE', *, *, #3533, .T. ) ;
#565=EDGE_CURVE ( 'NONE', #16083, #12428, #19535, .T. ) ;
#568=CARTESIAN_POINT ( 'NONE',  ( 19.99999999999999645, 64.80702306891095077, 7.581672767546655756 ) ) ;
#575=AXIS2_PLACEMENT_3D ( 'NONE', #4476, #9146, #4374 ) ;
#576=ORIENTED_EDGE ( 'NONE', *, *, #8396, .F. ) ;
#580=CARTESIAN_POINT ( 'NONE',  ( 19.99999999999999645, 0.000000000000000000, 0.000000000000000000 ) ) ;
#587=LINE ( 'NONE', #20169, #6447 ) ;
#593=CARTESIAN_POINT ( 'NONE',  ( 19.99999999999999645, 0.000000000000000000, 0.000000000000000000 ) ) ;
#596=ORIENTED_EDGE ( 'NONE', *, *, #15835, .F. ) ;
#598=AXIS2_PLACEMENT_3D ( 'NONE', #6935, #14894, #11405 ) ;
#601=EDGE_CURVE ( 'NONE', #3647, #5060, #13252, .T. ) ;
#602=VECTOR ( 'NONE', #1570, 1000.000000000000000 ) ;
#603=ORIENTED_EDGE ( 'NONE', *, *, #9501, .T. ) ;
#611=DIRECTION ( 'NONE',  ( -1.000000000000000000, 0.000000000000000000, -0.000000000000000000 ) ) ;
#612=ORIENTED_EDGE ( 'NONE', *, *, #3873, .T. ) ;
#616=ORIENTED_EDGE ( 'NONE', *, *, #20084, .T. ) ;
#620=LINE ( 'NONE', #13141, #16338 ) ;
#625=ORIENTED_EDGE ( 'NONE', *, *, #13485, .F. ) ;
#634=CYLINDRICAL_SURFACE ( 'NONE', #10755, 65.24900000006525147 ) ;
#635=ORIENTED_EDGE ( 'NONE', *, *, #20904, .T. ) ;
#640=CYLINDRICAL_SURFACE ( 'NONE', #9217, 27.60000000002759890 ) ;
#643=DIRECTION ( 'NONE',  ( 0.000000000000000000, 0.000000000000000000, 1.000000000000000000 ) ) ;
#645=VERTEX_POINT ( 'NONE', #3417 ) ;
#646=DIRECTION ( 'NONE',  ( -1.000000000000000000, 0.000000000000000000, 0.000000000000000000 ) ) ;
#647=CYLINDRICAL_SURFACE ( 'NONE', #5864, 27.60000000002759890 ) ;
#648=EDGE_CURVE ( 'NONE', #19326, #1518, #3112, .T. ) ;
#649=EDGE_CURVE ( 'NONE', #14031, #7362, #7493, .T. ) ;
#650=DIRECTION ( 'NONE',  ( -1.000000000000000000, 0.000000000000000000, 0.000000000000000000 ) ) ;
#653=EDGE_CURVE ( 'NONE', #2314, #5904, #10208, .T. ) ;
#654=DIRECTION ( 'NONE',  ( -1.000000000000000000, -0.000000000000000000, 0.000000000000000000 ) ) ;
#655=CARTESIAN_POINT ( 'NONE',  ( 150.0000507999999968, 3.872983346207417021, 1.000000000000000000 ) ) ;
#659=VERTEX_POINT ( 'NONE', #6491 ) ;
#662=ORIENTED_EDGE ( 'NONE', *, *, #17967, .F. ) ;
#666=CARTESIAN_POINT ( 'NONE',  ( 0.000000000000000000, -10.77748419466653651, -63.93680186330482940 ) ) ;
#671=CARTESIAN_POINT ( 'NONE',  ( 9.999999999999998224, 8.857208570069802889, 71.45313048675089362 ) ) ;
#673=EDGE_CURVE ( 'NONE', #7171, #9017, #7154, .T. ) ;
#676=EDGE_LOOP ( 'NONE', ( #14258, #7952, #17095, #1754 ) ) ;
#677=FACE_OUTER_BOUND ( 'NONE', #6851, .T. ) ;
#680=AXIS2_PLACEMENT_3D ( 'NONE', #4749, #2450, #15271 ) ;
#681=ORIENTED_EDGE ( 'NONE', *, *, #8710, .T. ) ;
#683=ORIENTED_EDGE ( 'NONE', *, *, #6446, .T. ) ;
#688=DIRECTION ( 'NONE',  ( 1.000000000000000000, 0.000000000000000000, 0.000000000000000000 ) ) ;
#689=EDGE_LOOP ( 'NONE', ( #19136, #7856, #17886, #8453 ) ) ;
#691=ORIENTED_EDGE ( 'NONE', *, *, #14028, .T. ) ;
#692=DIRECTION ( 'NONE',  ( -1.000000000000000000, 0.000000000000000000, 0.000000000000000000 ) ) ;
#702=AXIS2_PLACEMENT_3D ( 'NONE', #6719, #16070, #19647 ) ;
#706=DIRECTION ( 'NONE',  ( -1.000000000000000000, 0.000000000000000000, 0.000000000000000000 ) ) ;
#708=ORIENTED_EDGE ( 'NONE', *, *, #9616, .T. ) ;
#712=EDGE_LOOP ( 'NONE', ( #17560, #19304, #1121, #19993 ) ) ;
#714=VERTEX_POINT ( 'NONE', #2352 ) ;
#715=FACE_OUTER_BOUND ( 'NONE', #1941, .T. ) ;
#720=CIRCLE ( 'NONE', #13579, 65.24900000006525147 ) ;
#721=CARTESIAN_POINT ( 'NONE',  ( -10.00000000000000000, 0.000000000000000000, 0.000000000000000000 ) ) ;
#722=LINE ( 'NONE', #17049, #1451 ) ;
#723=VECTOR ( 'NONE', #7308, 1000.000000000000000 ) ;
#728=VECTOR ( 'NONE', #758, 1000.000000000000000 ) ;
#729=CARTESIAN_POINT ( 'NONE',  ( 85.00002539999999840, 0.000000000000000000, -1.000000000000000000 ) ) ;
#736=CIRCLE ( 'NONE', #20705, 72.00000000007199219 ) ;
#737=ORIENTED_EDGE ( 'NONE', *, *, #16854, .F. ) ;
#740=LINE ( 'NONE', #16744, #4658 ) ;
#741=AXIS2_PLACEMENT_3D ( 'NONE', #18003, #20868, #12835 ) ;
#743=DIRECTION ( 'NONE',  ( 0.000000000000000000, 0.000000000000000000, 1.000000000000000000 ) ) ;
#745=CARTESIAN_POINT ( 'NONE',  ( 19.99999999999999645, 31.17893654894229982, 57.31758819669181548 ) ) ;
#749=ORIENTED_EDGE ( 'NONE', *, *, #1732, .F. ) ;
#752=CIRCLE ( 'NONE', #4129, 72.00000000007199219 ) ;
#754=CIRCLE ( 'NONE', #9564, 27.60000000002760601 ) ;
#755=DIRECTION ( 'NONE',  ( -1.000000000000000000, -0.000000000000000000, 0.000000000000000000 ) ) ;
#756=VECTOR ( 'NONE', #17494, 1000.000000000000000 ) ;
#758=DIRECTION ( 'NONE',  ( 1.000000000000000000, 0.000000000000000000, -0.000000000000000000 ) ) ;
#761=LINE ( 'NONE', #10413, #12310 ) ;
#766=LINE ( 'NONE', #10420, #4559 ) ;
#769=EDGE_CURVE ( 'NONE', #12727, #12459, #736, .T. ) ;
#772=ORIENTED_EDGE ( 'NONE', *, *, #14173, .F. ) ;
#775=AXIS2_PLACEMENT_3D ( 'NONE', #1152, #12379, #14081 ) ;
#780=CYLINDRICAL_SURFACE ( 'NONE', #9366, 27.60000000002759890 ) ;
#782=DIRECTION ( 'NONE',  ( 0.000000000000000000, 0.000000000000000000, 1.000000000000000000 ) ) ;
#784=CARTESIAN_POINT ( 'NONE',  ( 0.000000000000000000, 38.22257254261740655, 61.01667762370151848 ) ) ;
#787=CIRCLE ( 'NONE', #16695, 65.24900000006526568 ) ;
#788=VERTEX_POINT ( 'NONE', #18252 ) ;
#796=CARTESIAN_POINT ( 'NONE',  ( 19.99999999999999645, 0.000000000000000000, 0.000000000000000000 ) ) ;
#797=VECTOR ( 'NONE', #13935, 1000.000000000000000 ) ;
#799=EDGE_CURVE ( 'NONE', #18653, #12132, #3118, .T. ) ;
#802=DIRECTION ( 'NONE',  ( 0.000000000000000000, -0.7308359642781301346, 0.6825531432186475733 ) ) ;
#805=AXIS2_PLACEMENT_3D ( 'NONE', #12015, #3844, #1003 ) ;
#806=CYLINDRICAL_SURFACE ( 'NONE', #17716, 72.00000000007199219 ) ;
#812=CIRCLE ( 'NONE', #14370, 72.00000000007199219 ) ;
#814=AXIS2_PLACEMENT_3D ( 'NONE', #311, #5176, #18637 ) ;
#815=ORIENTED_EDGE ( 'NONE', *, *, #9394, .T. ) ;
#816=LINE ( 'NONE', #10243, #8539 ) ;
#822=DIRECTION ( 'NONE',  ( -1.000000000000000000, 0.000000000000000000, 0.000000000000000000 ) ) ;
#826=DIRECTION ( 'NONE',  ( -1.000000000000000000, 0.000000000000000000, 0.000000000000000000 ) ) ;
#827=AXIS2_PLACEMENT_3D ( 'NONE', #10753, #14041, #6069 ) ;
#828=ORIENTED_EDGE ( 'NONE', *, *, #1732, .T. ) ;
#833=VERTEX_POINT ( 'NONE', #18577 ) ;
#835=DIRECTION ( 'NONE',  ( -1.000000000000000000, -0.000000000000000000, 0.000000000000000000 ) ) ;
#836=VECTOR ( 'NONE', #4368, 1000.000000000000000 ) ;
#838=DIRECTION ( 'NONE',  ( -1.000000000000000000, -0.000000000000000000, -0.000000000000000000 ) ) ;
#841=CYLINDRICAL_SURFACE ( 'NONE', #7833, 27.60000000002760245 ) ;
#846=CARTESIAN_POINT ( 'NONE',  ( 9.999999999999998224, -36.59093685910587368, -62.00889726308067651 ) ) ;
#851=CARTESIAN_POINT ( 'NONE',  ( 9.999999999999998224, -67.51707036274397922, -25.00890260772446894 ) ) ;
#852=ORIENTED_EDGE ( 'NONE', *, *, #20744, .T. ) ;
#853=CARTESIAN_POINT ( 'NONE',  ( 85.00002539999999840, 0.000000000000000000, 0.000000000000000000 ) ) ;
#854=EDGE_LOOP ( 'NONE', ( #53, #3141, #1269, #10123 ) ) ;
#857=VERTEX_POINT ( 'NONE', #10629 ) ;
#859=CIRCLE ( 'NONE', #9469, 65.24900000006526568 ) ;
#862=CARTESIAN_POINT ( 'NONE',  ( -10.00000000000000000, 0.000000000000000000, 0.000000000000000000 ) ) ;
#863=AXIS2_PLACEMENT_3D ( 'NONE', #4172, #11904, #3847 ) ;
#864=LINE ( 'NONE', #6900, #20781 ) ;
#867=DIRECTION ( 'NONE',  ( -1.000000000000000000, 0.000000000000000000, 0.000000000000000000 ) ) ;
#868=CYLINDRICAL_SURFACE ( 'NONE', #16265, 27.60000000002759890 ) ;
#870=CARTESIAN_POINT ( 'NONE',  ( 0.000000000000000000, 8.857208570069802889, 71.45313048675089362 ) ) ;
#879=CYLINDRICAL_SURFACE ( 'NONE', #19072, 72.00000000007199219 ) ;
#893=CARTESIAN_POINT ( 'NONE',  ( 19.99999999999999645, 0.000000000000000000, 0.000000000000000000 ) ) ;
#897=CIRCLE ( 'NONE', #7709, 27.60000000002759535 ) ;
#899=CYLINDRICAL_SURFACE ( 'NONE', #11693, 27.60000000002759890 ) ;
#908=ORIENTED_EDGE ( 'NONE', *, *, #8321, .T. ) ;
#910=AXIS2_PLACEMENT_3D ( 'NONE', #8362, #2107, #19388 ) ;
#915=CIRCLE ( 'NONE', #3928, 27.60000000002759535 ) ;
#917=ADVANCED_FACE ( 'NONE', ( #7647 ), #16971, .T. ) ;
#918=DIRECTION ( 'NONE',  ( -1.000000000000000000, 0.000000000000000000, 0.000000000000000000 ) ) ;
#923=ORIENTED_EDGE ( 'NONE', *, *, #7287, .F. ) ;
#925=ADVANCED_FACE ( 'NONE', ( #12205 ), #9036, .T. ) ;
#932=CARTESIAN_POINT ( 'NONE',  ( 0.000000000000000000, -28.84646472442495480, 58.52617768068423487 ) ) ;
#934=EDGE_CURVE ( 'NONE', #273, #10935, #17300, .T. ) ;
#936=LINE ( 'NONE', #1034, #3948 ) ;
#938=VECTOR ( 'NONE', #2750, 1000.000000000000000 ) ;
#939=VERTEX_POINT ( 'NONE', #17201 ) ;
#941=ORIENTED_EDGE ( 'NONE', *, *, #9394, .F. ) ;
#946=EDGE_LOOP ( 'NONE', ( #5356, #19237, #20255, #9417 ) ) ;
#948=CARTESIAN_POINT ( 'NONE',  ( 19.99999999999999645, -59.31169354540720207, -27.19476070466916795 ) ) ;
#950=CARTESIAN_POINT ( 'NONE',  ( 0.000000000000000000, -58.26603306961992956, 42.29739224042451440 ) ) ;
#951=CARTESIAN_POINT ( 'NONE',  ( 19.99999999999999645, 10.77748419466781726, -63.93680186330462334 ) ) ;
#956=ADVANCED_FACE ( 'NONE', ( #9136 ), #20672, .T. ) ;
#962=EDGE_CURVE ( 'NONE', #13763, #5564, #20472, .T. ) ;
#963=CYLINDRICAL_SURFACE ( 'NONE', #14801, 4.000000000000000000 ) ;
#965=DIRECTION ( 'NONE',  ( -1.000000000000000000, -0.000000000000000000, -0.000000000000000000 ) ) ;
#969=DIRECTION ( 'NONE',  ( 0.000000000000000000, 0.000000000000000000, 1.000000000000000000 ) ) ;
#970=ORIENTED_EDGE ( 'NONE', *, *, #1090, .T. ) ;
#972=DIRECTION ( 'NONE',  ( 1.000000000000000000, -0.000000000000000000, -0.000000000000000000 ) ) ;
#973=ORIENTED_EDGE ( 'NONE', *, *, #11043, .T. ) ;
#974=ORIENTED_EDGE ( 'NONE', *, *, #9877, .F. ) ;
#976=EDGE_CURVE ( 'NONE', #1075, #15567, #19684, .T. ) ;
#978=EDGE_CURVE ( 'NONE', #11163, #4471, #17333, .T. ) ;
#979=DIRECTION ( 'NONE',  ( 0.000000000000000000, 0.000000000000000000, 1.000000000000000000 ) ) ;
#984=DIRECTION ( 'NONE',  ( -1.000000000000000000, -0.000000000000000000, 0.000000000000000000 ) ) ;
#985=ORIENTED_EDGE ( 'NONE', *, *, #409, .T. ) ;
#986=EDGE_CURVE ( 'NONE', #3717, #7729, #20374, .T. ) ;
#987=DIRECTION ( 'NONE',  ( -1.000000000000000000, -0.000000000000000000, -0.000000000000000000 ) ) ;
#992=CARTESIAN_POINT ( 'NONE',  ( 85.00002539999999840, 0.000000000000000000, 1.000000000000000000 ) ) ;
#997=ORIENTED_EDGE ( 'NONE', *, *, #9866, .T. ) ;
#1000=DIRECTION ( 'NONE',  ( 0.000000000000000000, 0.000000000000000000, -1.000000000000000000 ) ) ;
#1002=CARTESIAN_POINT ( 'NONE',  ( 19.99999999999999645, 0.000000000000000000, 0.000000000000000000 ) ) ;
#1003=DIRECTION ( 'NONE',  ( 0.000000000000000000, 0.000000000000000000, 1.000000000000000000 ) ) ;
#1004=ORIENTED_EDGE ( 'NONE', *, *, #9228, .F. ) ;
#1007=CARTESIAN_POINT ( 'NONE',  ( 19.99999999999999645, 56.63599015375672963, 31.56633360682482703 ) ) ;
#1010=EDGE_LOOP ( 'NONE', ( #1177, #17232, #20244, #6388 ) ) ;
#1013=CARTESIAN_POINT ( 'NONE',  ( 19.99999999999999645, -19.38316218894255627, 61.87375713200982119 ) ) ;
#1015=EDGE_LOOP ( 'NONE', ( #7142, #11524, #9589, #1232 ) ) ;
#1016=DIRECTION ( 'NONE',  ( 0.000000000000000000, 0.000000000000000000, 1.000000000000000000 ) ) ;
#1017=ORIENTED_EDGE ( 'NONE', *, *, #9002, .F. ) ;
#1018=DIRECTION ( 'NONE',  ( 0.000000000000000000, 0.000000000000000000, 1.000000000000000000 ) ) ;
#1019=ORIENTED_EDGE ( 'NONE', *, *, #7241, .F. ) ;
#1024=ADVANCED_FACE ( 'NONE', ( #12950 ), #10, .T. ) ;
#1028=ORIENTED_EDGE ( 'NONE', *, *, #9501, .F. ) ;
#1029=LINE ( 'NONE', #7476, #16566 ) ;
#1034=CARTESIAN_POINT ( 'NONE',  ( 19.99999999999999645, -56.42118728228177105, 32.77318456705422278 ) ) ;
#1036=AXIS2_PLACEMENT_3D ( 'NONE', #5114, #5025, #13402 ) ;
#1039=ADVANCED_FACE ( 'NONE', ( #3196 ), #1713, .T. ) ;
#1040=CARTESIAN_POINT ( 'NONE',  ( 0.000000000000000000, -46.17500197033020015, -55.24372537266445704 ) ) ;
#1044=ORIENTED_EDGE ( 'NONE', *, *, #7397, .F. ) ;
#1045=ORIENTED_EDGE ( 'NONE', *, *, #12467, .F. ) ;
#1047=CARTESIAN_POINT ( 'NONE',  ( 0.000000000000000000, 38.22257254261821657, -61.01667762370101400 ) ) ;
#1050=DIRECTION ( 'NONE',  ( 0.000000000000000000, 0.000000000000000000, 1.000000000000000000 ) ) ;
#1053=ADVANCED_FACE ( 'NONE', ( #11041 ), #19206, .T. ) ;
#1064=CARTESIAN_POINT ( 'NONE',  ( 0.000000000000000000, 31.98952867950324830, 56.39803944231596944 ) ) ;
#1067=DIRECTION ( 'NONE',  ( -1.000000000000000000, -0.000000000000000000, -0.000000000000000000 ) ) ;
#1068=AXIS2_PLACEMENT_3D ( 'NONE', #11739, #18208, #9405 ) ;
#1070=DIRECTION ( 'NONE',  ( -1.000000000000000000, -0.000000000000000000, 0.000000000000000000 ) ) ;
#1072=ADVANCED_FACE ( 'NONE', ( #6572 ), #9550, .T. ) ;
#1075=VERTEX_POINT ( 'NONE', #2991 ) ;
#1079=DIRECTION ( 'NONE',  ( -1.000000000000000000, 0.000000000000000000, 0.000000000000000000 ) ) ;
#1083=AXIS2_PLACEMENT_3D ( 'NONE', #14869, #8398, #3931 ) ;
#1085=DIRECTION ( 'NONE',  ( 0.000000000000000000, 0.000000000000000000, 1.000000000000000000 ) ) ;
#1089=DIRECTION ( 'NONE',  ( -1.000000000000000000, 0.000000000000000000, 0.000000000000000000 ) ) ;
#1090=EDGE_CURVE ( 'NONE', #9449, #20554, #16633, .T. ) ;
#1093=ORIENTED_EDGE ( 'NONE', *, *, #16885, .F. ) ;
#1095=CARTESIAN_POINT ( 'NONE',  ( 9.999999999999998224, 58.26603306961963824, 42.29739224042493362 ) ) ;
#1098=CARTESIAN_POINT ( 'NONE',  ( 0.000000000000000000, 0.000000000000000000, 0.000000000000000000 ) ) ;
#1099=VERTEX_POINT ( 'NONE', #18442 ) ;
#1104=ORIENTED_EDGE ( 'NONE', *, *, #20743, .F. ) ;
#1106=AXIS2_PLACEMENT_3D ( 'NONE', #20639, #6117, #6226 ) ;
#1109=CYLINDRICAL_SURFACE ( 'NONE', #5621, 65.24900000006525147 ) ;
#1114=DIRECTION ( 'NONE',  ( 0.000000000000000000, 0.000000000000000000, 1.000000000000000000 ) ) ;
#1117=AXIS2_PLACEMENT_3D ( 'NONE', #10896, #20640, #17584 ) ;
#1119=LINE ( 'NONE', #20388, #2474 ) ;
#1120=VECTOR ( 'NONE', #11332, 1000.000000000000000 ) ;
#1121=ORIENTED_EDGE ( 'NONE', *, *, #14490, .T. ) ;
#1124=VECTOR ( 'NONE', #2201, 1000.000000000000000 ) ;
#1125=CARTESIAN_POINT ( 'NONE',  ( -65.00002539999999840, 0.000000000000000000, 0.000000000000000000 ) ) ;
#1128=CARTESIAN_POINT ( 'NONE',  ( 19.99999999999999645, -8.857208570070305598, 71.45313048675082257 ) ) ;
#1129=ORIENTED_EDGE ( 'NONE', *, *, #7364, .T. ) ;
#1130=FACE_OUTER_BOUND ( 'NONE', #6284, .T. ) ;
#1137=ORIENTED_EDGE ( 'NONE', *, *, #15695, .T. ) ;
#1138=CARTESIAN_POINT ( 'NONE',  ( 0.000000000000000000, 0.000000000000000000, 0.000000000000000000 ) ) ;
#1142=CIRCLE ( 'NONE', #12662, 65.24900000006525147 ) ;
#1144=DIRECTION ( 'NONE',  ( -1.000000000000000000, 0.000000000000000000, 0.000000000000000000 ) ) ;
#1145=LINE ( 'NONE', #18944, #6305 ) ;
#1147=CIRCLE ( 'NONE', #8224, 72.00000000007199219 ) ;
#1148=ORIENTED_EDGE ( 'NONE', *, *, #5311, .F. ) ;
#1151=ORIENTED_EDGE ( 'NONE', *, *, #17537, .T. ) ;
#1152=CARTESIAN_POINT ( 'NONE',  ( 0.000000000000000000, 0.000000000000000000, 0.000000000000000000 ) ) ;
#1156=ORIENTED_EDGE ( 'NONE', *, *, #6424, .T. ) ;
#1159=AXIS2_PLACEMENT_3D ( 'NONE', #14472, #7776, #9575 ) ;
#1160=CARTESIAN_POINT ( 'NONE',  ( 0.000000000000000000, 0.000000000000000000, 0.000000000000000000 ) ) ;
#1161=EDGE_CURVE ( 'NONE', #7789, #5332, #14980, .T. ) ;
#1162=CARTESIAN_POINT ( 'NONE',  ( 0.000000000000000000, 36.54710069451054011, 54.05313526368126276 ) ) ;
#1166=AXIS2_PLACEMENT_3D ( 'NONE', #9873, #14559, #8482 ) ;
#1172=DIRECTION ( 'NONE',  ( -1.000000000000000000, -0.000000000000000000, 0.000000000000000000 ) ) ;
#1177=ORIENTED_EDGE ( 'NONE', *, *, #15640, .F. ) ;
#1181=AXIS2_PLACEMENT_3D ( 'NONE', #6590, #9881, #17748 ) ;
#1182=VERTEX_POINT ( 'NONE', #11768 ) ;
#1184=ORIENTED_EDGE ( 'NONE', *, *, #15598, .T. ) ;
#1193=EDGE_CURVE ( 'NONE', #10244, #7176, #5295, .T. ) ;
#1199=ORIENTED_EDGE ( 'NONE', *, *, #18611, .F. ) ;
#1201=ORIENTED_EDGE ( 'NONE', *, *, #13871, .T. ) ;
#1207=ORIENTED_EDGE ( 'NONE', *, *, #18193, .F. ) ;
#1208=DIRECTION ( 'NONE',  ( 0.000000000000000000, 0.000000000000000000, 1.000000000000000000 ) ) ;
#1217=LINE ( 'NONE', #7663, #17114 ) ;
#1220=CARTESIAN_POINT ( 'NONE',  ( 0.000000000000000000, 0.000000000000000000, 0.000000000000000000 ) ) ;
#1229=CARTESIAN_POINT ( 'NONE',  ( 19.99999999999999645, 56.42118728228154367, 32.77318456705460648 ) ) ;
#1230=VECTOR ( 'NONE', #984, 1000.000000000000000 ) ;
#1231=ADVANCED_FACE ( 'NONE', ( #6774 ), #15157, .T. ) ;
#1232=ORIENTED_EDGE ( 'NONE', *, *, #1161, .T. ) ;
#1237=CARTESIAN_POINT ( 'NONE',  ( 19.99999999999999645, -56.42118728228177105, 32.77318456705422278 ) ) ;
#1240=EDGE_LOOP ( 'NONE', ( #13575, #8868, #19150, #7093 ) ) ;
#1243=EDGE_CURVE ( 'NONE', #5717, #20215, #4131, .T. ) ;
#1244=AXIS2_PLACEMENT_3D ( 'NONE', #4937, #17777, #277 ) ;
#1250=CARTESIAN_POINT ( 'NONE',  ( -10.00000000000000000, 0.000000000000000000, 0.000000000000000000 ) ) ;
#1251=ORIENTED_EDGE ( 'NONE', *, *, #20171, .F. ) ;
#1253=AXIS2_PLACEMENT_3D ( 'NONE', #309, #11755, #18221 ) ;
#1255=AXIS2_PLACEMENT_3D ( 'NONE', #12708, #4424, #4330 ) ;
#1257=CYLINDRICAL_SURFACE ( 'NONE', #17485, 72.00000000007199219 ) ;
#1258=CIRCLE ( 'NONE', #6320, 65.24900000006525147 ) ;
#1261=EDGE_CURVE ( 'NONE', #9697, #4217, #5473, .T. ) ;
#1268=CIRCLE ( 'NONE', #18495, 27.60000000002759890 ) ;
#1269=ORIENTED_EDGE ( 'NONE', *, *, #18258, .T. ) ;
#1270=DIRECTION ( 'NONE',  ( -1.000000000000000000, -0.000000000000000000, 0.000000000000000000 ) ) ;
#1271=DIRECTION ( 'NONE',  ( 0.000000000000000000, 0.000000000000000000, 1.000000000000000000 ) ) ;
#1281=DIRECTION ( 'NONE',  ( 1.000000000000000000, 0.000000000000000000, 0.000000000000000000 ) ) ;
#1287=AXIS2_PLACEMENT_3D ( 'NONE', #1447, #15948, #11287 ) ;
#1291=DIRECTION ( 'NONE',  ( -1.000000000000000000, -0.000000000000000000, 0.000000000000000000 ) ) ;
#1292=CIRCLE ( 'NONE', #2284, 72.00000000007199219 ) ;
#1293=ORIENTED_EDGE ( 'NONE', *, *, #10415, .F. ) ;
#1294=CARTESIAN_POINT ( 'NONE',  ( 0.000000000000000000, -70.68211945903199478, 13.71269443944184196 ) ) ;
#1295=FACE_OUTER_BOUND ( 'NONE', #6113, .T. ) ;
#1297=ORIENTED_EDGE ( 'NONE', *, *, #3568, .T. ) ;
#1304=DIRECTION ( 'NONE',  ( -1.000000000000000000, 0.000000000000000000, -0.000000000000000000 ) ) ;
#1309=EDGE_LOOP ( 'NONE', ( #5582, #5255, #19087, #7565 ) ) ;
#1315=LINE ( 'NONE', #992, #18069 ) ;
#1321=DIRECTION ( 'NONE',  ( -1.000000000000000000, -0.000000000000000000, 0.000000000000000000 ) ) ;
#1328=EDGE_CURVE ( 'NONE', #10217, #3338, #17694, .T. ) ;
#1329=ORIENTED_EDGE ( 'NONE', *, *, #17632, .F. ) ;
#1330=DIRECTION ( 'NONE',  ( 1.000000000000000000, -0.000000000000000000, 0.000000000000000000 ) ) ;
#1331=DIRECTION ( 'NONE',  ( 0.000000000000000000, 0.000000000000000000, 1.000000000000000000 ) ) ;
#1335=ORIENTED_EDGE ( 'NONE', *, *, #13765, .F. ) ;
#1339=ORIENTED_EDGE ( 'NONE', *, *, #16121, .F. ) ;
#1341=CARTESIAN_POINT ( 'NONE',  ( 19.99999999999999645, -63.05226888949902531, 15.11556105343437828 ) ) ;
#1343=DIRECTION ( 'NONE',  ( -1.000000000000000000, 0.000000000000000000, 0.000000000000000000 ) ) ;
#1344=ORIENTED_EDGE ( 'NONE', *, *, #20119, .T. ) ;
#1362=LINE ( 'NONE', #20629, #12090 ) ;
#1365=CARTESIAN_POINT ( 'NONE',  ( 0.000000000000000000, 46.17500197033058384, 55.24372537266413730 ) ) ;
#1368=EDGE_CURVE ( 'NONE', #14689, #5761, #15305, .T. ) ;
#1369=VERTEX_POINT ( 'NONE', #15252 ) ;
#1371=DIRECTION ( 'NONE',  ( 0.000000000000000000, -0.8169698930104354329, -0.5766803221148765202 ) ) ;
#1378=CARTESIAN_POINT ( 'NONE',  ( 0.000000000000000000, 0.000000000000000000, 0.000000000000000000 ) ) ;
#1385=CARTESIAN_POINT ( 'NONE',  ( 19.99999999999999645, 0.000000000000000000, 0.000000000000000000 ) ) ;
#1387=CYLINDRICAL_SURFACE ( 'NONE', #406, 65.24900000006525147 ) ;
#1388=ORIENTED_EDGE ( 'NONE', *, *, #9463, .T. ) ;
#1389=CARTESIAN_POINT ( 'NONE',  ( 0.000000000000000000, -15.58726123847893774, 62.93731870009398932 ) ) ;
#1390=CARTESIAN_POINT ( 'NONE',  ( 0.000000000000000000, -46.17500197033096754, 55.24372537266381755 ) ) ;
#1392=ORIENTED_EDGE ( 'NONE', *, *, #18298, .T. ) ;
#1395=AXIS2_PLACEMENT_3D ( 'NONE', #1849, #6710, #13290 ) ;
#1397=ADVANCED_FACE ( 'NONE', ( #17382 ), #12291, .T. ) ;
#1403=FACE_OUTER_BOUND ( 'NONE', #10542, .T. ) ;
#1411=VERTEX_POINT ( 'NONE', #7508 ) ;
#1412=DIRECTION ( 'NONE',  ( -1.000000000000000000, -0.000000000000000000, 0.000000000000000000 ) ) ;
#1413=ORIENTED_EDGE ( 'NONE', *, *, #9828, .T. ) ;
#1415=LINE ( 'NONE', #20481, #13457 ) ;
#1417=ORIENTED_EDGE ( 'NONE', *, *, #12888, .T. ) ;
#1418=DIRECTION ( 'NONE',  ( -1.000000000000000000, 0.000000000000000000, 0.000000000000000000 ) ) ;
#1420=CARTESIAN_POINT ( 'NONE',  ( 0.000000000000000000, -14.55863677812166124, 63.60407295269099137 ) ) ;
#1421=CIRCLE ( 'NONE', #15324, 72.00000000007199219 ) ;
#1425=VECTOR ( 'NONE', #15655, 1000.000000000000000 ) ;
#1429=VERTEX_POINT ( 'NONE', #17174 ) ;
#1432=ADVANCED_FACE ( 'NONE', ( #2657 ), #15568, .T. ) ;
#1434=DIRECTION ( 'NONE',  ( -1.000000000000000000, -0.000000000000000000, -0.000000000000000000 ) ) ;
#1437=VECTOR ( 'NONE', #5990, 1000.000000000000000 ) ;
#1439=AXIS2_PLACEMENT_3D ( 'NONE', #1624, #11245, #8269 ) ;
#1440=DIRECTION ( 'NONE',  ( 0.000000000000000000, 0.7308359642781206977, 0.6825531432186578984 ) ) ;
#1446=EDGE_CURVE ( 'NONE', #2775, #12799, #7943, .T. ) ;
#1447=CARTESIAN_POINT ( 'NONE',  ( 19.99999999999999645, -24.01204443665229604, 60.22865198596116443 ) ) ;
#1448=DIRECTION ( 'NONE',  ( -1.000000000000000000, -0.000000000000000000, 0.000000000000000000 ) ) ;
#1451=VECTOR ( 'NONE', #2646, 1000.000000000000000 ) ;
#1452=AXIS2_PLACEMENT_3D ( 'NONE', #4891, #4778, #12644 ) ;
#1457=ORIENTED_EDGE ( 'NONE', *, *, #16113, .F. ) ;
#1458=ADVANCED_FACE ( 'NONE', ( #8139 ), #20860, .T. ) ;
#1459=EDGE_CURVE ( 'NONE', #8383, #8626, #18037, .T. ) ;
#1464=ADVANCED_FACE ( 'NONE', ( #14613 ), #19375, .T. ) ;
#1467=ADVANCED_FACE ( 'NONE', ( #12829 ), #6545, .T. ) ;
#1469=AXIS2_PLACEMENT_3D ( 'NONE', #18399, #13530, #5455 ) ;
#1476=ORIENTED_EDGE ( 'NONE', *, *, #20774, .F. ) ;
#1481=EDGE_CURVE ( 'NONE', #18587, #17728, #20405, .T. ) ;
#1484=EDGE_CURVE ( 'NONE', #18498, #3220, #443, .T. ) ;
#1487=FACE_BOUND ( 'NONE', #13030, .T. ) ;
#1488=AXIS2_PLACEMENT_3D ( 'NONE', #350, #19238, #4715 ) ;
#1490=EDGE_CURVE ( 'NONE', #9017, #17731, #20650, .T. ) ;
#1497=ORIENTED_EDGE ( 'NONE', *, *, #14164, .F. ) ;
#1500=ORIENTED_EDGE ( 'NONE', *, *, #19442, .T. ) ;
#1503=ORIENTED_EDGE ( 'NONE', *, *, #2780, .T. ) ;
#1507=CIRCLE ( 'NONE', #3494, 27.60000000002759535 ) ;
#1509=CARTESIAN_POINT ( 'NONE',  ( 19.99999999999999645, -42.42902769288503606, -49.02903636734241388 ) ) ;
#1515=CARTESIAN_POINT ( 'NONE',  ( 0.000000000000000000, 0.000000000000000000, 0.000000000000000000 ) ) ;
#1517=AXIS2_PLACEMENT_3D ( 'NONE', #7998, #14477, #2807 ) ;
#1518=VERTEX_POINT ( 'NONE', #17804 ) ;
#1519=CARTESIAN_POINT ( 'NONE',  ( 19.99999999999999645, 15.58726123847937828, -62.93731870009387563 ) ) ;
#1524=CARTESIAN_POINT ( 'NONE',  ( 0.000000000000000000, 0.000000000000000000, 0.000000000000000000 ) ) ;
#1529=EDGE_CURVE ( 'NONE', #14269, #13959, #7882, .T. ) ;
#1530=AXIS2_PLACEMENT_3D ( 'NONE', #13066, #19523, #12966 ) ;
#1531=ORIENTED_EDGE ( 'NONE', *, *, #2872, .F. ) ;
#1538=CARTESIAN_POINT ( 'NONE',  ( 0.000000000000000000, -55.05624179292004072, 35.01774179823764399 ) ) ;
#1539=VERTEX_POINT ( 'NONE', #14206 ) ;
#1541=CARTESIAN_POINT ( 'NONE',  ( 0.000000000000000000, 64.79224928664392280, -2.456263514197840614 ) ) ;
#1542=DIRECTION ( 'NONE',  ( -1.000000000000000000, -0.000000000000000000, -0.000000000000000000 ) ) ;
#1549=ORIENTED_EDGE ( 'NONE', *, *, #18148, .T. ) ;
#1552=ADVANCED_FACE ( 'NONE', ( #6132 ), #11012, .T. ) ;
#1553=VERTEX_POINT ( 'NONE', #6240 ) ;
#1555=EDGE_CURVE ( 'NONE', #6474, #18397, #14521, .T. ) ;
#1559=CIRCLE ( 'NONE', #12741, 27.60000000002760245 ) ;
#1570=DIRECTION ( 'NONE',  ( -1.000000000000000000, 0.000000000000000000, -0.000000000000000000 ) ) ;
#1574=FACE_OUTER_BOUND ( 'NONE', #17556, .T. ) ;
#1576=ORIENTED_EDGE ( 'NONE', *, *, #7144, .F. ) ;
#1586=CARTESIAN_POINT ( 'NONE',  ( 0.000000000000000000, 64.79224928664392280, -2.456263514197840614 ) ) ;
#1587=EDGE_CURVE ( 'NONE', #17270, #8626, #15654, .T. ) ;
#1589=AXIS2_PLACEMENT_3D ( 'NONE', #13396, #14977, #3419 ) ;
#1594=CARTESIAN_POINT ( 'NONE',  ( 150.0000507999999968, 5.400000000000000355, -1.000000000000000000 ) ) ;
#1597=FACE_OUTER_BOUND ( 'NONE', #513, .T. ) ;
#1600=CARTESIAN_POINT ( 'NONE',  ( 0.000000000000000000, 0.000000000000000000, 0.000000000000000000 ) ) ;
#1602=EDGE_LOOP ( 'NONE', ( #19739, #6514, #5985, #17463 ) ) ;
#1603=DIRECTION ( 'NONE',  ( 0.000000000000000000, -0.3984010898462485573, 0.9172113015054500496 ) ) ;
#1607=VERTEX_POINT ( 'NONE', #11521 ) ;
#1608=DIRECTION ( 'NONE',  ( -1.000000000000000000, 0.000000000000000000, -0.000000000000000000 ) ) ;
#1609=EDGE_CURVE ( 'NONE', #9297, #4671, #18361, .T. ) ;
#1610=STYLED_ITEM ( 'NONE', ( #17077 ), #19794 ) ;
#1611=EDGE_CURVE ( 'NONE', #8077, #16773, #5553, .T. ) ;
#1617=AXIS2_PLACEMENT_3D ( 'NONE', #8638, #6834, #18196 ) ;
#1621=AXIS2_PLACEMENT_3D ( 'NONE', #10484, #20229, #7617 ) ;
#1622=EDGE_LOOP ( 'NONE', ( #15502, #16307, #20064, #1757 ) ) ;
#1624=CARTESIAN_POINT ( 'NONE',  ( 0.000000000000000000, 0.000000000000000000, 0.000000000000000000 ) ) ;
#1627=CARTESIAN_POINT ( 'NONE',  ( 0.000000000000000000, 3.141410481201988070, -65.17333458706183080 ) ) ;
#1628=VERTEX_POINT ( 'NONE', #3966 ) ;
#1630=DIRECTION ( 'NONE',  ( 0.000000000000000000, 0.000000000000000000, -1.000000000000000000 ) ) ;
#1632=EDGE_CURVE ( 'NONE', #3634, #12603, #12137, .T. ) ;
#1636=CIRCLE ( 'NONE', #9062, 27.60000000002759890 ) ;
#1640=ADVANCED_FACE ( 'NONE', ( #6651 ), #8838, .T. ) ;
#1641=CARTESIAN_POINT ( 'NONE',  ( 0.000000000000000000, -46.01927912072559224, 45.67597560296373871 ) ) ;
#1644=VERTEX_POINT ( 'NONE', #15313 ) ;
#1653=DIRECTION ( 'NONE',  ( 0.000000000000000000, -0.8878852184023795502, 0.4600650377311439332 ) ) ;
#1654=ORIENTED_EDGE ( 'NONE', *, *, #18193, .T. ) ;
#1662=ADVANCED_FACE ( 'NONE', ( #13136 ), #10549, .T. ) ;
#1665=EDGE_CURVE ( 'NONE', #13788, #3825, #18718, .T. ) ;
#1667=EDGE_LOOP ( 'NONE', ( #13083, #11527, #16791, #852 ) ) ;
#1670=LINE ( 'NONE', #9006, #11754 ) ;
#1672=EDGE_LOOP ( 'NONE', ( #10230, #4922, #16912, #8374 ) ) ;
#1676=DIRECTION ( 'NONE',  ( 0.000000000000000000, 0.3984010898462422290, -0.9172113015054527141 ) ) ;
#1678=ORIENTED_EDGE ( 'NONE', *, *, #17127, .F. ) ;
#1679=ADVANCED_FACE ( 'NONE', ( #20071 ), #8955, .T. ) ;
#1680=DIRECTION ( 'NONE',  ( -1.000000000000000000, 0.000000000000000000, 0.000000000000000000 ) ) ;
#1684=VERTEX_POINT ( 'NONE', #15421 ) ;
#1692=CARTESIAN_POINT ( 'NONE',  ( 0.000000000000000000, 0.000000000000000000, 0.000000000000000000 ) ) ;
#1693=DIRECTION ( 'NONE',  ( -1.000000000000000000, 0.000000000000000000, -0.000000000000000000 ) ) ;
#1696=CARTESIAN_POINT ( 'NONE',  ( 0.000000000000000000, -71.89099403602352822, -3.960426305689553228 ) ) ;
#1697=ORIENTED_EDGE ( 'NONE', *, *, #10399, .T. ) ;
#1700=ORIENTED_EDGE ( 'NONE', *, *, #1882, .T. ) ;
#1701=DIRECTION ( 'NONE',  ( -1.000000000000000000, 0.000000000000000000, 0.000000000000000000 ) ) ;
#1704=CARTESIAN_POINT ( 'NONE',  ( 19.99999999999999645, 36.54710069451054011, 54.05313526368126276 ) ) ;
#1706=CYLINDRICAL_SURFACE ( 'NONE', #19725, 72.00000000007199219 ) ;
#1713=CYLINDRICAL_SURFACE ( 'NONE', #1452, 27.60000000002759535 ) ;
#1714=EDGE_CURVE ( 'NONE', #12603, #20554, #11925, .T. ) ;
#1720=CARTESIAN_POINT ( 'NONE',  ( 9.999999999999998224, 59.36728637278019960, 40.73727173906807764 ) ) ;
#1722=EDGE_CURVE ( 'NONE', #18079, #19080, #12964, .T. ) ;
#1727=CYLINDRICAL_SURFACE ( 'NONE', #9639, 27.60000000002759890 ) ;
#1731=ORIENTED_EDGE ( 'NONE', *, *, #18227, .F. ) ;
#1732=EDGE_CURVE ( 'NONE', #17728, #18597, #14993, .T. ) ;
#1733=FACE_OUTER_BOUND ( 'NONE', #10053, .T. ) ;
#1736=DIRECTION ( 'NONE',  ( -1.000000000000000000, -0.000000000000000000, -0.000000000000000000 ) ) ;
#1738=ORIENTED_EDGE ( 'NONE', *, *, #7506, .T. ) ;
#1742=CARTESIAN_POINT ( 'NONE',  ( 19.99999999999999645, 64.44931368725534071, -10.18420179740539666 ) ) ;
#1743=ORIENTED_EDGE ( 'NONE', *, *, #9744, .F. ) ;
#1744=DIRECTION ( 'NONE',  ( -1.000000000000000000, 0.000000000000000000, 0.000000000000000000 ) ) ;
#1746=FACE_OUTER_BOUND ( 'NONE', #19191, .T. ) ;
#1747=VERTEX_POINT ( 'NONE', #19026 ) ;
#1750=FACE_OUTER_BOUND ( 'NONE', #13395, .T. ) ;
#1751=CARTESIAN_POINT ( 'NONE',  ( 9.999999999999998224, -70.68211945903199478, 13.71269443944183841 ) ) ;
#1754=ORIENTED_EDGE ( 'NONE', *, *, #11106, .T. ) ;
#1756=CARTESIAN_POINT ( 'NONE',  ( 9.999999999999998224, -70.29359119158475266, -15.58239511117358589 ) ) ;
#1757=ORIENTED_EDGE ( 'NONE', *, *, #3867, .T. ) ;
#1758=AXIS2_PLACEMENT_3D ( 'NONE', #7578, #6086, #17759 ) ;
#1759=DIRECTION ( 'NONE',  ( -1.000000000000000000, -0.000000000000000000, -0.000000000000000000 ) ) ;
#1762=AXIS2_PLACEMENT_3D ( 'NONE', #20211, #11949, #10154 ) ;
#1766=CARTESIAN_POINT ( 'NONE',  ( 19.99999999999999645, 43.56693332842786504, 48.57318520917521454 ) ) ;
#1771=ADVANCED_FACE ( 'NONE', ( #6192 ), #10770, .T. ) ;
#1772=VERTEX_POINT ( 'NONE', #1237 ) ;
#1774=CIRCLE ( 'NONE', #2443, 27.60000000002760245 ) ;
#1777=VECTOR ( 'NONE', #541, 1000.000000000000000 ) ;
#1780=PLANE ( 'NONE',  #10621 ) ;
#1784=AXIS2_PLACEMENT_3D ( 'NONE', #16285, #15014, #13323 ) ;
#1785=CIRCLE ( 'NONE', #4495, 27.60000000002759890 ) ;
#1786=ORIENTED_EDGE ( 'NONE', *, *, #13103, .F. ) ;
#1793=VERTEX_POINT ( 'NONE', #5987 ) ;
#1795=CARTESIAN_POINT ( 'NONE',  ( 85.00002539999999840, 5.400000000000000355, -1.000000000000000000 ) ) ;
#1796=EDGE_CURVE ( 'NONE', #4998, #13929, #18712, .T. ) ;
#1797=EDGE_LOOP ( 'NONE', ( #3719, #7779, #12178, #4788 ) ) ;
#1801=FACE_OUTER_BOUND ( 'NONE', #11292, .T. ) ;
#1805=CIRCLE ( 'NONE', #15690, 27.60000000002759890 ) ;
#1807=AXIS2_PLACEMENT_3D ( 'NONE', #1341, #10861, #15626 ) ;
#1813=FACE_OUTER_BOUND ( 'NONE', #439, .T. ) ;
#1815=DIRECTION ( 'NONE',  ( 0.000000000000000000, 0.000000000000000000, 1.000000000000000000 ) ) ;
#1820=AXIS2_PLACEMENT_3D ( 'NONE', #15711, #20585, #1208 ) ;
#1822=VERTEX_POINT ( 'NONE', #15941 ) ;
#1823=DIRECTION ( 'NONE',  ( -1.000000000000000000, 0.000000000000000000, 0.000000000000000000 ) ) ;
#1826=ORIENTED_EDGE ( 'NONE', *, *, #8476, .T. ) ;
#1830=AXIS2_PLACEMENT_3D ( 'NONE', #13244, #4984, #17710 ) ;
#1831=EDGE_CURVE ( 'NONE', #1822, #15515, #1785, .T. ) ;
#1834=CIRCLE ( 'NONE', #4542, 27.60000000002759890 ) ;
#1837=CARTESIAN_POINT ( 'NONE',  ( 0.000000000000000000, 64.80702306891106446, -7.581672767545749814 ) ) ;
#1845=CIRCLE ( 'NONE', #16054, 27.60000000002759890 ) ;
#1848=ORIENTED_EDGE ( 'NONE', *, *, #9782, .T. ) ;
#1849=CARTESIAN_POINT ( 'NONE',  ( 19.99999999999999645, -63.85430960833482317, -11.25592921604904539 ) ) ;
#1853=EDGE_CURVE ( 'NONE', #6239, #939, #2482, .T. ) ;
#1854=EDGE_CURVE ( 'NONE', #5525, #20917, #15335, .T. ) ;
#1858=EDGE_CURVE ( 'NONE', #7472, #2406, #12305, .T. ) ;
#1859=VERTEX_POINT ( 'NONE', #1128 ) ;
#1860=DIRECTION ( 'NONE',  ( 0.000000000000000000, 0.000000000000000000, 1.000000000000000000 ) ) ;
#1862=ORIENTED_EDGE ( 'NONE', *, *, #14738, .T. ) ;
#1867=ORIENTED_EDGE ( 'NONE', *, *, #14885, .T. ) ;
#1870=VERTEX_POINT ( 'NONE', #9481 ) ;
#1872=EDGE_CURVE ( 'NONE', #6580, #9743, #15011, .T. ) ;
#1875=DIRECTION ( 'NONE',  ( -1.000000000000000000, -0.000000000000000000, -0.000000000000000000 ) ) ;
#1880=CARTESIAN_POINT ( 'NONE',  ( 9.999999999999998224, 71.76067541710851572, 5.865617076724862322 ) ) ;
#1882=EDGE_CURVE ( 'NONE', #9743, #10658, #20419, .T. ) ;
#1887=CARTESIAN_POINT ( 'NONE',  ( 19.99999999999999645, 56.63599015375672963, 31.56633360682482703 ) ) ;
#1888=CARTESIAN_POINT ( 'NONE',  ( 19.99999999999999645, 35.35772184876879720, 54.34979580218204376 ) ) ;
#1890=ORIENTED_EDGE ( 'NONE', *, *, #6619, .F. ) ;
#1891=CARTESIAN_POINT ( 'NONE',  ( 9.999999999999998224, 38.22257254261740655, 61.01667762370151848 ) ) ;
#1896=ORIENTED_EDGE ( 'NONE', *, *, #2354, .T. ) ;
#1897=DIRECTION ( 'NONE',  ( -1.000000000000000000, 0.000000000000000000, 0.000000000000000000 ) ) ;
#1899=AXIS2_PLACEMENT_3D ( 'NONE', #13062, #19519, #5306 ) ;
#1900=FACE_OUTER_BOUND ( 'NONE', #18103, .T. ) ;
#1902=DIRECTION ( 'NONE',  ( -1.000000000000000000, -0.000000000000000000, 0.000000000000000000 ) ) ;
#1903=AXIS2_PLACEMENT_3D ( 'NONE', #13104, #10660, #8951 ) ;
#1907=EDGE_CURVE ( 'NONE', #281, #11746, #1147, .T. ) ;
#1913=DIRECTION ( 'NONE',  ( 0.000000000000000000, -0.5195839500354227924, -0.8544194045464950094 ) ) ;
#1918=CARTESIAN_POINT ( 'NONE',  ( 0.000000000000000000, -70.29359119158475266, -15.58239511117359299 ) ) ;
#1920=ORIENTED_EDGE ( 'NONE', *, *, #19688, .T. ) ;
#1922=DIRECTION ( 'NONE',  ( 1.000000000000000000, 0.000000000000000000, 0.000000000000000000 ) ) ;
#1923=ORIENTED_EDGE ( 'NONE', *, *, #9853, .T. ) ;
#1928=LINE ( 'NONE', #13270, #19772 ) ;
#1929=CIRCLE ( 'NONE', #8356, 27.60000000002760956 ) ;
#1930=DIRECTION ( 'NONE',  ( -1.000000000000000000, -0.000000000000000000, -0.000000000000000000 ) ) ;
#1935=DIRECTION ( 'NONE',  ( -1.000000000000000000, 0.000000000000000000, 0.000000000000000000 ) ) ;
#1937=CARTESIAN_POINT ( 'NONE',  ( 19.99999999999999645, -14.55863677812078016, -63.60407295269120453 ) ) ;
#1941=EDGE_LOOP ( 'NONE', ( #17646, #11307, #18490, #9324 ) ) ;
#1943=LINE ( 'NONE', #3522, #14378 ) ;
#1944=VECTOR ( 'NONE', #20097, 1000.000000000000000 ) ;
#1949=LINE ( 'NONE', #45, #17304 ) ;
#1950=DIRECTION ( 'NONE',  ( 0.000000000000000000, 0.000000000000000000, 1.000000000000000000 ) ) ;
#1955=ADVANCED_FACE ( 'NONE', ( #12981 ), #9693, .T. ) ;
#1958=FACE_OUTER_BOUND ( 'NONE', #4088, .T. ) ;
#1963=CIRCLE ( 'NONE', #6316, 27.60000000002760245 ) ;
#1967=ADVANCED_FACE ( 'NONE', ( #19435 ), #17863, .T. ) ;
#1968=ORIENTED_EDGE ( 'NONE', *, *, #16242, .F. ) ;
#1973=EDGE_LOOP ( 'NONE', ( #407, #2959, #7904, #616 ) ) ;
#1975=CARTESIAN_POINT ( 'NONE',  ( 19.99999999999999645, 0.000000000000000000, 0.000000000000000000 ) ) ;
#1982=CARTESIAN_POINT ( 'NONE',  ( 19.99999999999999645, -5.762283366690708064, -64.99406197038676680 ) ) ;
#1990=CARTESIAN_POINT ( 'NONE',  ( 19.99999999999999645, -51.43306257653170377, 40.15061736769546741 ) ) ;
#1993=ADVANCED_FACE ( 'NONE', ( #14874 ), #145, .T. ) ;
#2002=CARTESIAN_POINT ( 'NONE',  ( 19.99999999999999645, -46.01927912072495275, -45.67597560296436399 ) ) ;
#2004=ORIENTED_EDGE ( 'NONE', *, *, #18820, .T. ) ;
#2007=CARTESIAN_POINT ( 'NONE',  ( 0.000000000000000000, -36.59093685910587368, -62.00889726308067651 ) ) ;
#2011=CARTESIAN_POINT ( 'NONE',  ( 0.000000000000000000, 0.000000000000000000, 0.000000000000000000 ) ) ;
#2015=LINE ( 'NONE', #18328, #12395 ) ;
#2016=VERTEX_POINT ( 'NONE', #12882 ) ;
#2026=ORIENTED_EDGE ( 'NONE', *, *, #7603, .F. ) ;
#2031=CYLINDRICAL_SURFACE ( 'NONE', #1166, 65.24900000006525147 ) ;
#2034=CARTESIAN_POINT ( 'NONE',  ( 19.99999999999999645, 0.000000000000000000, 0.000000000000000000 ) ) ;
#2035=CARTESIAN_POINT ( 'NONE',  ( 19.99999999999999645, -31.98952867950364265, 56.39803944231574206 ) ) ;
#2036=DIRECTION ( 'NONE',  ( -1.000000000000000000, 0.000000000000000000, 0.000000000000000000 ) ) ;
#2041=CARTESIAN_POINT ( 'NONE',  ( 19.99999999999999645, -51.96384592647234513, 49.83732252579596889 ) ) ;
#2042=CIRCLE ( 'NONE', #4750, 27.60000000002759890 ) ;
#2043=ORIENTED_EDGE ( 'NONE', *, *, #4432, .F. ) ;
#2047=CARTESIAN_POINT ( 'NONE',  ( 0.000000000000000000, -51.43306257653114955, -40.15061736769617795 ) ) ;
#2052=DIRECTION ( 'NONE',  ( 0.000000000000000000, -0.6310879443260593025, 0.7757112907044144690 ) ) ;
#2057=ORIENTED_EDGE ( 'NONE', *, *, #1831, .T. ) ;
#2058=CARTESIAN_POINT ( 'NONE',  ( 19.99999999999999645, 42.42902769288536291, 49.02903636734212967 ) ) ;
#2062=ORIENTED_EDGE ( 'NONE', *, *, #8961, .T. ) ;
#2068=ORIENTED_EDGE ( 'NONE', *, *, #7031, .T. ) ;
#2070=AXIS2_PLACEMENT_3D ( 'NONE', #17600, #19186, #15576 ) ;
#2075=AXIS2_PLACEMENT_3D ( 'NONE', #4773, #12945, #3081 ) ;
#2077=DIRECTION ( 'NONE',  ( 0.000000000000000000, 0.000000000000000000, -1.000000000000000000 ) ) ;
#2082=CIRCLE ( 'NONE', #1068, 27.60000000002759535 ) ;
#2088=FACE_OUTER_BOUND ( 'NONE', #17108, .T. ) ;
#2090=EDGE_CURVE ( 'NONE', #11808, #12431, #787, .T. ) ;
#2094=ORIENTED_EDGE ( 'NONE', *, *, #17671, .T. ) ;
#2095=CIRCLE ( 'NONE', #1106, 27.60000000002759890 ) ;
#2098=VERTEX_POINT ( 'NONE', #18582 ) ;
#2102=CIRCLE ( 'NONE', #6500, 72.00000000007199219 ) ;
#2103=EDGE_CURVE ( 'NONE', #2406, #13848, #19737, .T. ) ;
#2105=CYLINDRICAL_SURFACE ( 'NONE', #19854, 27.60000000002759890 ) ;
#2106=ADVANCED_FACE ( 'NONE', ( #13594 ), #15281, .T. ) ;
#2107=DIRECTION ( 'NONE',  ( -1.000000000000000000, 0.000000000000000000, 0.000000000000000000 ) ) ;
#2109=DIRECTION ( 'NONE',  ( 0.000000000000000000, 0.000000000000000000, -1.000000000000000000 ) ) ;
#2113=CIRCLE ( 'NONE', #419, 72.00000000007199219 ) ;
#2118=DIRECTION ( 'NONE',  ( 0.000000000000000000, 0.000000000000000000, 1.000000000000000000 ) ) ;
#2126=CARTESIAN_POINT ( 'NONE',  ( 0.000000000000000000, 0.000000000000000000, 0.000000000000000000 ) ) ;
#2127=ORIENTED_EDGE ( 'NONE', *, *, #6225, .F. ) ;
#2129=CARTESIAN_POINT ( 'NONE',  ( 0.000000000000000000, 43.56693332842852584, -48.57318520917462479 ) ) ;
#2135=AXIS2_PLACEMENT_3D ( 'NONE', #11722, #15010, #7046 ) ;
#2136=CARTESIAN_POINT ( 'NONE',  ( 19.99999999999999645, 63.85430960833490843, 16.34407078397899582 ) ) ;
#2137=LINE ( 'NONE', #5620, #15369 ) ;
#2138=VECTOR ( 'NONE', #16410, 1000.000000000000000 ) ;
#2139=CIRCLE ( 'NONE', #6535, 4.000000000000000000 ) ;
#2143=CIRCLE ( 'NONE', #7558, 27.60000000002760245 ) ;
#2148=DIRECTION ( 'NONE',  ( -1.000000000000000000, -0.000000000000000000, -0.000000000000000000 ) ) ;
#2153=DIRECTION ( 'NONE',  ( -1.000000000000000000, 0.000000000000000000, 0.000000000000000000 ) ) ;
#2154=ORIENTED_EDGE ( 'NONE', *, *, #19458, .F. ) ;
#2155=DIRECTION ( 'NONE',  ( 0.000000000000000000, -0.7308359642781161458, -0.6825531432186624503 ) ) ;
#2165=AXIS2_PLACEMENT_3D ( 'NONE', #6082, #9274, #2700 ) ;
#2168=ORIENTED_EDGE ( 'NONE', *, *, #17652, .F. ) ;
#2169=DIRECTION ( 'NONE',  ( 0.000000000000000000, -0.9790840876823249106, 0.2034560130526240906 ) ) ;
#2171=ORIENTED_EDGE ( 'NONE', *, *, #5540, .F. ) ;
#2172=CIRCLE ( 'NONE', #7587, 72.00000000007199219 ) ;
#2174=ORIENTED_EDGE ( 'NONE', *, *, #19111, .F. ) ;
#2177=LINE ( 'NONE', #16487, #4615 ) ;
#2179=VECTOR ( 'NONE', #19320, 1000.000000000000000 ) ;
#2180=VERTEX_POINT ( 'NONE', #3830 ) ;
#2181=ORIENTED_EDGE ( 'NONE', *, *, #15321, .F. ) ;
#2183=EDGE_LOOP ( 'NONE', ( #16569, #15786, #17436, #19964, #1862, #18536 ) ) ;
#2184=LINE ( 'NONE', #10452, #7690 ) ;
#2187=VERTEX_POINT ( 'NONE', #10202 ) ;
#2188=CIRCLE ( 'NONE', #18440, 27.60000000002759890 ) ;
#2189=LINE ( 'NONE', #13744, #13343 ) ;
#2191=FACE_OUTER_BOUND ( 'NONE', #20815, .T. ) ;
#2194=DIRECTION ( 'NONE',  ( 0.000000000000000000, 0.9422609221188213979, -0.3348796121709835538 ) ) ;
#2195=ORIENTED_EDGE ( 'NONE', *, *, #13247, .T. ) ;
#2201=DIRECTION ( 'NONE',  ( 1.000000000000000000, -0.000000000000000000, -0.000000000000000000 ) ) ;
#2202=ORIENTED_EDGE ( 'NONE', *, *, #9853, .F. ) ;
#2207=ORIENTED_EDGE ( 'NONE', *, *, #12482, .F. ) ;
#2208=DIRECTION ( 'NONE',  ( -1.000000000000000000, -0.000000000000000000, 0.000000000000000000 ) ) ;
#2209=FACE_OUTER_BOUND ( 'NONE', #14366, .T. ) ;
#2214=CIRCLE ( 'NONE', #7634, 27.60000000002760245 ) ;
#2219=DIRECTION ( 'NONE',  ( 0.000000000000000000, -0.8169698930104356549, -0.5766803221148764091 ) ) ;
#2220=DIRECTION ( 'NONE',  ( -1.000000000000000000, 0.000000000000000000, -0.000000000000000000 ) ) ;
#2221=ADVANCED_FACE ( 'NONE', ( #12212 ), #879, .T. ) ;
#2222=ORIENTED_EDGE ( 'NONE', *, *, #4494, .F. ) ;
#2225=CARTESIAN_POINT ( 'NONE',  ( 0.000000000000000000, 0.000000000000000000, 0.000000000000000000 ) ) ;
#2227=EDGE_CURVE ( 'NONE', #16282, #17758, #7202, .T. ) ;
#2231=CARTESIAN_POINT ( 'NONE',  ( 0.000000000000000000, -1.971042061627920727, -64.80882494896108881 ) ) ;
#2232=AXIS2_PLACEMENT_3D ( 'NONE', #17625, #11368, #11671 ) ;
#2234=EDGE_LOOP ( 'NONE', ( #16109, #2711, #18909, #7545 ) ) ;
#2235=VERTEX_POINT ( 'NONE', #7436 ) ;
#2236=DIRECTION ( 'NONE',  ( 0.000000000000000000, 0.000000000000000000, 1.000000000000000000 ) ) ;
#2238=CIRCLE ( 'NONE', #4265, 72.00000000007199219 ) ;
#2239=DIRECTION ( 'NONE',  ( -1.000000000000000000, -0.000000000000000000, 0.000000000000000000 ) ) ;
#2245=CARTESIAN_POINT ( 'NONE',  ( 0.000000000000000000, -24.01204443665145405, -60.22865198596149838 ) ) ;
#2249=VECTOR ( 'NONE', #8492, 1000.000000000000000 ) ;
#2250=AXIS2_PLACEMENT_3D ( 'NONE', #11196, #10880, #14501 ) ;
#2251=VERTEX_POINT ( 'NONE', #10743 ) ;
#2256=DIRECTION ( 'NONE',  ( -1.000000000000000000, -0.000000000000000000, 0.000000000000000000 ) ) ;
#2260=CARTESIAN_POINT ( 'NONE',  ( 19.99999999999999645, 60.40676135667469282, -23.56039007468977431 ) ) ;
#2262=EDGE_CURVE ( 'NONE', #18834, #7712, #10955, .T. ) ;
#2264=ORIENTED_EDGE ( 'NONE', *, *, #11136, .T. ) ;
#2265=AXIS2_PLACEMENT_3D ( 'NONE', #2535, #18317, #7071 ) ;
#2274=( LENGTH_UNIT ( ) NAMED_UNIT ( * ) SI_UNIT ( .MILLI., .METRE. ) );
#2281=CARTESIAN_POINT ( 'NONE',  ( 0.000000000000000000, -53.26727847779572045, 48.44168704307611506 ) ) ;
#2284=AXIS2_PLACEMENT_3D ( 'NONE', #17168, #15669, #2652 ) ;
#2286=ORIENTED_EDGE ( 'NONE', *, *, #20426, .T. ) ;
#2288=AXIS2_PLACEMENT_3D ( 'NONE', #6398, #4606, #10858 ) ;
#2291=AXIS2_PLACEMENT_3D ( 'NONE', #19254, #8406, #5330 ) ;
#2292=VERTEX_POINT ( 'NONE', #9249 ) ;
#2294=EDGE_CURVE ( 'NONE', #6278, #12115, #6540, .T. ) ;
#2305=CARTESIAN_POINT ( 'NONE',  ( 19.99999999999999645, 54.08351995568756365, -35.76369202524444546 ) ) ;
#2307=DIRECTION ( 'NONE',  ( -1.000000000000000000, 0.000000000000000000, 0.000000000000000000 ) ) ;
#2310=DIRECTION ( 'NONE',  ( 0.000000000000000000, 0.000000000000000000, 1.000000000000000000 ) ) ;
#2312=DIRECTION ( 'NONE',  ( -1.000000000000000000, -0.000000000000000000, 0.000000000000000000 ) ) ;
#2314=VERTEX_POINT ( 'NONE', #18793 ) ;
#2315=ORIENTED_EDGE ( 'NONE', *, *, #16854, .T. ) ;
#2317=FACE_OUTER_BOUND ( 'NONE', #17971, .T. ) ;
#2320=CARTESIAN_POINT ( 'NONE',  ( 19.99999999999999645, 46.01927912072526539, 45.67597560296404424 ) ) ;
#2322=CARTESIAN_POINT ( 'NONE',  ( 9.999999999999998224, -59.36728637277992249, -40.73727173906846843 ) ) ;
#2323=EDGE_CURVE ( 'NONE', #15053, #11776, #13664, .T. ) ;
#2326=VERTEX_POINT ( 'NONE', #4263 ) ;
#2329=DIRECTION ( 'NONE',  ( -1.000000000000000000, 0.000000000000000000, 0.000000000000000000 ) ) ;
#2330=EDGE_CURVE ( 'NONE', #11776, #11750, #17206, .T. ) ;
#2339=CARTESIAN_POINT ( 'NONE',  ( 0.000000000000000000, 0.000000000000000000, 0.000000000000000000 ) ) ;
#2340=AXIS2_PLACEMENT_3D ( 'NONE', #5183, #8072, #16017 ) ;
#2343=DIRECTION ( 'NONE',  ( -1.000000000000000000, 0.000000000000000000, 0.000000000000000000 ) ) ;
#2345=EDGE_CURVE ( 'NONE', #10694, #11336, #1315, .T. ) ;
#2347=EDGE_CURVE ( 'NONE', #3334, #8219, #11626, .T. ) ;
#2348=DIRECTION ( 'NONE',  ( 0.000000000000000000, 0.000000000000000000, 1.000000000000000000 ) ) ;
#2352=CARTESIAN_POINT ( 'NONE',  ( 19.99999999999999645, 44.69367065308644271, 56.44887778834761605 ) ) ;
#2354=EDGE_CURVE ( 'NONE', #5060, #5564, #1507, .T. ) ;
#2356=CARTESIAN_POINT ( 'NONE',  ( -65.00002539999999840, 0.000000000000000000, -7.500000000000000000 ) ) ;
#2362=DIRECTION ( 'NONE',  ( -1.000000000000000000, 0.000000000000000000, 0.000000000000000000 ) ) ;
#2369=ADVANCED_FACE ( 'NONE', ( #13817 ), #9455, .T. ) ;
#2372=ORIENTED_EDGE ( 'NONE', *, *, #16212, .F. ) ;
#2373=DIRECTION ( 'NONE',  ( 0.000000000000000000, 0.000000000000000000, -1.000000000000000000 ) ) ;
#2374=ADVANCED_FACE ( 'NONE', ( #18904 ), #4152, .T. ) ;
#2385=LINE ( 'NONE', #9170, #12249 ) ;
#2386=AXIS2_PLACEMENT_3D ( 'NONE', #20275, #14362, #11377 ) ;
#2387=EDGE_LOOP ( 'NONE', ( #10662, #11563, #2719, #10655 ) ) ;
#2388=CARTESIAN_POINT ( 'NONE',  ( -10.00000000000000000, 0.000000000000000000, 0.000000000000000000 ) ) ;
#2393=DIRECTION ( 'NONE',  ( -1.000000000000000000, -0.000000000000000000, -0.000000000000000000 ) ) ;
#2398=DIRECTION ( 'NONE',  ( -1.000000000000000000, -0.000000000000000000, -0.000000000000000000 ) ) ;
#2399=CARTESIAN_POINT ( 'NONE',  ( 19.99999999999999645, 0.000000000000000000, 0.000000000000000000 ) ) ;
#2403=EDGE_CURVE ( 'NONE', #2438, #12530, #13333, .T. ) ;
#2406=VERTEX_POINT ( 'NONE', #9670 ) ;
#2409=DIRECTION ( 'NONE',  ( -1.000000000000000000, -0.000000000000000000, -0.000000000000000000 ) ) ;
#2413=CARTESIAN_POINT ( 'NONE',  ( 19.99999999999999645, -60.40676135667420965, -23.56039007469101421 ) ) ;
#2414=VECTOR ( 'NONE', #14278, 1000.000000000000000 ) ;
#2416=DIRECTION ( 'NONE',  ( -1.000000000000000000, 0.000000000000000000, 0.000000000000000000 ) ) ;
#2417=CIRCLE ( 'NONE', #7157, 65.24900000006526568 ) ;
#2427=ADVANCED_FACE ( 'NONE', ( #14450 ), #9862, .T. ) ;
#2430=DIRECTION ( 'NONE',  ( 0.000000000000000000, 0.000000000000000000, 1.000000000000000000 ) ) ;
#2433=CARTESIAN_POINT ( 'NONE',  ( 0.000000000000000000, 0.000000000000000000, 0.000000000000000000 ) ) ;
#2435=DIRECTION ( 'NONE',  ( -1.000000000000000000, 0.000000000000000000, 0.000000000000000000 ) ) ;
#2436=FACE_OUTER_BOUND ( 'NONE', #5477, .T. ) ;
#2438=VERTEX_POINT ( 'NONE', #19510 ) ;
#2439=CARTESIAN_POINT ( 'NONE',  ( 19.99999999999999645, -63.85430960833482317, -11.25592921604904539 ) ) ;
#2441=SHAPE_REPRESENTATION_RELATIONSHIP ( 'NONE' , 'NONE' ,  #13064, #19794 ) ;
#2442=CARTESIAN_POINT ( 'NONE',  ( 9.999999999999998224, -68.15657073222419626, -23.20952102120350702 ) ) ;
#2443=AXIS2_PLACEMENT_3D ( 'NONE', #3785, #17737, #12863 ) ;
#2446=CYLINDRICAL_SURFACE ( 'NONE', #2515, 27.60000000002760245 ) ;
#2450=DIRECTION ( 'NONE',  ( 1.000000000000000000, -0.000000000000000000, -0.000000000000000000 ) ) ;
#2451=CIRCLE ( 'NONE', #18370, 27.60000000002759535 ) ;
#2452=CARTESIAN_POINT ( 'NONE',  ( 0.000000000000000000, -31.17893654894190902, -57.31758819669202865 ) ) ;
#2453=CARTESIAN_POINT ( 'NONE',  ( 9.999999999999998224, 67.51707036274413554, 25.00890260772400708 ) ) ;
#2474=VECTOR ( 'NONE', #15517, 1000.000000000000000 ) ;
#2475=CARTESIAN_POINT ( 'NONE',  ( 19.99999999999999645, 59.31169354540775629, -27.19476070466793871 ) ) ;
#2477=CARTESIAN_POINT ( 'NONE',  ( 19.99999999999999645, 0.000000000000000000, 0.000000000000000000 ) ) ;
#2478=AXIS2_PLACEMENT_3D ( 'NONE', #18141, #6476, #16545 ) ;
#2482=CIRCLE ( 'NONE', #14664, 65.24900000006526568 ) ;
#2493=AXIS2_PLACEMENT_3D ( 'NONE', #15387, #16874, #7323 ) ;
#2497=DIRECTION ( 'NONE',  ( 0.000000000000000000, 0.000000000000000000, 1.000000000000000000 ) ) ;
#2503=EDGE_CURVE ( 'NONE', #15688, #8604, #17730, .T. ) ;
#2505=CARTESIAN_POINT ( 'NONE',  ( 19.99999999999999645, 0.000000000000000000, 0.000000000000000000 ) ) ;
#2509=VECTOR ( 'NONE', #15178, 1000.000000000000000 ) ;
#2511=VECTOR ( 'NONE', #20879, 1000.000000000000000 ) ;
#2512=ORIENTED_EDGE ( 'NONE', *, *, #9952, .T. ) ;
#2515=AXIS2_PLACEMENT_3D ( 'NONE', #7099, #19929, #18246 ) ;
#2518=AXIS2_PLACEMENT_3D ( 'NONE', #9789, #3223, #1653 ) ;
#2520=ADVANCED_FACE ( 'NONE', ( #6377 ), #11556, .T. ) ;
#2522=CYLINDRICAL_SURFACE ( 'NONE', #20546, 72.00000000007199219 ) ;
#2524=AXIS2_PLACEMENT_3D ( 'NONE', #580, #20270, #10531 ) ;
#2525=ORIENTED_EDGE ( 'NONE', *, *, #19695, .F. ) ;
#2530=VERTEX_POINT ( 'NONE', #19300 ) ;
#2533=AXIS2_PLACEMENT_3D ( 'NONE', #3699, #8469, #7192 ) ;
#2534=CARTESIAN_POINT ( 'NONE',  ( 19.99999999999999645, -63.85430960833497949, 11.25592921604817676 ) ) ;
#2535=CARTESIAN_POINT ( 'NONE',  ( -10.00000000000000000, 0.000000000000000000, 0.000000000000000000 ) ) ;
#2544=CIRCLE ( 'NONE', #3219, 72.00000000007199219 ) ;
#2550=ORIENTED_EDGE ( 'NONE', *, *, #14654, .T. ) ;
#2551=CARTESIAN_POINT ( 'NONE',  ( 0.000000000000000000, 1.971042061629218356, -64.80882494896104618 ) ) ;
#2552=ORIENTED_EDGE ( 'NONE', *, *, #14792, .F. ) ;
#2553=CARTESIAN_POINT ( 'NONE',  ( 0.000000000000000000, 0.000000000000000000, 0.000000000000000000 ) ) ;
#2557=VERTEX_POINT ( 'NONE', #19783 ) ;
#2558=DIRECTION ( 'NONE',  ( 0.000000000000000000, 0.000000000000000000, 1.000000000000000000 ) ) ;
#2562=EDGE_CURVE ( 'NONE', #7334, #17345, #3822, .T. ) ;
#2563=DIRECTION ( 'NONE',  ( 0.000000000000000000, 0.9976687691905390398, 0.06824241336467466723 ) ) ;
#2569=ORIENTED_EDGE ( 'NONE', *, *, #1609, .T. ) ;
#2570=DIRECTION ( 'NONE',  ( -1.000000000000000000, 0.000000000000000000, 0.000000000000000000 ) ) ;
#2576=DIRECTION ( 'NONE',  ( 0.000000000000000000, 0.000000000000000000, -1.000000000000000000 ) ) ;
#2578=AXIS2_PLACEMENT_3D ( 'NONE', #20888, #9762, #9663 ) ;
#2580=DIRECTION ( 'NONE',  ( -1.000000000000000000, -0.000000000000000000, 0.000000000000000000 ) ) ;
#2582=ORIENTED_EDGE ( 'NONE', *, *, #14780, .T. ) ;
#2593=CARTESIAN_POINT ( 'NONE',  ( 19.99999999999999645, -29.55812890831937878, -65.65300461859717984 ) ) ;
#2597=EDGE_CURVE ( 'NONE', #15726, #9191, #19090, .T. ) ;
#2602=CIRCLE ( 'NONE', #13781, 27.60000000002759890 ) ;
#2606=CARTESIAN_POINT ( 'NONE',  ( 9.999999999999998224, -64.36139404985986801, 32.27399814043853610 ) ) ;
#2612=EDGE_CURVE ( 'NONE', #7632, #18559, #15691, .T. ) ;
#2613=CYLINDRICAL_SURFACE ( 'NONE', #16848, 27.60000000002760245 ) ;
#2615=VECTOR ( 'NONE', #18973, 1000.000000000000000 ) ;
#2631=EDGE_CURVE ( 'NONE', #2098, #7589, #9928, .T. ) ;
#2632=DIRECTION ( 'NONE',  ( -1.000000000000000000, 0.000000000000000000, 0.000000000000000000 ) ) ;
#2633=CARTESIAN_POINT ( 'NONE',  ( 0.000000000000000000, 0.000000000000000000, 0.000000000000000000 ) ) ;
#2634=AXIS2_PLACEMENT_3D ( 'NONE', #13403, #467, #14394 ) ;
#2640=VERTEX_POINT ( 'NONE', #19819 ) ;
#2642=CARTESIAN_POINT ( 'NONE',  ( 19.99999999999999645, -64.79224928664389438, -2.456263514198281150 ) ) ;
#2643=VECTOR ( 'NONE', #19368, 1000.000000000000000 ) ;
#2644=DIRECTION ( 'NONE',  ( -1.000000000000000000, -0.000000000000000000, 0.000000000000000000 ) ) ;
#2646=DIRECTION ( 'NONE',  ( -1.000000000000000000, -0.000000000000000000, 0.000000000000000000 ) ) ;
#2652=DIRECTION ( 'NONE',  ( 0.000000000000000000, 0.000000000000000000, 1.000000000000000000 ) ) ;
#2655=CARTESIAN_POINT ( 'NONE',  ( 150.0000507999999968, 0.000000000000000000, 0.000000000000000000 ) ) ;
#2656=ORIENTED_EDGE ( 'NONE', *, *, #20426, .F. ) ;
#2657=FACE_OUTER_BOUND ( 'NONE', #14793, .T. ) ;
#2659=DIRECTION ( 'NONE',  ( 0.000000000000000000, -0.9422609221188236184, 0.3348796121709771145 ) ) ;
#2663=DIRECTION ( 'NONE',  ( -1.000000000000000000, 0.000000000000000000, 0.000000000000000000 ) ) ;
#2664=LINE ( 'NONE', #12623, #19397 ) ;
#2668=CARTESIAN_POINT ( 'NONE',  ( 19.99999999999999645, -36.54710069451090959, 54.05313526368099986 ) ) ;
#2669=CARTESIAN_POINT ( 'NONE',  ( 0.000000000000000000, 64.79224928664386596, 2.456263514198732345 ) ) ;
#2671=CYLINDRICAL_SURFACE ( 'NONE', #14285, 27.60000000002760245 ) ;
#2674=ORIENTED_EDGE ( 'NONE', *, *, #1796, .T. ) ;
#2676=ORIENTED_EDGE ( 'NONE', *, *, #8532, .F. ) ;
#2679=ORIENTED_EDGE ( 'NONE', *, *, #18054, .T. ) ;
#2680=DIRECTION ( 'NONE',  ( -1.000000000000000000, -0.000000000000000000, -0.000000000000000000 ) ) ;
#2681=ORIENTED_EDGE ( 'NONE', *, *, #3636, .T. ) ;
#2691=CARTESIAN_POINT ( 'NONE',  ( 0.000000000000000000, 64.79224928664392280, 25.14373648582975918 ) ) ;
#2692=VERTEX_POINT ( 'NONE', #11772 ) ;
#2693=CARTESIAN_POINT ( 'NONE',  ( 0.000000000000000000, -64.79224928664389438, 25.14373648582931864 ) ) ;
#2694=VERTEX_POINT ( 'NONE', #1918 ) ;
#2697=VERTEX_POINT ( 'NONE', #434 ) ;
#2699=FACE_OUTER_BOUND ( 'NONE', #9816, .T. ) ;
#2700=DIRECTION ( 'NONE',  ( 0.000000000000000000, 0.8169698930104432044, -0.5766803221148655290 ) ) ;
#2702=DIRECTION ( 'NONE',  ( -1.000000000000000000, 0.000000000000000000, 0.000000000000000000 ) ) ;
#2705=EDGE_CURVE ( 'NONE', #4710, #10182, #10175, .T. ) ;
#2707=FACE_OUTER_BOUND ( 'NONE', #6289, .T. ) ;
#2711=ORIENTED_EDGE ( 'NONE', *, *, #13485, .T. ) ;
#2712=DIRECTION ( 'NONE',  ( 0.000000000000000000, 0.000000000000000000, -1.000000000000000000 ) ) ;
#2716=CARTESIAN_POINT ( 'NONE',  ( 0.000000000000000000, 0.000000000000000000, 0.000000000000000000 ) ) ;
#2719=ORIENTED_EDGE ( 'NONE', *, *, #6257, .T. ) ;
#2720=FACE_OUTER_BOUND ( 'NONE', #10015, .T. ) ;
#2722=AXIS2_PLACEMENT_3D ( 'NONE', #7827, #7939, #18669 ) ;
#2728=DIRECTION ( 'NONE',  ( 0.000000000000000000, 0.000000000000000000, 1.000000000000000000 ) ) ;
#2729=ADVANCED_FACE ( 'NONE', ( #14850 ), #640, .T. ) ;
#2732=AXIS2_PLACEMENT_3D ( 'NONE', #17567, #3034, #9494 ) ;
#2734=CARTESIAN_POINT ( 'NONE',  ( 0.000000000000000000, -42.42902769288568976, 49.02903636734183124 ) ) ;
#2740=DIRECTION ( 'NONE',  ( 0.000000000000000000, 0.000000000000000000, 1.000000000000000000 ) ) ;
#2741=VECTOR ( 'NONE', #14956, 1000.000000000000000 ) ;
#2742=EDGE_CURVE ( 'NONE', #10180, #19485, #19690, .T. ) ;
#2744=CARTESIAN_POINT ( 'NONE',  ( 19.99999999999999645, -58.44960523466261293, 28.06621538408569805 ) ) ;
#2750=DIRECTION ( 'NONE',  ( -1.000000000000000000, 0.000000000000000000, 0.000000000000000000 ) ) ;
#2752=EDGE_CURVE ( 'NONE', #12799, #9697, #10910, .T. ) ;
#2756=DIRECTION ( 'NONE',  ( 0.000000000000000000, 0.7308359642781253607, -0.6825531432186527914 ) ) ;
#2758=ORIENTED_EDGE ( 'NONE', *, *, #280, .T. ) ;
#2759=AXIS2_PLACEMENT_3D ( 'NONE', #11981, #13478, #7196 ) ;
#2768=AXIS2_PLACEMENT_3D ( 'NONE', #15496, #987, #18787 ) ;
#2770=AXIS2_PLACEMENT_3D ( 'NONE', #20102, #2409, #8869 ) ;
#2772=DIRECTION ( 'NONE',  ( -1.000000000000000000, -0.000000000000000000, -0.000000000000000000 ) ) ;
#2775=VERTEX_POINT ( 'NONE', #2860 ) ;
#2777=DIRECTION ( 'NONE',  ( -1.000000000000000000, 0.000000000000000000, -0.000000000000000000 ) ) ;
#2778=VECTOR ( 'NONE', #15661, 1000.000000000000000 ) ;
#2780=EDGE_CURVE ( 'NONE', #15314, #3307, #15642, .T. ) ;
#2781=DIRECTION ( 'NONE',  ( 1.000000000000000000, 0.000000000000000000, 0.000000000000000000 ) ) ;
#2782=VERTEX_POINT ( 'NONE', #9325 ) ;
#2787=CARTESIAN_POINT ( 'NONE',  ( 19.99999999999999645, -63.17103598352115057, -16.33561182745204476 ) ) ;
#2788=AXIS2_PLACEMENT_3D ( 'NONE', #13993, #20450, #5930 ) ;
#2792=LINE ( 'NONE', #17536, #14704 ) ;
#2795=CARTESIAN_POINT ( 'NONE',  ( 19.99999999999999645, 11.98658579560587789, 64.13855129306472236 ) ) ;
#2796=ADVANCED_FACE ( 'NONE', ( #10606 ), #8898, .T. ) ;
#2797=DIRECTION ( 'NONE',  ( -1.000000000000000000, -0.000000000000000000, 0.000000000000000000 ) ) ;
#2800=CARTESIAN_POINT ( 'NONE',  ( 19.99999999999999645, 65.23577793412344761, -1.313498510941930153 ) ) ;
#2807=DIRECTION ( 'NONE',  ( 0.000000000000000000, 0.000000000000000000, 1.000000000000000000 ) ) ;
#2809=DIRECTION ( 'NONE',  ( -1.000000000000000000, 0.000000000000000000, 0.000000000000000000 ) ) ;
#2810=ORIENTED_EDGE ( 'NONE', *, *, #5239, .F. ) ;
#2811=DIRECTION ( 'NONE',  ( -1.000000000000000000, -0.000000000000000000, -0.000000000000000000 ) ) ;
#2813=FACE_OUTER_BOUND ( 'NONE', #1797, .T. ) ;
#2814=AXIS2_PLACEMENT_3D ( 'NONE', #14812, #918, #10556 ) ;
#2816=CYLINDRICAL_SURFACE ( 'NONE', #2827, 27.60000000002760245 ) ;
#2819=EDGE_CURVE ( 'NONE', #2406, #9297, #17068, .T. ) ;
#2827=AXIS2_PLACEMENT_3D ( 'NONE', #6406, #1448, #4618 ) ;
#2828=AXIS2_PLACEMENT_3D ( 'NONE', #3495, #1412, #7862 ) ;
#2829=VERTEX_POINT ( 'NONE', #7627 ) ;
#2830=DIRECTION ( 'NONE',  ( -1.000000000000000000, 0.000000000000000000, 0.000000000000000000 ) ) ;
#2837=ORIENTED_EDGE ( 'NONE', *, *, #2262, .T. ) ;
#2839=CIRCLE ( 'NONE', #1830, 27.60000000002759535 ) ;
#2840=CARTESIAN_POINT ( 'NONE',  ( 9.999999999999998224, 18.50424539729845463, 69.58155576219121485 ) ) ;
#2842=CARTESIAN_POINT ( 'NONE',  ( 0.000000000000000000, 0.9548212943365497196, 71.99366858485716136 ) ) ;
#2848=ORIENTED_EDGE ( 'NONE', *, *, #15763, .F. ) ;
#2849=PLANE ( 'NONE',  #18202 ) ;
#2854=DIRECTION ( 'NONE',  ( 0.000000000000000000, 0.000000000000000000, 1.000000000000000000 ) ) ;
#2858=AXIS2_PLACEMENT_3D ( 'NONE', #2035, #4910, #12874 ) ;
#2859=ORIENTED_EDGE ( 'NONE', *, *, #20832, .F. ) ;
#2860=CARTESIAN_POINT ( 'NONE',  ( 19.99999999999999645, 56.42118728228200553, -32.77318456705383198 ) ) ;
#2861=ORIENTED_EDGE ( 'NONE', *, *, #16747, .T. ) ;
#2863=CARTESIAN_POINT ( 'NONE',  ( 19.99999999999999645, 56.63599015375715595, -31.56633360682406675 ) ) ;
#2864=DIRECTION ( 'NONE',  ( 0.000000000000000000, 0.000000000000000000, 1.000000000000000000 ) ) ;
#2865=ORIENTED_EDGE ( 'NONE', *, *, #2103, .T. ) ;
#2866=EDGE_CURVE ( 'NONE', #8899, #14496, #2102, .T. ) ;
#2867=ORIENTED_EDGE ( 'NONE', *, *, #10506, .F. ) ;
#2870=DIRECTION ( 'NONE',  ( 1.000000000000000000, 0.000000000000000000, 0.000000000000000000 ) ) ;
#2872=EDGE_CURVE ( 'NONE', #19105, #18360, #10226, .T. ) ;
#2876=FACE_OUTER_BOUND ( 'NONE', #7626, .T. ) ;
#2878=ADVANCED_FACE ( 'NONE', ( #13789 ), #20240, .T. ) ;
#2879=ORIENTED_EDGE ( 'NONE', *, *, #9976, .T. ) ;
#2882=ORIENTED_EDGE ( 'NONE', *, *, #1261, .T. ) ;
#2884=DIRECTION ( 'NONE',  ( 0.000000000000000000, 0.7308359642781253607, -0.6825531432186527914 ) ) ;
#2887=DIRECTION ( 'NONE',  ( -1.000000000000000000, -0.000000000000000000, -0.000000000000000000 ) ) ;
#2895=CIRCLE ( 'NONE', #4920, 72.00000000007199219 ) ;
#2902=EDGE_CURVE ( 'NONE', #19080, #14722, #9435, .T. ) ;
#2903=CARTESIAN_POINT ( 'NONE',  ( 0.000000000000000000, -56.63599015375651646, -31.56633360682521072 ) ) ;
#2904=CIRCLE ( 'NONE', #14750, 27.60000000002759535 ) ;
#2905=DIRECTION ( 'NONE',  ( -1.000000000000000000, -0.000000000000000000, 0.000000000000000000 ) ) ;
#2907=DIRECTION ( 'NONE',  ( 0.000000000000000000, 0.8169698930104430934, -0.5766803221148655290 ) ) ;
#2908=DIRECTION ( 'NONE',  ( -1.000000000000000000, -0.000000000000000000, 0.000000000000000000 ) ) ;
#2912=EDGE_CURVE ( 'NONE', #714, #5717, #3455, .T. ) ;
#2913=DIRECTION ( 'NONE',  ( 1.000000000000000000, -0.000000000000000000, -0.000000000000000000 ) ) ;
#2919=VERTEX_POINT ( 'NONE', #1696 ) ;
#2925=CARTESIAN_POINT ( 'NONE',  ( 0.000000000000000000, 51.81019761368373366, -38.98425606966007706 ) ) ;
#2928=ORIENTED_EDGE ( 'NONE', *, *, #6486, .T. ) ;
#2934=VECTOR ( 'NONE', #5279, 1000.000000000000000 ) ;
#2939=ORIENTED_EDGE ( 'NONE', *, *, #15465, .T. ) ;
#2942=LINE ( 'NONE', #12584, #19881 ) ;
#2943=ORIENTED_EDGE ( 'NONE', *, *, #20228, .T. ) ;
#2944=CARTESIAN_POINT ( 'NONE',  ( 0.000000000000000000, 59.31169354540738681, 27.19476070466876649 ) ) ;
#2949=ORIENTED_EDGE ( 'NONE', *, *, #12308, .F. ) ;
#2951=FACE_OUTER_BOUND ( 'NONE', #19937, .T. ) ;
#2952=AXIS2_PLACEMENT_3D ( 'NONE', #14706, #6633, #13118 ) ;
#2959=ORIENTED_EDGE ( 'NONE', *, *, #16591, .F. ) ;
#2964=EDGE_CURVE ( 'NONE', #2973, #2187, #7175, .T. ) ;
#2965=VERTEX_POINT ( 'NONE', #3277 ) ;
#2967=AXIS2_PLACEMENT_3D ( 'NONE', #19335, #3335, #14678 ) ;
#2968=DIRECTION ( 'NONE',  ( 0.000000000000000000, 0.000000000000000000, -1.000000000000000000 ) ) ;
#2972=CIRCLE ( 'NONE', #10074, 72.00000000007199219 ) ;
#2973=VERTEX_POINT ( 'NONE', #3370 ) ;
#2975=CARTESIAN_POINT ( 'NONE',  ( 9.999999999999998224, -8.857208570070309150, 71.45313048675083678 ) ) ;
#2976=EDGE_CURVE ( 'NONE', #15515, #659, #16108, .T. ) ;
#2980=CARTESIAN_POINT ( 'NONE',  ( 0.000000000000000000, 0.000000000000000000, 0.000000000000000000 ) ) ;
#2981=EDGE_CURVE ( 'NONE', #18447, #20602, #14617, .T. ) ;
#2982=CARTESIAN_POINT ( 'NONE',  ( 0.000000000000000000, 0.000000000000000000, 0.000000000000000000 ) ) ;
#2989=EDGE_CURVE ( 'NONE', #18776, #16343, #9546, .T. ) ;
#2990=ORIENTED_EDGE ( 'NONE', *, *, #16574, .F. ) ;
#2991=CARTESIAN_POINT ( 'NONE',  ( 0.000000000000000000, 64.44931368725519860, 10.18420179740629727 ) ) ;
#3005=ADVANCED_FACE ( 'NONE', ( #9834 ), #1387, .T. ) ;
#3011=ORIENTED_EDGE ( 'NONE', *, *, #2964, .F. ) ;
#3013=DIRECTION ( 'NONE',  ( 0.000000000000000000, 0.3984010898462422290, -0.9172113015054527141 ) ) ;
#3017=DIRECTION ( 'NONE',  ( 0.000000000000000000, -0.7308359642781161458, -0.6825531432186624503 ) ) ;
#3020=ORIENTED_EDGE ( 'NONE', *, *, #4456, .T. ) ;
#3021=DIRECTION ( 'NONE',  ( 0.000000000000000000, 0.1361666490962400444, 0.9906859460363315328 ) ) ;
#3023=DIRECTION ( 'NONE',  ( -1.000000000000000000, -0.000000000000000000, -0.000000000000000000 ) ) ;
#3025=ORIENTED_EDGE ( 'NONE', *, *, #14545, .T. ) ;
#3026=EDGE_CURVE ( 'NONE', #8080, #1369, #12833, .T. ) ;
#3028=ADVANCED_FACE ( 'NONE', ( #4867 ), #17808, .T. ) ;
#3032=ORIENTED_EDGE ( 'NONE', *, *, #3080, .F. ) ;
#3034=DIRECTION ( 'NONE',  ( -1.000000000000000000, 0.000000000000000000, -0.000000000000000000 ) ) ;
#3037=DIRECTION ( 'NONE',  ( -1.000000000000000000, 0.000000000000000000, -0.000000000000000000 ) ) ;
#3039=CARTESIAN_POINT ( 'NONE',  ( 19.99999999999999645, 28.84646472442533494, -58.52617768068405013 ) ) ;
#3041=ORIENTED_EDGE ( 'NONE', *, *, #20155, .T. ) ;
#3045=ORIENTED_EDGE ( 'NONE', *, *, #8074, .T. ) ;
#3052=DIRECTION ( 'NONE',  ( 0.000000000000000000, -0.2697967711570115057, -0.9629172873478029082 ) ) ;
#3056=DIRECTION ( 'NONE',  ( 0.000000000000000000, 0.000000000000000000, 1.000000000000000000 ) ) ;
#3058=EDGE_CURVE ( 'NONE', #9385, #10906, #5062, .T. ) ;
#3059=CARTESIAN_POINT ( 'NONE',  ( 19.99999999999999645, 10.74906464462217848, -71.19310085447956737 ) ) ;
#3060=VERTEX_POINT ( 'NONE', #19683 ) ;
#3061=CARTESIAN_POINT ( 'NONE',  ( 19.99999999999999645, -27.62776854598897813, 58.65812137498992485 ) ) ;
#3063=DIRECTION ( 'NONE',  ( -1.000000000000000000, 0.000000000000000000, 0.000000000000000000 ) ) ;
#3064=VERTEX_POINT ( 'NONE', #11842 ) ;
#3065=DIRECTION ( 'NONE',  ( 0.000000000000000000, 0.000000000000000000, 1.000000000000000000 ) ) ;
#3067=DIRECTION ( 'NONE',  ( 0.000000000000000000, 0.3984010898462361228, 0.9172113015054552676 ) ) ;
#3069=AXIS2_PLACEMENT_3D ( 'NONE', #13931, #14247, #17221 ) ;
#3070=EDGE_LOOP ( 'NONE', ( #10488, #17439, #828, #19141 ) ) ;
#3073=VECTOR ( 'NONE', #3820, 1000.000000000000000 ) ;
#3076=DIRECTION ( 'NONE',  ( 0.000000000000000000, 0.000000000000000000, 1.000000000000000000 ) ) ;
#3080=EDGE_CURVE ( 'NONE', #297, #7334, #620, .T. ) ;
#3081=DIRECTION ( 'NONE',  ( 0.000000000000000000, 0.5195839500354287877, 0.8544194045464914566 ) ) ;
#3084=ORIENTED_EDGE ( 'NONE', *, *, #2866, .F. ) ;
#3090=ADVANCED_FACE ( 'NONE', ( #14830 ), #11947, .T. ) ;
#3098=AXIS2_PLACEMENT_3D ( 'NONE', #10998, #10583, #12494 ) ;
#3099=ORIENTED_EDGE ( 'NONE', *, *, #16627, .T. ) ;
#3105=ORIENTED_EDGE ( 'NONE', *, *, #15117, .T. ) ;
#3112=LINE ( 'NONE', #7996, #16631 ) ;
#3113=CARTESIAN_POINT ( 'NONE',  ( 0.000000000000000000, -27.80658314415180499, -66.41380830714152239 ) ) ;
#3115=AXIS2_PLACEMENT_3D ( 'NONE', #15849, #1343, #14261 ) ;
#3116=VERTEX_POINT ( 'NONE', #11745 ) ;
#3118=CIRCLE ( 'NONE', #8854, 72.00000000007199219 ) ;
#3128=AXIS2_PLACEMENT_3D ( 'NONE', #12388, #13980, #4222 ) ;
#3130=VERTEX_POINT ( 'NONE', #11526 ) ;
#3131=DIRECTION ( 'NONE',  ( 0.000000000000000000, 0.9790840876823234673, -0.2034560130526308908 ) ) ;
#3139=DIRECTION ( 'NONE',  ( -1.000000000000000000, -0.000000000000000000, -0.000000000000000000 ) ) ;
#3140=EDGE_CURVE ( 'NONE', #3060, #16924, #6188, .T. ) ;
#3141=ORIENTED_EDGE ( 'NONE', *, *, #15957, .F. ) ;
#3142=EDGE_CURVE ( 'NONE', #20917, #2697, #13449, .T. ) ;
#3143=DIRECTION ( 'NONE',  ( -1.000000000000000000, 0.000000000000000000, 0.000000000000000000 ) ) ;
#3146=CIRCLE ( 'NONE', #17357, 72.00000000007199219 ) ;
#3148=VECTOR ( 'NONE', #8243, 1000.000000000000000 ) ;
#3152=EDGE_LOOP ( 'NONE', ( #2943, #6034, #6957, #14481 ) ) ;
#3158=AXIS2_PLACEMENT_3D ( 'NONE', #862, #3709, #18455 ) ;
#3161=CARTESIAN_POINT ( 'NONE',  ( 9.999999999999998224, -27.80658314415272159, 66.41380830714115291 ) ) ;
#3163=ADVANCED_FACE ( 'NONE', ( #6753 ), #6961, .T. ) ;
#3169=DIRECTION ( 'NONE',  ( 0.000000000000000000, 0.000000000000000000, 1.000000000000000000 ) ) ;
#3170=EDGE_CURVE ( 'NONE', #19379, #11771, #20719, .T. ) ;
#3171=LINE ( 'NONE', #3572, #6644 ) ;
#3194=AXIS2_PLACEMENT_3D ( 'NONE', #3627, #6800, #6493 ) ;
#3195=ORIENTED_EDGE ( 'NONE', *, *, #11286, .F. ) ;
#3196=FACE_OUTER_BOUND ( 'NONE', #3994, .T. ) ;
#3199=CARTESIAN_POINT ( 'NONE',  ( 19.99999999999999645, -70.68211945903178162, -13.71269443944282074 ) ) ;
#3203=CARTESIAN_POINT ( 'NONE',  ( 0.000000000000000000, 0.000000000000000000, 0.000000000000000000 ) ) ;
#3204=CARTESIAN_POINT ( 'NONE',  ( 0.000000000000000000, 15.58726123847937828, -62.93731870009387563 ) ) ;
#3209=ADVANCED_FACE ( 'NONE', ( #13757 ), #16925, .T. ) ;
#3212=VECTOR ( 'NONE', #14447, 1000.000000000000000 ) ;
#3216=DIRECTION ( 'NONE',  ( -1.000000000000000000, 0.000000000000000000, 0.000000000000000000 ) ) ;
#3219=AXIS2_PLACEMENT_3D ( 'NONE', #1515, #16322, #13250 ) ;
#3220=VERTEX_POINT ( 'NONE', #1040 ) ;
#3221=DIRECTION ( 'NONE',  ( -1.000000000000000000, -0.000000000000000000, -0.000000000000000000 ) ) ;
#3222=CARTESIAN_POINT ( 'NONE',  ( 19.99999999999999645, 5.762283366692075859, -64.99406197038663890 ) ) ;
#3223=DIRECTION ( 'NONE',  ( -1.000000000000000000, 0.000000000000000000, 0.000000000000000000 ) ) ;
#3224=ORIENTED_EDGE ( 'NONE', *, *, #19175, .F. ) ;
#3228=DIRECTION ( 'NONE',  ( -1.000000000000000000, 0.000000000000000000, 0.000000000000000000 ) ) ;
#3230=CARTESIAN_POINT ( 'NONE',  ( -10.00000000000000000, 0.000000000000000000, 0.000000000000000000 ) ) ;
#3234=EDGE_LOOP ( 'NONE', ( #14699, #18134, #8606, #15597 ) ) ;
#3235=AXIS2_PLACEMENT_3D ( 'NONE', #8186, #19832, #14759 ) ;
#3236=DIRECTION ( 'NONE',  ( -1.000000000000000000, 0.000000000000000000, -0.000000000000000000 ) ) ;
#3238=ORIENTED_EDGE ( 'NONE', *, *, #11240, .F. ) ;
#3245=AXIS2_PLACEMENT_3D ( 'NONE', #17678, #16085, #8029 ) ;
#3247=VERTEX_POINT ( 'NONE', #16084 ) ;
#3248=CARTESIAN_POINT ( 'NONE',  ( -10.00000000000000000, 0.000000000000000000, 0.000000000000000000 ) ) ;
#3251=DIRECTION ( 'NONE',  ( -1.000000000000000000, 0.000000000000000000, -0.000000000000000000 ) ) ;
#3253=ORIENTED_EDGE ( 'NONE', *, *, #4985, .F. ) ;
#3259=EDGE_CURVE ( 'NONE', #8741, #1553, #17004, .T. ) ;
#3266=AXIS2_PLACEMENT_3D ( 'NONE', #19153, #12479, #4834 ) ;
#3269=CARTESIAN_POINT ( 'NONE',  ( 19.99999999999999645, -60.35829202194891252, 24.78524934717529504 ) ) ;
#3272=DIRECTION ( 'NONE',  ( 0.000000000000000000, -0.9976687691905398170, 0.06824241336466072005 ) ) ;
#3273=CIRCLE ( 'NONE', #10034, 27.60000000002759535 ) ;
#3277=CARTESIAN_POINT ( 'NONE',  ( 19.99999999999999645, -56.42118728228132341, -32.77318456705499017 ) ) ;
#3278=CIRCLE ( 'NONE', #19524, 65.24900000006525147 ) ;
#3280=CARTESIAN_POINT ( 'NONE',  ( 0.000000000000000000, -60.35829202194857857, -24.78524934717611572 ) ) ;
#3282=CIRCLE ( 'NONE', #11403, 27.60000000002760601 ) ;
#3283=ORIENTED_EDGE ( 'NONE', *, *, #19521, .T. ) ;
#3286=DIRECTION ( 'NONE',  ( -1.000000000000000000, -0.000000000000000000, -0.000000000000000000 ) ) ;
#3287=ADVANCED_FACE ( 'NONE', ( #8028 ), #20942, .T. ) ;
#3288=AXIS2_PLACEMENT_3D ( 'NONE', #4941, #6418, #14592 ) ;
#3290=DIRECTION ( 'NONE',  ( -1.000000000000000000, 0.000000000000000000, 0.000000000000000000 ) ) ;
#3295=VECTOR ( 'NONE', #14523, 1000.000000000000000 ) ;
#3300=DIRECTION ( 'NONE',  ( 0.000000000000000000, 0.000000000000000000, -1.000000000000000000 ) ) ;
#3301=AXIS2_PLACEMENT_3D ( 'NONE', #20681, #14136, #4475 ) ;
#3303=AXIS2_PLACEMENT_3D ( 'NONE', #424, #20120, #11970 ) ;
#3307=VERTEX_POINT ( 'NONE', #6110 ) ;
#3309=VERTEX_POINT ( 'NONE', #70 ) ;
#3312=ORIENTED_EDGE ( 'NONE', *, *, #17259, .F. ) ;
#3315=CARTESIAN_POINT ( 'NONE',  ( 0.000000000000000000, -0.9548212943360432359, -71.99366858485717557 ) ) ;
#3319=DIRECTION ( 'NONE',  ( -1.000000000000000000, -0.000000000000000000, 0.000000000000000000 ) ) ;
#3320=ORIENTED_EDGE ( 'NONE', *, *, #16116, .F. ) ;
#3323=DIRECTION ( 'NONE',  ( 0.000000000000000000, 0.9976687691905390398, 0.06824241336467466723 ) ) ;
#3326=ADVANCED_FACE ( 'NONE', ( #17784 ), #15869, .T. ) ;
#3332=ORIENTED_EDGE ( 'NONE', *, *, #14716, .T. ) ;
#3334=VERTEX_POINT ( 'NONE', #2944 ) ;
#3335=DIRECTION ( 'NONE',  ( -1.000000000000000000, 0.000000000000000000, 0.000000000000000000 ) ) ;
#3338=VERTEX_POINT ( 'NONE', #1365 ) ;
#3340=DIRECTION ( 'NONE',  ( -1.000000000000000000, 0.000000000000000000, 0.000000000000000000 ) ) ;
#3345=CARTESIAN_POINT ( 'NONE',  ( 19.99999999999999645, 48.70996102988680576, 42.79495875147792106 ) ) ;
#3347=ORIENTED_EDGE ( 'NONE', *, *, #5149, .T. ) ;
#3348=DIRECTION ( 'NONE',  ( -1.000000000000000000, -0.000000000000000000, 0.000000000000000000 ) ) ;
#3352=CARTESIAN_POINT ( 'NONE',  ( 19.99999999999999645, -43.56693332842751687, -48.57318520917550586 ) ) ;
#3354=ORIENTED_EDGE ( 'NONE', *, *, #18282, .F. ) ;
#3355=CYLINDRICAL_SURFACE ( 'NONE', #2952, 27.60000000002760245 ) ;
#3361=DIRECTION ( 'NONE',  ( 0.000000000000000000, 0.000000000000000000, 1.000000000000000000 ) ) ;
#3364=ORIENTED_EDGE ( 'NONE', *, *, #17671, .F. ) ;
#3370=CARTESIAN_POINT ( 'NONE',  ( 19.99999999999999645, -64.80702306891090814, -7.581672767547114944 ) ) ;
#3372=CYLINDRICAL_SURFACE ( 'NONE', #14952, 65.24900000006525147 ) ;
#3375=ORIENTED_EDGE ( 'NONE', *, *, #8127, .F. ) ;
#3377=CARTESIAN_POINT ( 'NONE',  ( 0.000000000000000000, -67.51707036274397922, -25.00890260772446538 ) ) ;
#3384=CIRCLE ( 'NONE', #7793, 27.60000000002759535 ) ;
#3389=ORIENTED_EDGE ( 'NONE', *, *, #9192, .F. ) ;
#3396=DIRECTION ( 'NONE',  ( 0.000000000000000000, 0.000000000000000000, 1.000000000000000000 ) ) ;
#3400=EDGE_CURVE ( 'NONE', #4144, #11163, #18708, .T. ) ;
#3402=ORIENTED_EDGE ( 'NONE', *, *, #13641, .T. ) ;
#3403=DIRECTION ( 'NONE',  ( 0.000000000000000000, -0.2697967711570313232, 0.9629172873477972461 ) ) ;
#3407=VECTOR ( 'NONE', #16481, 1000.000000000000000 ) ;
#3409=ORIENTED_EDGE ( 'NONE', *, *, #7338, .T. ) ;
#3412=CIRCLE ( 'NONE', #20676, 27.60000000002759890 ) ;
#3413=CARTESIAN_POINT ( 'NONE',  ( 0.000000000000000000, 59.36728637278019960, 40.73727173906807764 ) ) ;
#3417=CARTESIAN_POINT ( 'NONE',  ( 19.99999999999999645, -38.69327817041812523, 52.53819777490620169 ) ) ;
#3418=ORIENTED_EDGE ( 'NONE', *, *, #12695, .T. ) ;
#3419=DIRECTION ( 'NONE',  ( 0.000000000000000000, -0.5195839500354229035, -0.8544194045464950094 ) ) ;
#3423=ORIENTED_EDGE ( 'NONE', *, *, #5844, .F. ) ;
#3424=DIRECTION ( 'NONE',  ( 0.000000000000000000, 0.000000000000000000, 1.000000000000000000 ) ) ;
#3425=ORIENTED_EDGE ( 'NONE', *, *, #3867, .F. ) ;
#3431=AXIS2_PLACEMENT_3D ( 'NONE', #4885, #6366, #16015 ) ;
#3437=CIRCLE ( 'NONE', #8853, 72.00000000007199219 ) ;
#3448=CARTESIAN_POINT ( 'NONE',  ( 9.999999999999998224, 8.857208570070804754, -71.45313048675076573 ) ) ;
#3451=VECTOR ( 'NONE', #15978, 1000.000000000000000 ) ;
#3453=EDGE_CURVE ( 'NONE', #18447, #15935, #20047, .T. ) ;
#3455=CIRCLE ( 'NONE', #5478, 72.00000000007199219 ) ;
#3464=DIRECTION ( 'NONE',  ( 0.000000000000000000, -0.6310879443260593025, 0.7757112907044144690 ) ) ;
#3470=DIRECTION ( 'NONE',  ( 0.000000000000000000, 0.000000000000000000, 1.000000000000000000 ) ) ;
#3471=CARTESIAN_POINT ( 'NONE',  ( 0.000000000000000000, 51.43306257653143376, 40.15061736769582268 ) ) ;
#3474=DIRECTION ( 'NONE',  ( 0.000000000000000000, 0.000000000000000000, 1.000000000000000000 ) ) ;
#3479=CARTESIAN_POINT ( 'NONE',  ( 19.99999999999999645, 51.81019761368373366, -38.98425606966007706 ) ) ;
#3487=AXIS2_PLACEMENT_3D ( 'NONE', #18984, #20344, #10922 ) ;
#3488=ORIENTED_EDGE ( 'NONE', *, *, #17541, .F. ) ;
#3492=EDGE_CURVE ( 'NONE', #17770, #14722, #8550, .T. ) ;
#3493=ORIENTED_EDGE ( 'NONE', *, *, #20509, .T. ) ;
#3494=AXIS2_PLACEMENT_3D ( 'NONE', #7761, #4472, #20678 ) ;
#3495=CARTESIAN_POINT ( 'NONE',  ( 19.99999999999999645, 0.000000000000000000, 0.000000000000000000 ) ) ;
#3501=ORIENTED_EDGE ( 'NONE', *, *, #11043, .F. ) ;
#3504=DIRECTION ( 'NONE',  ( -1.000000000000000000, -0.000000000000000000, 0.000000000000000000 ) ) ;
#3512=ADVANCED_FACE ( 'NONE', ( #15319 ), #806, .T. ) ;
#3517=ORIENTED_EDGE ( 'NONE', *, *, #18343, .T. ) ;
#3519=VERTEX_POINT ( 'NONE', #17014 ) ;
#3521=LINE ( 'NONE', #9788, #2249 ) ;
#3522=CARTESIAN_POINT ( 'NONE',  ( 9.999999999999998224, -59.36728637278047671, 40.73727173906767973 ) ) ;
#3531=EDGE_CURVE ( 'NONE', #17620, #254, #19726, .T. ) ;
#3532=CARTESIAN_POINT ( 'NONE',  ( 0.000000000000000000, -51.96384592647165590, -49.83732252579670075 ) ) ;
#3533=EDGE_CURVE ( 'NONE', #17222, #9460, #9582, .T. ) ;
#3534=CARTESIAN_POINT ( 'NONE',  ( 19.99999999999999645, 63.05226888949912478, -15.11556105343395906 ) ) ;
#3537=ORIENTED_EDGE ( 'NONE', *, *, #10477, .F. ) ;
#3541=EDGE_LOOP ( 'NONE', ( #20306, #18788, #20233, #635 ) ) ;
#3544=VERTEX_POINT ( 'NONE', #340 ) ;
#3546=CYLINDRICAL_SURFACE ( 'NONE', #12052, 27.60000000002759535 ) ;
#3551=EDGE_LOOP ( 'NONE', ( #3644, #9218, #121, #10134 ) ) ;
#3553=CARTESIAN_POINT ( 'NONE',  ( 19.99999999999999645, 63.48283426024897835, -33.96954156735303343 ) ) ;
#3555=ORIENTED_EDGE ( 'NONE', *, *, #17909, .F. ) ;
#3562=DIRECTION ( 'NONE',  ( -1.000000000000000000, 0.000000000000000000, -0.000000000000000000 ) ) ;
#3563=DIRECTION ( 'NONE',  ( 0.000000000000000000, 0.000000000000000000, 1.000000000000000000 ) ) ;
#3568=EDGE_CURVE ( 'NONE', #2187, #13609, #558, .T. ) ;
#3569=CIRCLE ( 'NONE', #14097, 27.60000000002759535 ) ;
#3571=EDGE_CURVE ( 'NONE', #16945, #11468, #11856, .T. ) ;
#3572=CARTESIAN_POINT ( 'NONE',  ( 9.999999999999998224, 18.50424539729942808, -69.58155576219097327 ) ) ;
#3575=CARTESIAN_POINT ( 'NONE',  ( 150.0000507999999968, 5.400000000000000355, 1.000000000000000000 ) ) ;
#3579=ORIENTED_EDGE ( 'NONE', *, *, #19224, .F. ) ;
#3584=CARTESIAN_POINT ( 'NONE',  ( 0.000000000000000000, 0.000000000000000000, -7.500000000000000000 ) ) ;
#3587=CIRCLE ( 'NONE', #18539, 27.60000000002759890 ) ;
#3593=CYLINDRICAL_SURFACE ( 'NONE', #7695, 65.24900000006525147 ) ;
#3596=VERTEX_POINT ( 'NONE', #6698 ) ;
#3601=CYLINDRICAL_SURFACE ( 'NONE', #15132, 65.24900000006525147 ) ;
#3604=VERTEX_POINT ( 'NONE', #19932 ) ;
#3606=LINE ( 'NONE', #16432, #20536 ) ;
#3610=EDGE_CURVE ( 'NONE', #18776, #10147, #14581, .T. ) ;
#3614=DIRECTION ( 'NONE',  ( -1.000000000000000000, 0.000000000000000000, -0.000000000000000000 ) ) ;
#3615=ADVANCED_FACE ( 'NONE', ( #11881 ), #453, .T. ) ;
#3624=DIRECTION ( 'NONE',  ( 0.000000000000000000, 0.000000000000000000, 1.000000000000000000 ) ) ;
#3625=ORIENTED_EDGE ( 'NONE', *, *, #16188, .F. ) ;
#3627=CARTESIAN_POINT ( 'NONE',  ( 19.99999999999999645, 54.08351995568706627, 35.76369202524519864 ) ) ;
#3631=LINE ( 'NONE', #19849, #6436 ) ;
#3634=VERTEX_POINT ( 'NONE', #15176 ) ;
#3636=EDGE_CURVE ( 'NONE', #12585, #7176, #2042, .T. ) ;
#3638=CARTESIAN_POINT ( 'NONE',  ( 0.000000000000000000, -31.17893654894269773, 57.31758819669160232 ) ) ;
#3639=ADVANCED_FACE ( 'NONE', ( #16872 ), #13277, .T. ) ;
#3644=ORIENTED_EDGE ( 'NONE', *, *, #8540, .T. ) ;
#3647=VERTEX_POINT ( 'NONE', #18352 ) ;
#3653=EDGE_CURVE ( 'NONE', #1772, #19446, #7111, .T. ) ;
#3655=ORIENTED_EDGE ( 'NONE', *, *, #9080, .F. ) ;
#3661=VERTEX_POINT ( 'NONE', #12105 ) ;
#3664=CARTESIAN_POINT ( 'NONE',  ( 0.000000000000000000, -6.872116855663586321, 64.47358224882414390 ) ) ;
#3668=LINE ( 'NONE', #11734, #5496 ) ;
#3672=AXIS2_PLACEMENT_3D ( 'NONE', #19102, #15907, #14224 ) ;
#3677=ORIENTED_EDGE ( 'NONE', *, *, #3770, .T. ) ;
#3678=CARTESIAN_POINT ( 'NONE',  ( 19.99999999999999645, -63.05226888949880504, -15.11556105343524514 ) ) ;
#3679=ORIENTED_EDGE ( 'NONE', *, *, #17282, .T. ) ;
#3680=CARTESIAN_POINT ( 'NONE',  ( 19.99999999999999645, 27.62776854598936538, -58.65812137498974721 ) ) ;
#3682=VERTEX_POINT ( 'NONE', #3059 ) ;
#3683=ORIENTED_EDGE ( 'NONE', *, *, #17475, .F. ) ;
#3686=CARTESIAN_POINT ( 'NONE',  ( 0.000000000000000000, -59.31169354540756444, 27.19476070466835438 ) ) ;
#3691=CARTESIAN_POINT ( 'NONE',  ( 0.000000000000000000, 18.50424539729942808, -69.58155576219097327 ) ) ;
#3696=ORIENTED_EDGE ( 'NONE', *, *, #10532, .T. ) ;
#3699=CARTESIAN_POINT ( 'NONE',  ( 0.000000000000000000, 0.000000000000000000, 0.000000000000000000 ) ) ;
#3702=CIRCLE ( 'NONE', #15898, 72.00000000007199219 ) ;
#3703=ORIENTED_EDGE ( 'NONE', *, *, #14681, .T. ) ;
#3705=CARTESIAN_POINT ( 'NONE',  ( 19.99999999999999645, 0.000000000000000000, 0.000000000000000000 ) ) ;
#3708=CYLINDRICAL_SURFACE ( 'NONE', #19167, 27.60000000002759890 ) ;
#3709=DIRECTION ( 'NONE',  ( -1.000000000000000000, -0.000000000000000000, -0.000000000000000000 ) ) ;
#3713=AXIS2_PLACEMENT_3D ( 'NONE', #5653, #20598, #18810 ) ;
#3717=VERTEX_POINT ( 'NONE', #13807 ) ;
#3719=ORIENTED_EDGE ( 'NONE', *, *, #2752, .F. ) ;
#3721=DIRECTION ( 'NONE',  ( 0.000000000000000000, 0.000000000000000000, 1.000000000000000000 ) ) ;
#3722=CIRCLE ( 'NONE', #15583, 27.60000000002760601 ) ;
#3723=ORIENTED_EDGE ( 'NONE', *, *, #12491, .T. ) ;
#3727=CARTESIAN_POINT ( 'NONE',  ( 19.99999999999999645, -1.971042061628798470, 64.80882494896106039 ) ) ;
#3729=ORIENTED_EDGE ( 'NONE', *, *, #8582, .T. ) ;
#3733=VECTOR ( 'NONE', #5318, 1000.000000000000000 ) ;
#3742=ORIENTED_EDGE ( 'NONE', *, *, #150, .F. ) ;
#3746=CARTESIAN_POINT ( 'NONE',  ( 19.99999999999999645, -18.50424539729892359, 69.58155576219108696 ) ) ;
#3749=CIRCLE ( 'NONE', #7822, 27.60000000002759890 ) ;
#3750=ADVANCED_FACE ( 'NONE', ( #14307 ), #5624, .T. ) ;
#3752=CARTESIAN_POINT ( 'NONE',  ( 19.99999999999999645, 1.971042061628357933, 64.80882494896107460 ) ) ;
#3755=DIRECTION ( 'NONE',  ( -1.000000000000000000, -0.000000000000000000, 0.000000000000000000 ) ) ;
#3759=ADVANCED_FACE ( 'NONE', ( #5725 ), #868, .T. ) ;
#3763=ORIENTED_EDGE ( 'NONE', *, *, #18343, .F. ) ;
#3764=FACE_OUTER_BOUND ( 'NONE', #7305, .T. ) ;
#3765=ADVANCED_FACE ( 'NONE', ( #13904 ), #7321, .T. ) ;
#3767=EDGE_CURVE ( 'NONE', #141, #5576, #19633, .T. ) ;
#3770=EDGE_CURVE ( 'NONE', #7037, #4233, #3384, .T. ) ;
#3784=FACE_OUTER_BOUND ( 'NONE', #18898, .T. ) ;
#3785=CARTESIAN_POINT ( 'NONE',  ( 19.99999999999999645, 63.05226888949891162, 15.11556105343481882 ) ) ;
#3788=ADVANCED_FACE ( 'NONE', ( #14414 ), #17487, .T. ) ;
#3791=AXIS2_PLACEMENT_3D ( 'NONE', #8035, #11210, #11113 ) ;
#3792=AXIS2_PLACEMENT_3D ( 'NONE', #10664, #4293, #17334 ) ;
#3795=LINE ( 'NONE', #846, #6006 ) ;
#3796=DIRECTION ( 'NONE',  ( 1.000000000000000000, 0.000000000000000000, 0.000000000000000000 ) ) ;
#3804=ORIENTED_EDGE ( 'NONE', *, *, #3653, .F. ) ;
#3806=ADVANCED_FACE ( 'NONE', ( #13694 ), #16259, .T. ) ;
#3808=ORIENTED_EDGE ( 'NONE', *, *, #14738, .F. ) ;
#3812=CYLINDRICAL_SURFACE ( 'NONE', #15681, 27.60000000002760245 ) ;
#3815=AXIS2_PLACEMENT_3D ( 'NONE', #17913, #305, #7951 ) ;
#3817=CARTESIAN_POINT ( 'NONE',  ( 0.000000000000000000, 0.000000000000000000, 0.000000000000000000 ) ) ;
#3818=DIRECTION ( 'NONE',  ( 0.000000000000000000, 0.000000000000000000, -1.000000000000000000 ) ) ;
#3820=DIRECTION ( 'NONE',  ( 1.000000000000000000, -0.000000000000000000, -0.000000000000000000 ) ) ;
#3822=CIRCLE ( 'NONE', #10627, 65.24900000006525147 ) ;
#3825=VERTEX_POINT ( 'NONE', #2047 ) ;
#3829=ADVANCED_FACE ( 'NONE', ( #1746 ), #13188, .T. ) ;
#3830=CARTESIAN_POINT ( 'NONE',  ( 19.99999999999999645, -64.79224928664389438, 25.14373648582931864 ) ) ;
#3831=ORIENTED_EDGE ( 'NONE', *, *, #8684, .F. ) ;
#3836=EDGE_LOOP ( 'NONE', ( #8434, #12612, #11629, #11127 ) ) ;
#3838=VECTOR ( 'NONE', #6290, 1000.000000000000000 ) ;
#3839=CARTESIAN_POINT ( 'NONE',  ( 19.99999999999999645, 10.74906464462118372, 71.19310085447972369 ) ) ;
#3842=AXIS2_PLACEMENT_3D ( 'NONE', #1098, #7333, #4370 ) ;
#3844=DIRECTION ( 'NONE',  ( -1.000000000000000000, -0.000000000000000000, -0.000000000000000000 ) ) ;
#3846=ORIENTED_EDGE ( 'NONE', *, *, #18298, .F. ) ;
#3847=DIRECTION ( 'NONE',  ( 0.000000000000000000, -0.8878852184023794392, 0.4600650377311439887 ) ) ;
#3853=ORIENTED_EDGE ( 'NONE', *, *, #1481, .F. ) ;
#3855=DIRECTION ( 'NONE',  ( 0.000000000000000000, 0.2697967711570182225, 0.9629172873478010208 ) ) ;
#3856=LINE ( 'NONE', #15521, #14783 ) ;
#3857=CIRCLE ( 'NONE', #15722, 65.24900000006523726 ) ;
#3859=CARTESIAN_POINT ( 'NONE',  ( 0.000000000000000000, 0.000000000000000000, 0.000000000000000000 ) ) ;
#3867=EDGE_CURVE ( 'NONE', #5132, #2314, #3722, .T. ) ;
#3868=DIRECTION ( 'NONE',  ( -1.000000000000000000, 0.000000000000000000, 0.000000000000000000 ) ) ;
#3873=EDGE_CURVE ( 'NONE', #1539, #8201, #3631, .T. ) ;
#3879=DIRECTION ( 'NONE',  ( 0.000000000000000000, 0.9422609221188191775, 0.3348796121709901041 ) ) ;
#3884=AXIS2_PLACEMENT_3D ( 'NONE', #2903, #14152, #9682 ) ;
#3890=EDGE_CURVE ( 'NONE', #3519, #8383, #19747, .T. ) ;
#3891=EDGE_CURVE ( 'NONE', #12535, #3064, #18640, .T. ) ;
#3892=DIRECTION ( 'NONE',  ( 0.000000000000000000, 0.9790840876823234673, -0.2034560130526309185 ) ) ;
#3893=CARTESIAN_POINT ( 'NONE',  ( 0.000000000000000000, 0.000000000000000000, 72.00000000007199219 ) ) ;
#3904=ORIENTED_EDGE ( 'NONE', *, *, #2347, .F. ) ;
#3905=DIRECTION ( 'NONE',  ( -1.000000000000000000, 0.000000000000000000, -0.000000000000000000 ) ) ;
#3907=CYLINDRICAL_SURFACE ( 'NONE', #11657, 72.00000000007199219 ) ;
#3909=ORIENTED_EDGE ( 'NONE', *, *, #18825, .F. ) ;
#3912=ORIENTED_EDGE ( 'NONE', *, *, #19682, .F. ) ;
#3913=CYLINDRICAL_SURFACE ( 'NONE', #2759, 27.60000000002759890 ) ;
#3915=ORIENTED_EDGE ( 'NONE', *, *, #8388, .F. ) ;
#3917=CYLINDRICAL_SURFACE ( 'NONE', #5611, 27.60000000002759890 ) ;
#3920=( NAMED_UNIT ( * ) PLANE_ANGLE_UNIT ( ) SI_UNIT ( $, .RADIAN. ) );
#3921=DIRECTION ( 'NONE',  ( 0.000000000000000000, 0.000000000000000000, 1.000000000000000000 ) ) ;
#3923=DIRECTION ( 'NONE',  ( 1.000000000000000000, 0.000000000000000000, 0.000000000000000000 ) ) ;
#3925=DIRECTION ( 'NONE',  ( -1.000000000000000000, -0.000000000000000000, -0.000000000000000000 ) ) ;
#3927=CARTESIAN_POINT ( 'NONE',  ( 0.000000000000000000, 0.000000000000000000, 0.000000000000000000 ) ) ;
#3928=AXIS2_PLACEMENT_3D ( 'NONE', #19077, #4553, #2968 ) ;
#3931=DIRECTION ( 'NONE',  ( 0.000000000000000000, 0.000000000000000000, 1.000000000000000000 ) ) ;
#3932=ORIENTED_EDGE ( 'NONE', *, *, #2262, .F. ) ;
#3934=CARTESIAN_POINT ( 'NONE',  ( -65.00002539999999840, 0.000000000000000000, 0.000000000000000000 ) ) ;
#3936=CARTESIAN_POINT ( 'NONE',  ( 19.99999999999999645, -54.08351995568730786, 35.76369202524482915 ) ) ;
#3937=EDGE_LOOP ( 'NONE', ( #5520, #480, #4060, #3025 ) ) ;
#3941=ORIENTED_EDGE ( 'NONE', *, *, #6424, .F. ) ;
#3942=LINE ( 'NONE', #10430, #19155 ) ;
#3945=CARTESIAN_POINT ( 'NONE',  ( 19.99999999999999645, 0.000000000000000000, 0.000000000000000000 ) ) ;
#3948=VECTOR ( 'NONE', #2830, 1000.000000000000000 ) ;
#3952=ORIENTED_EDGE ( 'NONE', *, *, #3142, .F. ) ;
#3956=ORIENTED_EDGE ( 'NONE', *, *, #10477, .T. ) ;
#3959=ORIENTED_EDGE ( 'NONE', *, *, #13412, .F. ) ;
#3966=CARTESIAN_POINT ( 'NONE',  ( 0.000000000000000000, 71.76067541710851572, 5.865617076724869428 ) ) ;
#3967=ORIENTED_EDGE ( 'NONE', *, *, #13897, .F. ) ;
#3969=AXIS2_PLACEMENT_3D ( 'NONE', #18081, #19560, #10125 ) ;
#3971=DIRECTION ( 'NONE',  ( 0.000000000000000000, 0.9422609221188213979, -0.3348796121709836648 ) ) ;
#3973=ORIENTED_EDGE ( 'NONE', *, *, #18256, .F. ) ;
#3982=DIRECTION ( 'NONE',  ( 0.000000000000000000, -0.9976687691905385957, -0.06824241336468162000 ) ) ;
#3985=EDGE_CURVE ( 'NONE', #7047, #4150, #1949, .T. ) ;
#3994=EDGE_LOOP ( 'NONE', ( #9300, #8665, #12301, #14059 ) ) ;
#3997=DIRECTION ( 'NONE',  ( -1.000000000000000000, 0.000000000000000000, -0.000000000000000000 ) ) ;
#3998=CARTESIAN_POINT ( 'NONE',  ( 150.0000507999999968, 5.400000000000000355, -1.000000000000000000 ) ) ;
#4005=EDGE_CURVE ( 'NONE', #5332, #19322, #8478, .T. ) ;
#4009=EDGE_CURVE ( 'NONE', #17803, #15688, #12905, .T. ) ;
#4011=CARTESIAN_POINT ( 'NONE',  ( -10.00000000000000000, 0.000000000000000000, 0.000000000000000000 ) ) ;
#4019=EDGE_CURVE ( 'NONE', #7176, #5705, #17962, .T. ) ;
#4021=DIRECTION ( 'NONE',  ( -1.000000000000000000, 0.000000000000000000, -0.000000000000000000 ) ) ;
#4024=( LENGTH_UNIT ( ) NAMED_UNIT ( * ) SI_UNIT ( .MILLI., .METRE. ) );
#4029=CARTESIAN_POINT ( 'NONE',  ( 19.99999999999999645, -19.38316218894255627, 61.87375713200982119 ) ) ;
#4037=ADVANCED_FACE ( 'NONE', ( #8928 ), #15283, .T. ) ;
#4038=ORIENTED_EDGE ( 'NONE', *, *, #1490, .T. ) ;
#4045=CARTESIAN_POINT ( 'NONE',  ( 0.000000000000000000, 0.000000000000000000, 0.000000000000000000 ) ) ;
#4048=DIRECTION ( 'NONE',  ( -1.000000000000000000, -0.000000000000000000, -0.000000000000000000 ) ) ;
#4049=DIRECTION ( 'NONE',  ( -1.000000000000000000, 0.000000000000000000, -0.000000000000000000 ) ) ;
#4055=ADVANCED_FACE ( 'NONE', ( #5526 ), #10638, .T. ) ;
#4056=FACE_OUTER_BOUND ( 'NONE', #17062, .T. ) ;
#4060=ORIENTED_EDGE ( 'NONE', *, *, #1446, .T. ) ;
#4062=DIRECTION ( 'NONE',  ( -1.000000000000000000, 0.000000000000000000, -0.000000000000000000 ) ) ;
#4064=EDGE_LOOP ( 'NONE', ( #13615, #9861, #16001, #19899 ) ) ;
#4065=DIRECTION ( 'NONE',  ( 0.000000000000000000, 0.1361666490962400722, 0.9906859460363316439 ) ) ;
#4073=DIRECTION ( 'NONE',  ( 1.000000000000000000, -0.000000000000000000, -0.000000000000000000 ) ) ;
#4078=ORIENTED_EDGE ( 'NONE', *, *, #19175, .T. ) ;
#4080=ORIENTED_EDGE ( 'NONE', *, *, #10392, .F. ) ;
#4086=DIRECTION ( 'NONE',  ( -1.000000000000000000, -0.000000000000000000, -0.000000000000000000 ) ) ;
#4087=CARTESIAN_POINT ( 'NONE',  ( 0.000000000000000000, 19.38316218894212639, 61.87375713200996330 ) ) ;
#4088=EDGE_LOOP ( 'NONE', ( #12384, #14226, #7359, #16071 ) ) ;
#4090=ORIENTED_EDGE ( 'NONE', *, *, #4414, .T. ) ;
#4094=ORIENTED_EDGE ( 'NONE', *, *, #16869, .T. ) ;
#4095=ORIENTED_EDGE ( 'NONE', *, *, #15439, .T. ) ;
#4098=AXIS2_PLACEMENT_3D ( 'NONE', #7377, #822, #18620 ) ;
#4101=DIRECTION ( 'NONE',  ( 0.000000000000000000, 0.000000000000000000, 1.000000000000000000 ) ) ;
#4102=AXIS2_PLACEMENT_3D ( 'NONE', #14527, #4870, #16409 ) ;
#4104=DIRECTION ( 'NONE',  ( -1.000000000000000000, -0.000000000000000000, -0.000000000000000000 ) ) ;
#4106=PLANE ( 'NONE',  #8282 ) ;
#4109=AXIS2_PLACEMENT_3D ( 'NONE', #9131, #15270, #15384 ) ;
#4115=ORIENTED_EDGE ( 'NONE', *, *, #17918, .F. ) ;
#4119=AXIS2_PLACEMENT_3D ( 'NONE', #4445, #10913, #20560 ) ;
#4122=ORIENTED_EDGE ( 'NONE', *, *, #15323, .F. ) ;
#4124=DIRECTION ( 'NONE',  ( 0.000000000000000000, 0.8169698930104393186, 0.5766803221148710801 ) ) ;
#4129=AXIS2_PLACEMENT_3D ( 'NONE', #15461, #15554, #1050 ) ;
#4130=EDGE_CURVE ( 'NONE', #18621, #11808, #20663, .T. ) ;
#4131=CIRCLE ( 'NONE', #10575, 27.60000000002760245 ) ;
#4140=CIRCLE ( 'NONE', #14986, 27.60000000002760245 ) ;
#4144=VERTEX_POINT ( 'NONE', #20044 ) ;
#4150=VERTEX_POINT ( 'NONE', #12006 ) ;
#4152=CYLINDRICAL_SURFACE ( 'NONE', #17397, 72.00000000007199219 ) ;
#4156=CARTESIAN_POINT ( 'NONE',  ( 19.99999999999999645, 0.000000000000000000, 0.000000000000000000 ) ) ;
#4164=LINE ( 'NONE', #671, #6564 ) ;
#4170=AXIS2_PLACEMENT_3D ( 'NONE', #5327, #18362, #16977 ) ;
#4171=ORIENTED_EDGE ( 'NONE', *, *, #20774, .T. ) ;
#4172=CARTESIAN_POINT ( 'NONE',  ( 0.000000000000000000, 0.000000000000000000, 0.000000000000000000 ) ) ;
#4189=ORIENTED_EDGE ( 'NONE', *, *, #8496, .F. ) ;
#4190=VECTOR ( 'NONE', #3319, 1000.000000000000000 ) ;
#4192=EDGE_CURVE ( 'NONE', #17681, #141, #12762, .T. ) ;
#4193=CARTESIAN_POINT ( 'NONE',  ( 0.000000000000000000, 28.84646472442454979, 58.52617768068444093 ) ) ;
#4200=CARTESIAN_POINT ( 'NONE',  ( 19.99999999999999645, -10.74906464462069167, -71.19310085447979475 ) ) ;
#4201=ORIENTED_EDGE ( 'NONE', *, *, #16066, .F. ) ;
#4202=LINE ( 'NONE', #13851, #13194 ) ;
#4204=CIRCLE ( 'NONE', #3194, 27.60000000002759890 ) ;
#4207=ORIENTED_EDGE ( 'NONE', *, *, #15117, .F. ) ;
#4211=ORIENTED_EDGE ( 'NONE', *, *, #16340, .F. ) ;
#4217=VERTEX_POINT ( 'NONE', #9557 ) ;
#4219=VECTOR ( 'NONE', #16881, 1000.000000000000000 ) ;
#4220=CARTESIAN_POINT ( 'NONE',  ( 9.999999999999998224, 64.36139404985965484, 32.27399814043898374 ) ) ;
#4221=CYLINDRICAL_SURFACE ( 'NONE', #12418, 65.24900000006525147 ) ;
#4222=DIRECTION ( 'NONE',  ( 0.000000000000000000, 0.000000000000000000, 1.000000000000000000 ) ) ;
#4230=EDGE_CURVE ( 'NONE', #8697, #4546, #10518, .T. ) ;
#4233=VERTEX_POINT ( 'NONE', #14454 ) ;
#4235=CARTESIAN_POINT ( 'NONE',  ( 0.000000000000000000, 63.48283426024851650, 33.96954156735390740 ) ) ;
#4237=ORIENTED_EDGE ( 'NONE', *, *, #11804, .F. ) ;
#4243=ORIENTED_EDGE ( 'NONE', *, *, #6100, .F. ) ;
#4252=DIRECTION ( 'NONE',  ( -1.000000000000000000, 0.000000000000000000, 0.000000000000000000 ) ) ;
#4253=DIRECTION ( 'NONE',  ( -1.000000000000000000, 0.000000000000000000, 0.000000000000000000 ) ) ;
#4255=ORIENTED_EDGE ( 'NONE', *, *, #5061, .F. ) ;
#4258=EDGE_LOOP ( 'NONE', ( #5088, #8970, #5031, #681 ) ) ;
#4261=ORIENTED_EDGE ( 'NONE', *, *, #1854, .F. ) ;
#4263=CARTESIAN_POINT ( 'NONE',  ( 19.99999999999999645, 64.44931368725519860, 10.18420179740629727 ) ) ;
#4265=AXIS2_PLACEMENT_3D ( 'NONE', #14019, #2772, #8073 ) ;
#4269=CARTESIAN_POINT ( 'NONE',  ( -65.00002539999999840, 9.184850993605147944E-16, 7.500000000000000000 ) ) ;
#4271=CARTESIAN_POINT ( 'NONE',  ( 19.99999999999999645, 49.77519642624007901, 42.18840861821802690 ) ) ;
#4272=LINE ( 'NONE', #10949, #13822 ) ;
#4280=DIRECTION ( 'NONE',  ( -1.000000000000000000, 0.000000000000000000, -0.000000000000000000 ) ) ;
#4282=DIRECTION ( 'NONE',  ( -1.000000000000000000, -0.000000000000000000, -0.000000000000000000 ) ) ;
#4284=CARTESIAN_POINT ( 'NONE',  ( 0.000000000000000000, 0.000000000000000000, 0.000000000000000000 ) ) ;
#4285=DIRECTION ( 'NONE',  ( -1.000000000000000000, 0.000000000000000000, -0.000000000000000000 ) ) ;
#4286=ORIENTED_EDGE ( 'NONE', *, *, #8961, .F. ) ;
#4288=AXIS2_PLACEMENT_3D ( 'NONE', #15260, #12093, #4124 ) ;
#4292=EDGE_CURVE ( 'NONE', #7789, #9697, #17529, .T. ) ;
#4293=DIRECTION ( 'NONE',  ( -1.000000000000000000, -0.000000000000000000, 0.000000000000000000 ) ) ;
#4296=CARTESIAN_POINT ( 'NONE',  ( 19.99999999999999645, 0.000000000000000000, 0.000000000000000000 ) ) ;
#4297=AXIS2_PLACEMENT_3D ( 'NONE', #14532, #13350, #17916 ) ;
#4299=ORIENTED_EDGE ( 'NONE', *, *, #13558, .F. ) ;
#4310=DIRECTION ( 'NONE',  ( 0.000000000000000000, 0.000000000000000000, -1.000000000000000000 ) ) ;
#4314=VECTOR ( 'NONE', #14203, 1000.000000000000000 ) ;
#4318=DIRECTION ( 'NONE',  ( -1.000000000000000000, 0.000000000000000000, 0.000000000000000000 ) ) ;
#4319=ORIENTED_EDGE ( 'NONE', *, *, #20509, .F. ) ;
#4320=EDGE_CURVE ( 'NONE', #6274, #17007, #328, .T. ) ;
#4321=CARTESIAN_POINT ( 'NONE',  ( 19.99999999999999645, 0.000000000000000000, 0.000000000000000000 ) ) ;
#4322=DIRECTION ( 'NONE',  ( -1.000000000000000000, 0.000000000000000000, 0.000000000000000000 ) ) ;
#4323=ORIENTED_EDGE ( 'NONE', *, *, #6615, .F. ) ;
#4330=DIRECTION ( 'NONE',  ( 0.000000000000000000, 0.000000000000000000, 1.000000000000000000 ) ) ;
#4332=CYLINDRICAL_SURFACE ( 'NONE', #19016, 27.60000000002759890 ) ;
#4337=UNCERTAINTY_MEASURE_WITH_UNIT (LENGTH_MEASURE( 1.000000000000000082E-05 ), #4024, 'distance_accuracy_value', 'NONE');
#4339=EDGE_LOOP ( 'NONE', ( #8825, #6400, #4631, #13400 ) ) ;
#4347=CARTESIAN_POINT ( 'NONE',  ( 19.99999999999999645, 0.000000000000000000, 0.000000000000000000 ) ) ;
#4349=DIRECTION ( 'NONE',  ( 0.000000000000000000, -0.8169698930104356549, -0.5766803221148764091 ) ) ;
#4352=DIRECTION ( 'NONE',  ( -1.000000000000000000, -0.000000000000000000, -0.000000000000000000 ) ) ;
#4356=EDGE_CURVE ( 'NONE', #18180, #6701, #11253, .T. ) ;
#4357=FILL_AREA_STYLE_COLOUR ( '', #16152 ) ;
#4358=LINE ( 'NONE', #9442, #15349 ) ;
#4361=CARTESIAN_POINT ( 'NONE',  ( 9.999999999999998224, -46.17500197033020015, -55.24372537266445704 ) ) ;
#4363=DIRECTION ( 'NONE',  ( -1.000000000000000000, 0.000000000000000000, -0.000000000000000000 ) ) ;
#4368=DIRECTION ( 'NONE',  ( 1.000000000000000000, -0.000000000000000000, -0.000000000000000000 ) ) ;
#4370=DIRECTION ( 'NONE',  ( 0.000000000000000000, 0.3984010898462422845, -0.9172113015054527141 ) ) ;
#4371=ORIENTED_EDGE ( 'NONE', *, *, #12460, .T. ) ;
#4374=DIRECTION ( 'NONE',  ( 0.000000000000000000, -0.7308359642781302457, 0.6825531432186475733 ) ) ;
#4375=EDGE_LOOP ( 'NONE', ( #5203, #17782, #16517, #14685 ) ) ;
#4379=DIRECTION ( 'NONE',  ( -1.000000000000000000, 0.000000000000000000, 0.000000000000000000 ) ) ;
#4383=CARTESIAN_POINT ( 'NONE',  ( 19.99999999999999645, -65.23577793412346182, 1.313498510941474740 ) ) ;
#4384=LINE ( 'NONE', #20496, #7447 ) ;
#4385=ORIENTED_EDGE ( 'NONE', *, *, #15915, .T. ) ;
#4390=CARTESIAN_POINT ( 'NONE',  ( 150.0000507999999968, 0.000000000000000000, 0.000000000000000000 ) ) ;
#4394=DIRECTION ( 'NONE',  ( -1.000000000000000000, 0.000000000000000000, -0.000000000000000000 ) ) ;
#4396=DIRECTION ( 'NONE',  ( 0.000000000000000000, 0.8169698930104392076, 0.5766803221148710801 ) ) ;
#4399=APPLICATION_CONTEXT ( 'automotive_design' ) ;
#4412=CIRCLE ( 'NONE', #19968, 72.00000000007199219 ) ;
#4414=EDGE_CURVE ( 'NONE', #10695, #12643, #9185, .T. ) ;
#4419=ORIENTED_EDGE ( 'NONE', *, *, #14792, .T. ) ;
#4424=DIRECTION ( 'NONE',  ( -1.000000000000000000, -0.000000000000000000, -0.000000000000000000 ) ) ;
#4426=DIRECTION ( 'NONE',  ( 0.000000000000000000, 0.000000000000000000, 1.000000000000000000 ) ) ;
#4427=CIRCLE ( 'NONE', #10171, 27.60000000002759890 ) ;
#4432=EDGE_CURVE ( 'NONE', #1628, #6474, #374, .T. ) ;
#4435=AXIS2_PLACEMENT_3D ( 'NONE', #3727, #5740, #8812 ) ;
#4436=ORIENTED_EDGE ( 'NONE', *, *, #6100, .T. ) ;
#4437=DIRECTION ( 'NONE',  ( -1.000000000000000000, -0.000000000000000000, 0.000000000000000000 ) ) ;
#4441=CARTESIAN_POINT ( 'NONE',  ( 0.000000000000000000, 0.000000000000000000, 0.000000000000000000 ) ) ;
#4445=CARTESIAN_POINT ( 'NONE',  ( 0.000000000000000000, 0.000000000000000000, 0.000000000000000000 ) ) ;
#4446=ORIENTED_EDGE ( 'NONE', *, *, #986, .F. ) ;
#4449=VERTEX_POINT ( 'NONE', #11466 ) ;
#4451=VERTEX_POINT ( 'NONE', #437 ) ;
#4455=DIRECTION ( 'NONE',  ( 0.000000000000000000, 0.000000000000000000, 1.000000000000000000 ) ) ;
#4456=EDGE_CURVE ( 'NONE', #2016, #5196, #8173, .T. ) ;
#4458=CIRCLE ( 'NONE', #15637, 27.60000000002759890 ) ;
#4461=FACE_OUTER_BOUND ( 'NONE', #13655, .T. ) ;
#4463=DIRECTION ( 'NONE',  ( -1.000000000000000000, 0.000000000000000000, 0.000000000000000000 ) ) ;
#4467=VERTEX_POINT ( 'NONE', #13571 ) ;
#4471=VERTEX_POINT ( 'NONE', #745 ) ;
#4472=DIRECTION ( 'NONE',  ( -1.000000000000000000, -0.000000000000000000, 0.000000000000000000 ) ) ;
#4475=DIRECTION ( 'NONE',  ( 0.000000000000000000, 0.000000000000000000, 1.000000000000000000 ) ) ;
#4476=CARTESIAN_POINT ( 'NONE',  ( 19.99999999999999645, -19.38316218894168586, -61.87375713201008409 ) ) ;
#4478=DIRECTION ( 'NONE',  ( 0.000000000000000000, -0.8169698930104469792, 0.5766803221148600889 ) ) ;
#4481=AXIS2_PLACEMENT_3D ( 'NONE', #2305, #8650, #15128 ) ;
#4488=CARTESIAN_POINT ( 'NONE',  ( 85.00002539999999840, 3.872983346207417021, 1.000000000000000000 ) ) ;
#4489=DIRECTION ( 'NONE',  ( 0.000000000000000000, 0.000000000000000000, 1.000000000000000000 ) ) ;
#4494=EDGE_CURVE ( 'NONE', #10263, #18180, #8823, .T. ) ;
#4495=AXIS2_PLACEMENT_3D ( 'NONE', #14166, #14259, #7891 ) ;
#4496=ORIENTED_EDGE ( 'NONE', *, *, #12465, .F. ) ;
#4506=AXIS2_PLACEMENT_3D ( 'NONE', #9904, #11399, #4726 ) ;
#4508=AXIS2_PLACEMENT_3D ( 'NONE', #11490, #477, #14883 ) ;
#4511=EDGE_CURVE ( 'NONE', #16270, #2251, #10191, .T. ) ;
#4514=FACE_BOUND ( 'NONE', #18203, .T. ) ;
#4516=ORIENTED_EDGE ( 'NONE', *, *, #14170, .F. ) ;
#4523=AXIS2_PLACEMENT_3D ( 'NONE', #16441, #1930, #10503 ) ;
#4525=FACE_OUTER_BOUND ( 'NONE', #9708, .T. ) ;
#4528=ADVANCED_FACE ( 'NONE', ( #16860 ), #20242, .T. ) ;
#4532=AXIS2_PLACEMENT_3D ( 'NONE', #16969, #18250, #7011 ) ;
#4535=AXIS2_PLACEMENT_3D ( 'NONE', #16842, #13662, #2109 ) ;
#4542=AXIS2_PLACEMENT_3D ( 'NONE', #18456, #3923, #10406 ) ;
#4543=ADVANCED_FACE ( 'NONE', ( #10396 ), #3913, .T. ) ;
#4544=CIRCLE ( 'NONE', #2165, 65.24900000006525147 ) ;
#4546=VERTEX_POINT ( 'NONE', #5713 ) ;
#4550=AXIS2_PLACEMENT_3D ( 'NONE', #13171, #17941, #11566 ) ;
#4552=DIRECTION ( 'NONE',  ( -1.000000000000000000, 0.000000000000000000, 0.000000000000000000 ) ) ;
#4553=DIRECTION ( 'NONE',  ( 1.000000000000000000, 0.000000000000000000, 0.000000000000000000 ) ) ;
#4554=DIRECTION ( 'NONE',  ( -1.000000000000000000, -0.000000000000000000, 0.000000000000000000 ) ) ;
#4555=ORIENTED_EDGE ( 'NONE', *, *, #17653, .F. ) ;
#4556=ADVANCED_FACE ( 'NONE', ( #18448 ), #19921, .T. ) ;
#4557=DIRECTION ( 'NONE',  ( -1.000000000000000000, -0.000000000000000000, -0.000000000000000000 ) ) ;
#4559=VECTOR ( 'NONE', #16770, 1000.000000000000000 ) ;
#4560=DIRECTION ( 'NONE',  ( 1.000000000000000000, 0.000000000000000000, 0.000000000000000000 ) ) ;
#4561=DIRECTION ( 'NONE',  ( 0.000000000000000000, 0.000000000000000000, 1.000000000000000000 ) ) ;
#4562=EDGE_CURVE ( 'NONE', #12535, #10231, #14936, .T. ) ;
#4563=ORIENTED_EDGE ( 'NONE', *, *, #8441, .T. ) ;
#4578=ORIENTED_EDGE ( 'NONE', *, *, #10645, .F. ) ;
#4580=ORIENTED_EDGE ( 'NONE', *, *, #10663, .T. ) ;
#4586=EDGE_LOOP ( 'NONE', ( #5024, #11019, #6160, #16405 ) ) ;
#4587=DIRECTION ( 'NONE',  ( -1.000000000000000000, 0.000000000000000000, -0.000000000000000000 ) ) ;
#4592=CARTESIAN_POINT ( 'NONE',  ( 19.99999999999999645, 6.872116855663142232, 64.47358224882421496 ) ) ;
#4594=LINE ( 'NONE', #5966, #8301 ) ;
#4596=DIRECTION ( 'NONE',  ( 0.000000000000000000, 0.1361666490962468723, -0.9906859460363306447 ) ) ;
#4601=DIRECTION ( 'NONE',  ( 0.000000000000000000, -0.9976687691905384847, -0.06824241336468166164 ) ) ;
#4606=DIRECTION ( 'NONE',  ( -1.000000000000000000, -0.000000000000000000, -0.000000000000000000 ) ) ;
#4608=ORIENTED_EDGE ( 'NONE', *, *, #2597, .T. ) ;
#4610=VERTEX_POINT ( 'NONE', #10496 ) ;
#4611=CYLINDRICAL_SURFACE ( 'NONE', #15287, 72.00000000007199219 ) ;
#4615=VECTOR ( 'NONE', #13420, 1000.000000000000000 ) ;
#4617=EDGE_CURVE ( 'NONE', #20554, #14177, #3749, .T. ) ;
#4618=DIRECTION ( 'NONE',  ( 0.000000000000000000, 0.000000000000000000, 1.000000000000000000 ) ) ;
#4620=ORIENTED_EDGE ( 'NONE', *, *, #10209, .F. ) ;
#4623=ORIENTED_EDGE ( 'NONE', *, *, #4820, .F. ) ;
#4629=AXIS2_PLACEMENT_3D ( 'NONE', #15130, #20096, #3879 ) ;
#4631=ORIENTED_EDGE ( 'NONE', *, *, #8540, .F. ) ;
#4639=ORIENTED_EDGE ( 'NONE', *, *, #5061, .T. ) ;
#4640=CARTESIAN_POINT ( 'NONE',  ( 19.99999999999999645, -62.46228066917775834, -18.86519267363519958 ) ) ;
#4641=DIRECTION ( 'NONE',  ( -1.000000000000000000, 0.000000000000000000, 0.000000000000000000 ) ) ;
#4642=EDGE_CURVE ( 'NONE', #2640, #3596, #7141, .T. ) ;
#4652=EDGE_CURVE ( 'NONE', #5613, #8436, #14606, .T. ) ;
#4658=VECTOR ( 'NONE', #20125, 1000.000000000000000 ) ;
#4661=AXIS2_PLACEMENT_3D ( 'NONE', #7228, #10320, #18067 ) ;
#4664=ORIENTED_EDGE ( 'NONE', *, *, #19260, .T. ) ;
#4665=DIRECTION ( 'NONE',  ( 0.000000000000000000, 0.000000000000000000, 1.000000000000000000 ) ) ;
#4666=AXIS2_PLACEMENT_3D ( 'NONE', #9635, #6126, #17589 ) ;
#4669=FACE_OUTER_BOUND ( 'NONE', #14897, .T. ) ;
#4670=ORIENTED_EDGE ( 'NONE', *, *, #10683, .T. ) ;
#4671=VERTEX_POINT ( 'NONE', #1294 ) ;
#4675=CARTESIAN_POINT ( 'NONE',  ( 19.99999999999999645, -44.69367065308684062, 56.44887778834731051 ) ) ;
#4683=EDGE_LOOP ( 'NONE', ( #12243, #5784, #12054, #1848 ) ) ;
#4688=EDGE_CURVE ( 'NONE', #12530, #16309, #17654, .T. ) ;
#4689=ORIENTED_EDGE ( 'NONE', *, *, #9726, .T. ) ;
#4691=ORIENTED_EDGE ( 'NONE', *, *, #14542, .F. ) ;
#4694=DIRECTION ( 'NONE',  ( 0.000000000000000000, 0.9422609221188213979, -0.3348796121709835538 ) ) ;
#4696=FACE_OUTER_BOUND ( 'NONE', #5503, .T. ) ;
#4698=FACE_OUTER_BOUND ( 'NONE', #1672, .T. ) ;
#4704=EDGE_CURVE ( 'NONE', #8657, #18161, #3412, .T. ) ;
#4706=VERTEX_POINT ( 'NONE', #7516 ) ;
#4709=EDGE_CURVE ( 'NONE', #5222, #2180, #6791, .T. ) ;
#4710=VERTEX_POINT ( 'NONE', #20457 ) ;
#4715=DIRECTION ( 'NONE',  ( 0.000000000000000000, 0.000000000000000000, 1.000000000000000000 ) ) ;
#4719=DIRECTION ( 'NONE',  ( 0.000000000000000000, 0.000000000000000000, 1.000000000000000000 ) ) ;
#4721=CARTESIAN_POINT ( 'NONE',  ( 0.000000000000000000, 58.44960523466241398, 28.06621538408611016 ) ) ;
#4725=EDGE_CURVE ( 'NONE', #6520, #5761, #6124, .T. ) ;
#4726=DIRECTION ( 'NONE',  ( 0.000000000000000000, 0.000000000000000000, 1.000000000000000000 ) ) ;
#4733=EDGE_LOOP ( 'NONE', ( #15951, #17348, #5692, #9180 ) ) ;
#4736=DIRECTION ( 'NONE',  ( 1.000000000000000000, 0.000000000000000000, 0.000000000000000000 ) ) ;
#4737=EDGE_LOOP ( 'NONE', ( #8988, #2837, #18735, #12960 ) ) ;
#4739=CARTESIAN_POINT ( 'NONE',  ( 19.99999999999999645, 0.000000000000000000, 0.000000000000000000 ) ) ;
#4741=ORIENTED_EDGE ( 'NONE', *, *, #3767, .T. ) ;
#4743=CARTESIAN_POINT ( 'NONE',  ( 19.99999999999999645, 0.000000000000000000, 0.000000000000000000 ) ) ;
#4746=CARTESIAN_POINT ( 'NONE',  ( 19.99999999999999645, -5.762283366691622000, 64.99406197038668154 ) ) ;
#4749=CARTESIAN_POINT ( 'NONE',  ( -65.00002539999999840, 0.000000000000000000, 0.000000000000000000 ) ) ;
#4750=AXIS2_PLACEMENT_3D ( 'NONE', #2245, #654, #7103 ) ;
#4754=CARTESIAN_POINT ( 'NONE',  ( 19.99999999999999645, 39.37110852956887186, -51.51683813304829584 ) ) ;
#4758=DIRECTION ( 'NONE',  ( 0.000000000000000000, -0.1361666490962539222, 0.9906859460363298675 ) ) ;
#4761=CARTESIAN_POINT ( 'NONE',  ( 19.99999999999999645, 63.85430960833490843, -11.25592921604860663 ) ) ;
#4763=EDGE_LOOP ( 'NONE', ( #18938, #7814, #10914, #12327 ) ) ;
#4771=ADVANCED_FACE ( 'NONE', ( #11444 ), #19278, .T. ) ;
#4773=CARTESIAN_POINT ( 'NONE',  ( 0.000000000000000000, -35.35772184876915958, 54.34979580218180928 ) ) ;
#4775=DIRECTION ( 'NONE',  ( -1.000000000000000000, -0.000000000000000000, 0.000000000000000000 ) ) ;
#4778=DIRECTION ( 'NONE',  ( -1.000000000000000000, 0.000000000000000000, 0.000000000000000000 ) ) ;
#4779=VERTEX_POINT ( 'NONE', #3280 ) ;
#4784=DIRECTION ( 'NONE',  ( -1.000000000000000000, 0.000000000000000000, 0.000000000000000000 ) ) ;
#4785=ORIENTED_EDGE ( 'NONE', *, *, #16066, .T. ) ;
#4786=CARTESIAN_POINT ( 'NONE',  ( 19.99999999999999645, 64.80702306891106446, -7.581672767545749814 ) ) ;
#4787=CARTESIAN_POINT ( 'NONE',  ( 0.000000000000000000, -49.77519642623978058, -42.18840861821836796 ) ) ;
#4788=ORIENTED_EDGE ( 'NONE', *, *, #4292, .T. ) ;
#4798=CIRCLE ( 'NONE', #19349, 65.24900000006525147 ) ;
#4799=ADVANCED_FACE ( 'NONE', ( #11229 ), #3372, .T. ) ;
#4801=DIRECTION ( 'NONE',  ( -1.000000000000000000, -0.000000000000000000, -0.000000000000000000 ) ) ;
#4803=CIRCLE ( 'NONE', #17339, 27.60000000002760245 ) ;
#4805=DIRECTION ( 'NONE',  ( 0.000000000000000000, 0.000000000000000000, 1.000000000000000000 ) ) ;
#4808=CARTESIAN_POINT ( 'NONE',  ( 0.000000000000000000, 0.000000000000000000, 0.000000000000000000 ) ) ;
#4818=EDGE_CURVE ( 'NONE', #10364, #4779, #2417, .T. ) ;
#4820=EDGE_CURVE ( 'NONE', #7472, #12251, #6354, .T. ) ;
#4824=AXIS2_PLACEMENT_3D ( 'NONE', #5602, #10711, #12082 ) ;
#4825=ORIENTED_EDGE ( 'NONE', *, *, #12340, .T. ) ;
#4830=ORIENTED_EDGE ( 'NONE', *, *, #14562, .F. ) ;
#4834=DIRECTION ( 'NONE',  ( 0.000000000000000000, 0.000000000000000000, 1.000000000000000000 ) ) ;
#4836=ADVANCED_FACE ( 'NONE', ( #304 ), #19686, .T. ) ;
#4840=VECTOR ( 'NONE', #3755, 1000.000000000000000 ) ;
#4849=LINE ( 'NONE', #17369, #20386 ) ;
#4851=AXIS2_PLACEMENT_3D ( 'NONE', #4761, #9943, #6660 ) ;
#4853=VECTOR ( 'NONE', #5721, 1000.000000000000000 ) ;
#4855=FACE_OUTER_BOUND ( 'NONE', #19680, .T. ) ;
#4856=AXIS2_PLACEMENT_3D ( 'NONE', #15196, #13828, #5649 ) ;
#4860=ORIENTED_EDGE ( 'NONE', *, *, #10122, .F. ) ;
#4861=DIRECTION ( 'NONE',  ( 0.000000000000000000, 0.000000000000000000, -1.000000000000000000 ) ) ;
#4865=ORIENTED_EDGE ( 'NONE', *, *, #8954, .T. ) ;
#4867=FACE_OUTER_BOUND ( 'NONE', #4737, .T. ) ;
#4870=DIRECTION ( 'NONE',  ( -1.000000000000000000, 0.000000000000000000, 0.000000000000000000 ) ) ;
#4872=ORIENTED_EDGE ( 'NONE', *, *, #8954, .F. ) ;
#4874=DIRECTION ( 'NONE',  ( -1.000000000000000000, -0.000000000000000000, -0.000000000000000000 ) ) ;
#4878=CARTESIAN_POINT ( 'NONE',  ( 0.000000000000000000, -1.971042061628798470, 64.80882494896106039 ) ) ;
#4885=CARTESIAN_POINT ( 'NONE',  ( 19.99999999999999645, 64.52323195238628273, 6.389157729493382121 ) ) ;
#4891=CARTESIAN_POINT ( 'NONE',  ( 19.99999999999999645, -56.63599015375694989, 31.56633360682443268 ) ) ;
#4896=ORIENTED_EDGE ( 'NONE', *, *, #7082, .T. ) ;
#4898=CARTESIAN_POINT ( 'NONE',  ( 9.999999999999998224, -63.48283426024875808, 33.96954156735348107 ) ) ;
#4899=ORIENTED_EDGE ( 'NONE', *, *, #16885, .T. ) ;
#4902=CARTESIAN_POINT ( 'NONE',  ( 19.99999999999999645, 67.51707036274413554, 25.00890260772400708 ) ) ;
#4903=CIRCLE ( 'NONE', #17101, 27.60000000002759180 ) ;
#4910=DIRECTION ( 'NONE',  ( -1.000000000000000000, 0.000000000000000000, 0.000000000000000000 ) ) ;
#4911=DIRECTION ( 'NONE',  ( 0.000000000000000000, -0.9422609221188237294, 0.3348796121709771700 ) ) ;
#4916=CARTESIAN_POINT ( 'NONE',  ( 19.99999999999999645, -51.81019761368347787, 38.98425606966041101 ) ) ;
#4920=AXIS2_PLACEMENT_3D ( 'NONE', #10436, #15300, #15199 ) ;
#4922=ORIENTED_EDGE ( 'NONE', *, *, #10129, .T. ) ;
#4924=LINE ( 'NONE', #1751, #8905 ) ;
#4928=DIRECTION ( 'NONE',  ( 1.000000000000000000, -0.000000000000000000, 0.000000000000000000 ) ) ;
#4929=EDGE_CURVE ( 'NONE', #17883, #1644, #16636, .T. ) ;
#4932=CARTESIAN_POINT ( 'NONE',  ( 19.99999999999999645, -48.70996102988709708, 42.79495875147758710 ) ) ;
#4937=CARTESIAN_POINT ( 'NONE',  ( -10.00000000000000000, 0.000000000000000000, 0.000000000000000000 ) ) ;
#4941=CARTESIAN_POINT ( 'NONE',  ( 85.00002539999999840, 0.000000000000000000, 0.000000000000000000 ) ) ;
#4942=ADVANCED_FACE ( 'NONE', ( #19991 ), #16927, .T. ) ;
#4951=CIRCLE ( 'NONE', #8663, 27.60000000002760245 ) ;
#4954=ADVANCED_FACE ( 'NONE', ( #16609 ), #15343, .T. ) ;
#4955=ORIENTED_EDGE ( 'NONE', *, *, #7126, .F. ) ;
#4957=DIRECTION ( 'NONE',  ( 0.000000000000000000, 0.3984010898462361228, 0.9172113015054554896 ) ) ;
#4965=ORIENTED_EDGE ( 'NONE', *, *, #1854, .T. ) ;
#4966=DIRECTION ( 'NONE',  ( 1.000000000000000000, 0.000000000000000000, 0.000000000000000000 ) ) ;
#4969=DIRECTION ( 'NONE',  ( -1.000000000000000000, 0.000000000000000000, 0.000000000000000000 ) ) ;
#4978=ORIENTED_EDGE ( 'NONE', *, *, #17259, .T. ) ;
#4984=DIRECTION ( 'NONE',  ( -1.000000000000000000, 0.000000000000000000, 0.000000000000000000 ) ) ;
#4985=EDGE_CURVE ( 'NONE', #17007, #8697, #17667, .T. ) ;
#4986=DIRECTION ( 'NONE',  ( -1.000000000000000000, -0.000000000000000000, -0.000000000000000000 ) ) ;
#4988=AXIS2_PLACEMENT_3D ( 'NONE', #1385, #4554, #20755 ) ;
#4992=CARTESIAN_POINT ( 'NONE',  ( 85.00002539999999840, 0.000000000000000000, 0.000000000000000000 ) ) ;
#4993=ORIENTED_EDGE ( 'NONE', *, *, #16242, .T. ) ;
#4995=DIRECTION ( 'NONE',  ( -1.000000000000000000, 0.000000000000000000, -0.000000000000000000 ) ) ;
#4998=VERTEX_POINT ( 'NONE', #13346 ) ;
#5003=ADVANCED_FACE ( 'NONE', ( #715 ), #7172, .T. ) ;
#5004=ORIENTED_EDGE ( 'NONE', *, *, #4562, .T. ) ;
#5006=ORIENTED_EDGE ( 'NONE', *, *, #14101, .T. ) ;
#5011=FACE_OUTER_BOUND ( 'NONE', #3070, .T. ) ;
#5014=CYLINDRICAL_SURFACE ( 'NONE', #14243, 65.24900000006525147 ) ;
#5016=DIRECTION ( 'NONE',  ( 1.000000000000000000, 0.000000000000000000, 0.000000000000000000 ) ) ;
#5021=CARTESIAN_POINT ( 'NONE',  ( 0.000000000000000000, -64.80702306891100761, 7.581672767546201008 ) ) ;
#5024=ORIENTED_EDGE ( 'NONE', *, *, #14281, .T. ) ;
#5025=DIRECTION ( 'NONE',  ( -1.000000000000000000, -0.000000000000000000, 0.000000000000000000 ) ) ;
#5026=EDGE_CURVE ( 'NONE', #16083, #11557, #8505, .T. ) ;
#5031=ORIENTED_EDGE ( 'NONE', *, *, #3571, .T. ) ;
#5032=DIRECTION ( 'NONE',  ( 0.000000000000000000, 0.000000000000000000, 1.000000000000000000 ) ) ;
#5033=ORIENTED_EDGE ( 'NONE', *, *, #13131, .F. ) ;
#5039=DIRECTION ( 'NONE',  ( 0.000000000000000000, 0.000000000000000000, 1.000000000000000000 ) ) ;
#5043=ORIENTED_EDGE ( 'NONE', *, *, #15673, .F. ) ;
#5046=ADVANCED_FACE ( 'NONE', ( #5274 ), #18216, .T. ) ;
#5051=LINE ( 'NONE', #1880, #11971 ) ;
#5059=FACE_OUTER_BOUND ( 'NONE', #15710, .T. ) ;
#5060=VERTEX_POINT ( 'NONE', #15451 ) ;
#5061=EDGE_CURVE ( 'NONE', #15524, #11465, #9194, .T. ) ;
#5062=LINE ( 'NONE', #1891, #1124 ) ;
#5066=ORIENTED_EDGE ( 'NONE', *, *, #15321, .T. ) ;
#5067=ORIENTED_EDGE ( 'NONE', *, *, #20293, .T. ) ;
#5068=LINE ( 'NONE', #11344, #20541 ) ;
#5071=DIRECTION ( 'NONE',  ( -1.000000000000000000, -0.000000000000000000, -0.000000000000000000 ) ) ;
#5074=CARTESIAN_POINT ( 'NONE',  ( 0.000000000000000000, 38.69327817041845918, -52.53819777490596010 ) ) ;
#5080=DIRECTION ( 'NONE',  ( 0.000000000000000000, 0.000000000000000000, 1.000000000000000000 ) ) ;
#5083=CARTESIAN_POINT ( 'NONE',  ( 19.99999999999999645, -43.56693332842820610, 48.57318520917490190 ) ) ;
#5086=DIRECTION ( 'NONE',  ( 0.000000000000000000, -0.7308359642781300236, 0.6825531432186476843 ) ) ;
#5088=ORIENTED_EDGE ( 'NONE', *, *, #1529, .F. ) ;
#5096=CARTESIAN_POINT ( 'NONE',  ( 0.000000000000000000, 10.74906464462118016, 71.19310085447973790 ) ) ;
#5097=EDGE_CURVE ( 'NONE', #20910, #15314, #4798, .T. ) ;
#5099=CARTESIAN_POINT ( 'NONE',  ( 0.000000000000000000, -67.51707036274430607, 25.00890260772354523 ) ) ;
#5105=CARTESIAN_POINT ( 'NONE',  ( 19.99999999999999645, 0.000000000000000000, 0.000000000000000000 ) ) ;
#5106=ORIENTED_EDGE ( 'NONE', *, *, #17189, .F. ) ;
#5110=FACE_OUTER_BOUND ( 'NONE', #4586, .T. ) ;
#5114=CARTESIAN_POINT ( 'NONE',  ( 19.99999999999999645, -61.72688495901628869, 19.84591825363989415 ) ) ;
#5117=AXIS2_PLACEMENT_3D ( 'NONE', #20722, #1144, #19046 ) ;
#5118=AXIS2_PLACEMENT_3D ( 'NONE', #2002, #517, #12160 ) ;
#5128=ORIENTED_EDGE ( 'NONE', *, *, #12968, .T. ) ;
#5129=AXIS2_PLACEMENT_3D ( 'NONE', #18930, #11282, #4396 ) ;
#5132=VERTEX_POINT ( 'NONE', #9095 ) ;
#5133=CARTESIAN_POINT ( 'NONE',  ( 0.000000000000000000, 0.000000000000000000, 0.000000000000000000 ) ) ;
#5135=CARTESIAN_POINT ( 'NONE',  ( 0.000000000000000000, -64.52323195238632536, 6.389157729492951354 ) ) ;
#5136=CARTESIAN_POINT ( 'NONE',  ( 19.99999999999999645, 0.000000000000000000, 0.000000000000000000 ) ) ;
#5138=CARTESIAN_POINT ( 'NONE',  ( 19.99999999999999645, -10.77748419466653651, -63.93680186330482940 ) ) ;
#5142=EDGE_LOOP ( 'NONE', ( #19295, #20826, #16444, #612 ) ) ;
#5145=DIRECTION ( 'NONE',  ( 1.000000000000000000, 0.000000000000000000, 0.000000000000000000 ) ) ;
#5149=EDGE_CURVE ( 'NONE', #12516, #2692, #17337, .T. ) ;
#5150=DIRECTION ( 'NONE',  ( -1.000000000000000000, 0.000000000000000000, -0.000000000000000000 ) ) ;
#5156=AXIS2_PLACEMENT_3D ( 'NONE', #13027, #6346, #7734 ) ;
#5163=VERTEX_POINT ( 'NONE', #7811 ) ;
#5164=DIRECTION ( 'NONE',  ( 0.000000000000000000, 0.5195839500354290097, 0.8544194045464913456 ) ) ;
#5165=ORIENTED_EDGE ( 'NONE', *, *, #13394, .T. ) ;
#5166=DIRECTION ( 'NONE',  ( -1.000000000000000000, 0.000000000000000000, 0.000000000000000000 ) ) ;
#5173=AXIS2_PLACEMENT_3D ( 'NONE', #18779, #12522, #4455 ) ;
#5176=DIRECTION ( 'NONE',  ( -1.000000000000000000, -0.000000000000000000, -0.000000000000000000 ) ) ;
#5179=DIRECTION ( 'NONE',  ( 0.000000000000000000, -0.8878852184023701133, -0.4600650377311617523 ) ) ;
#5183=CARTESIAN_POINT ( 'NONE',  ( 19.99999999999999645, -39.37110852956848817, 51.51683813304857296 ) ) ;
#5186=EDGE_CURVE ( 'NONE', #12410, #1870, #2214, .T. ) ;
#5187=ORIENTED_EDGE ( 'NONE', *, *, #12888, .F. ) ;
#5188=DIRECTION ( 'NONE',  ( 0.000000000000000000, 0.7308359642781254717, -0.6825531432186525693 ) ) ;
#5193=ORIENTED_EDGE ( 'NONE', *, *, #19576, .F. ) ;
#5196=VERTEX_POINT ( 'NONE', #9619 ) ;
#5198=LINE ( 'NONE', #4898, #8677 ) ;
#5203=ORIENTED_EDGE ( 'NONE', *, *, #7961, .F. ) ;
#5204=CARTESIAN_POINT ( 'NONE',  ( 19.99999999999999645, 46.17500197033056963, 55.24372537266411598 ) ) ;
#5205=AXIS2_PLACEMENT_3D ( 'NONE', #12443, #14462, #17629 ) ;
#5207=DIRECTION ( 'NONE',  ( -1.000000000000000000, 0.000000000000000000, 0.000000000000000000 ) ) ;
#5208=CIRCLE ( 'NONE', #4535, 27.60000000002760245 ) ;
#5209=LINE ( 'NONE', #14756, #4190 ) ;
#5210=EDGE_CURVE ( 'NONE', #4467, #4451, #11205, .T. ) ;
#5212=ADVANCED_FACE ( 'NONE', ( #1574 ), #11506, .T. ) ;
#5222=VERTEX_POINT ( 'NONE', #17888 ) ;
#5233=CARTESIAN_POINT ( 'NONE',  ( 19.99999999999999645, 61.72688495901613948, -19.84591825364033468 ) ) ;
#5235=DIRECTION ( 'NONE',  ( 1.000000000000000000, 0.000000000000000000, 0.000000000000000000 ) ) ;
#5239=EDGE_CURVE ( 'NONE', #9794, #16683, #13408, .T. ) ;
#5241=DIRECTION ( 'NONE',  ( 0.000000000000000000, 0.000000000000000000, 1.000000000000000000 ) ) ;
#5249=VERTEX_POINT ( 'NONE', #3352 ) ;
#5250=FACE_OUTER_BOUND ( 'NONE', #17449, .T. ) ;
#5252=ORIENTED_EDGE ( 'NONE', *, *, #1853, .T. ) ;
#5255=ORIENTED_EDGE ( 'NONE', *, *, #9082, .F. ) ;
#5263=CARTESIAN_POINT ( 'NONE',  ( 19.99999999999999645, -56.42118728228132341, -32.77318456705499017 ) ) ;
#5266=ORIENTED_EDGE ( 'NONE', *, *, #12844, .T. ) ;
#5273=VERTEX_POINT ( 'NONE', #6327 ) ;
#5274=FACE_OUTER_BOUND ( 'NONE', #9226, .T. ) ;
#5279=DIRECTION ( 'NONE',  ( -1.000000000000000000, -0.000000000000000000, 0.000000000000000000 ) ) ;
#5280=AXIS2_PLACEMENT_3D ( 'NONE', #5827, #15264, #18777 ) ;
#5281=CYLINDRICAL_SURFACE ( 'NONE', #1253, 72.00000000007199219 ) ;
#5282=CARTESIAN_POINT ( 'NONE',  ( 19.99999999999999645, -45.48683723007179225, -46.78012013466265273 ) ) ;
#5286=CIRCLE ( 'NONE', #14765, 65.24900000006525147 ) ;
#5295=LINE ( 'NONE', #18129, #18704 ) ;
#5296=AXIS2_PLACEMENT_3D ( 'NONE', #11449, #1608, #2194 ) ;
#5298=CARTESIAN_POINT ( 'NONE',  ( -65.00002539999999840, 5.400000000000000355, 1.000000000000000000 ) ) ;
#5301=ORIENTED_EDGE ( 'NONE', *, *, #14264, .F. ) ;
#5306=DIRECTION ( 'NONE',  ( 0.000000000000000000, 0.000000000000000000, 1.000000000000000000 ) ) ;
#5308=CARTESIAN_POINT ( 'NONE',  ( -65.00002539999999840, 0.000000000000000000, 0.000000000000000000 ) ) ;
#5309=EDGE_CURVE ( 'NONE', #17187, #17770, #15426, .T. ) ;
#5310=CIRCLE ( 'NONE', #20556, 27.60000000002759535 ) ;
#5311=EDGE_CURVE ( 'NONE', #8808, #17307, #16280, .T. ) ;
#5312=CARTESIAN_POINT ( 'NONE',  ( 0.000000000000000000, -11.98658579560631843, 64.13855129306463709 ) ) ;
#5318=DIRECTION ( 'NONE',  ( -1.000000000000000000, 0.000000000000000000, 0.000000000000000000 ) ) ;
#5320=ORIENTED_EDGE ( 'NONE', *, *, #7082, .F. ) ;
#5322=ORIENTED_EDGE ( 'NONE', *, *, #7665, .T. ) ;
#5326=VERTEX_POINT ( 'NONE', #17785 ) ;
#5327=CARTESIAN_POINT ( 'NONE',  ( 19.99999999999999645, -19.38316218894168586, -61.87375713201008409 ) ) ;
#5328=ORIENTED_EDGE ( 'NONE', *, *, #18851, .T. ) ;
#5330=DIRECTION ( 'NONE',  ( 0.000000000000000000, 0.5195839500354345608, -0.8544194045464879039 ) ) ;
#5331=AXIS2_PLACEMENT_3D ( 'NONE', #2505, #19143, #5892 ) ;
#5332=VERTEX_POINT ( 'NONE', #8225 ) ;
#5338=DIRECTION ( 'NONE',  ( -1.000000000000000000, 0.000000000000000000, -0.000000000000000000 ) ) ;
#5341=DIRECTION ( 'NONE',  ( -1.000000000000000000, 0.000000000000000000, -0.000000000000000000 ) ) ;
#5342=ADVANCED_FACE ( 'NONE', ( #17100 ), #13599, .T. ) ;
#5344=ORIENTED_EDGE ( 'NONE', *, *, #4709, .T. ) ;
#5346=EDGE_LOOP ( 'NONE', ( #4689, #11571, #7382, #8286 ) ) ;
#5348=LINE ( 'NONE', #19764, #9021 ) ;
#5352=VERTEX_POINT ( 'NONE', #3553 ) ;
#5354=EDGE_CURVE ( 'NONE', #939, #2292, #545, .T. ) ;
#5355=EDGE_CURVE ( 'NONE', #6711, #12516, #20836, .T. ) ;
#5356=ORIENTED_EDGE ( 'NONE', *, *, #2902, .T. ) ;
#5362=ORIENTED_EDGE ( 'NONE', *, *, #4320, .T. ) ;
#5363=DIRECTION ( 'NONE',  ( 0.000000000000000000, 0.000000000000000000, 1.000000000000000000 ) ) ;
#5367=EDGE_CURVE ( 'NONE', #10658, #7264, #18588, .T. ) ;
#5376=DIRECTION ( 'NONE',  ( -1.000000000000000000, 0.000000000000000000, 0.000000000000000000 ) ) ;
#5378=ORIENTED_EDGE ( 'NONE', *, *, #8570, .T. ) ;
#5383=CYLINDRICAL_SURFACE ( 'NONE', #17739, 72.00000000007199219 ) ;
#5389=EDGE_CURVE ( 'NONE', #18397, #297, #16433, .T. ) ;
#5390=DIRECTION ( 'NONE',  ( -1.000000000000000000, -0.000000000000000000, -0.000000000000000000 ) ) ;
#5391=CARTESIAN_POINT ( 'NONE',  ( 19.99999999999999645, 0.000000000000000000, 0.000000000000000000 ) ) ;
#5393=DIRECTION ( 'NONE',  ( -1.000000000000000000, 0.000000000000000000, -0.000000000000000000 ) ) ;
#5396=VERTEX_POINT ( 'NONE', #6832 ) ;
#5405=DIRECTION ( 'NONE',  ( 1.000000000000000000, -0.000000000000000000, -0.000000000000000000 ) ) ;
#5415=ORIENTED_EDGE ( 'NONE', *, *, #17475, .T. ) ;
#5417=LINE ( 'NONE', #568, #4219 ) ;
#5418=AXIS2_PLACEMENT_3D ( 'NONE', #19624, #9985, #18248 ) ;
#5420=EDGE_CURVE ( 'NONE', #20609, #3307, #3942, .T. ) ;
#5422=ORIENTED_EDGE ( 'NONE', *, *, #13798, .T. ) ;
#5434=ORIENTED_EDGE ( 'NONE', *, *, #288, .T. ) ;
#5435=DIRECTION ( 'NONE',  ( 0.000000000000000000, 0.000000000000000000, -1.000000000000000000 ) ) ;
#5437=VERTEX_POINT ( 'NONE', #5643 ) ;
#5441=CARTESIAN_POINT ( 'NONE',  ( 19.99999999999999645, 58.26603306962021378, -42.29739224042413070 ) ) ;
#5449=VERTEX_POINT ( 'NONE', #2787 ) ;
#5451=EDGE_CURVE ( 'NONE', #5249, #18498, #20591, .T. ) ;
#5454=LINE ( 'NONE', #11726, #17867 ) ;
#5455=DIRECTION ( 'NONE',  ( 0.000000000000000000, 0.000000000000000000, 1.000000000000000000 ) ) ;
#5457=AXIS2_PLACEMENT_3D ( 'NONE', #6463, #8165, #17830 ) ;
#5458=ORIENTED_EDGE ( 'NONE', *, *, #1193, .F. ) ;
#5459=DIRECTION ( 'NONE',  ( -1.000000000000000000, -0.000000000000000000, 0.000000000000000000 ) ) ;
#5463=EDGE_CURVE ( 'NONE', #857, #254, #14353, .T. ) ;
#5466=AXIS2_PLACEMENT_3D ( 'NONE', #6811, #13296, #19752 ) ;
#5468=EDGE_CURVE ( 'NONE', #3247, #3717, #11704, .T. ) ;
#5473=CIRCLE ( 'NONE', #15989, 27.60000000002761311 ) ;
#5474=ORIENTED_EDGE ( 'NONE', *, *, #9828, .F. ) ;
#5475=DIRECTION ( 'NONE',  ( 0.000000000000000000, -0.6310879443260433153, -0.7757112907044274586 ) ) ;
#5477=EDGE_LOOP ( 'NONE', ( #19027, #19749, #1920, #8175 ) ) ;
#5478=AXIS2_PLACEMENT_3D ( 'NONE', #19082, #4557, #4665 ) ;
#5480=CARTESIAN_POINT ( 'NONE',  ( 0.000000000000000000, -64.79224928664393701, 2.456263514197400077 ) ) ;
#5481=DIRECTION ( 'NONE',  ( -1.000000000000000000, 0.000000000000000000, -0.000000000000000000 ) ) ;
#5482=CARTESIAN_POINT ( 'NONE',  ( 0.000000000000000000, 55.05624179291979914, 35.01774179823801347 ) ) ;
#5487=CARTESIAN_POINT ( 'NONE',  ( 9.999999999999998224, 36.59093685910629290, 62.00889726308043493 ) ) ;
#5491=CYLINDRICAL_SURFACE ( 'NONE', #5648, 27.60000000002759535 ) ;
#5495=DIRECTION ( 'NONE',  ( -1.000000000000000000, -0.000000000000000000, 0.000000000000000000 ) ) ;
#5496=VECTOR ( 'NONE', #18616, 1000.000000000000000 ) ;
#5497=EDGE_LOOP ( 'NONE', ( #12024, #148, #17837, #12677 ) ) ;
#5500=CARTESIAN_POINT ( 'NONE',  ( 0.000000000000000000, -64.52323195238624010, -6.389157729493822657 ) ) ;
#5501=DIRECTION ( 'NONE',  ( -1.000000000000000000, 0.000000000000000000, -0.000000000000000000 ) ) ;
#5503=EDGE_LOOP ( 'NONE', ( #6884, #8768, #12320, #3041 ) ) ;
#5505=VECTOR ( 'NONE', #9286, 1000.000000000000000 ) ;
#5506=AXIS2_PLACEMENT_3D ( 'NONE', #18928, #20506, #3021 ) ;
#5509=DIRECTION ( 'NONE',  ( -1.000000000000000000, 0.000000000000000000, -0.000000000000000000 ) ) ;
#5515=CARTESIAN_POINT ( 'NONE',  ( 85.00002539999999840, 4.898587196589412829E-16, -4.000000000000000000 ) ) ;
#5520=ORIENTED_EDGE ( 'NONE', *, *, #10415, .T. ) ;
#5523=EDGE_LOOP ( 'NONE', ( #691, #1654, #8331, #14371 ) ) ;
#5525=VERTEX_POINT ( 'NONE', #16143 ) ;
#5526=FACE_OUTER_BOUND ( 'NONE', #19612, .T. ) ;
#5527=CARTESIAN_POINT ( 'NONE',  ( 19.99999999999999645, 0.000000000000000000, 0.000000000000000000 ) ) ;
#5528=CIRCLE ( 'NONE', #15016, 72.00000000007199219 ) ;
#5531=CIRCLE ( 'NONE', #8934, 27.60000000002760601 ) ;
#5540=EDGE_CURVE ( 'NONE', #15627, #11338, #2904, .T. ) ;
#5541=ORIENTED_EDGE ( 'NONE', *, *, #15445, .F. ) ;
#5543=DIRECTION ( 'NONE',  ( 1.000000000000000000, 0.000000000000000000, 0.000000000000000000 ) ) ;
#5553=LINE ( 'NONE', #8742, #10252 ) ;
#5557=DIRECTION ( 'NONE',  ( 0.000000000000000000, 0.8878852184023731109, 0.4600650377311559791 ) ) ;
#5564=VERTEX_POINT ( 'NONE', #20484 ) ;
#5565=EDGE_CURVE ( 'NONE', #788, #12290, #8307, .T. ) ;
#5573=ORIENTED_EDGE ( 'NONE', *, *, #7368, .T. ) ;
#5576=VERTEX_POINT ( 'NONE', #7981 ) ;
#5579=VECTOR ( 'NONE', #19315, 1000.000000000000000 ) ;
#5582=ORIENTED_EDGE ( 'NONE', *, *, #409, .F. ) ;
#5583=ORIENTED_EDGE ( 'NONE', *, *, #10013, .F. ) ;
#5587=CARTESIAN_POINT ( 'NONE',  ( 19.99999999999999645, 31.17893654894229982, 57.31758819669181548 ) ) ;
#5592=EDGE_CURVE ( 'NONE', #2692, #1099, #19493, .T. ) ;
#5598=EDGE_CURVE ( 'NONE', #2326, #8735, #17831, .T. ) ;
#5600=DIRECTION ( 'NONE',  ( 0.000000000000000000, 0.000000000000000000, 1.000000000000000000 ) ) ;
#5601=ORIENTED_EDGE ( 'NONE', *, *, #649, .F. ) ;
#5602=CARTESIAN_POINT ( 'NONE',  ( 19.99999999999999645, 0.000000000000000000, 0.000000000000000000 ) ) ;
#5608=ORIENTED_EDGE ( 'NONE', *, *, #15200, .F. ) ;
#5609=CARTESIAN_POINT ( 'NONE',  ( 19.99999999999999645, 39.37110852956887186, -51.51683813304829584 ) ) ;
#5611=AXIS2_PLACEMENT_3D ( 'NONE', #2439, #646, #2558 ) ;
#5613=VERTEX_POINT ( 'NONE', #19218 ) ;
#5614=DIRECTION ( 'NONE',  ( -1.000000000000000000, -0.000000000000000000, 0.000000000000000000 ) ) ;
#5615=ADVANCED_FACE ( 'NONE', ( #4696 ), #11157, .T. ) ;
#5616=AXIS2_PLACEMENT_3D ( 'NONE', #1013, #7457, #20176 ) ;
#5618=CYLINDRICAL_SURFACE ( 'NONE', #3158, 72.00000000007199219 ) ;
#5620=CARTESIAN_POINT ( 'NONE',  ( 9.999999999999998224, -71.89099403602357086, 3.960426305688546922 ) ) ;
#5621=AXIS2_PLACEMENT_3D ( 'NONE', #7662, #20592, #6067 ) ;
#5623=CARTESIAN_POINT ( 'NONE',  ( 0.000000000000000000, 20.34307325858786442, 69.06634035770315450 ) ) ;
#5624=CYLINDRICAL_SURFACE ( 'NONE', #680, 7.500000000000000000 ) ;
#5629=EDGE_LOOP ( 'NONE', ( #18866, #81, #10256, #5608 ) ) ;
#5630=EDGE_CURVE ( 'NONE', #6239, #15053, #19415, .T. ) ;
#5631=( GEOMETRIC_REPRESENTATION_CONTEXT ( 3 ) GLOBAL_UNCERTAINTY_ASSIGNED_CONTEXT ( ( #19802 ) ) GLOBAL_UNIT_ASSIGNED_CONTEXT ( ( #20023, #12192, #9229 ) ) REPRESENTATION_CONTEXT ( 'NONE', 'WORKASPACE' ) );
#5638=ORIENTED_EDGE ( 'NONE', *, *, #11033, .F. ) ;
#5640=FACE_OUTER_BOUND ( 'NONE', #14676, .T. ) ;
#5643=CARTESIAN_POINT ( 'NONE',  ( 0.000000000000000000, 44.69367065308723141, -56.44887778834702630 ) ) ;
#5645=CARTESIAN_POINT ( 'NONE',  ( 0.000000000000000000, 10.77748419466696284, 63.93680186330476545 ) ) ;
#5648=AXIS2_PLACEMENT_3D ( 'NONE', #18550, #10383, #5600 ) ;
#5649=DIRECTION ( 'NONE',  ( 0.000000000000000000, -0.9976687691905398170, 0.06824241336466078944 ) ) ;
#5651=ORIENTED_EDGE ( 'NONE', *, *, #17762, .T. ) ;
#5652=( NAMED_UNIT ( * ) PLANE_ANGLE_UNIT ( ) SI_UNIT ( $, .RADIAN. ) );
#5653=CARTESIAN_POINT ( 'NONE',  ( -10.00000000000000000, 0.000000000000000000, 0.000000000000000000 ) ) ;
#5659=CIRCLE ( 'NONE', #1287, 27.60000000002760245 ) ;
#5661=CARTESIAN_POINT ( 'NONE',  ( 0.000000000000000000, 49.77519642624066165, -42.18840861821735189 ) ) ;
#5662=DIRECTION ( 'NONE',  ( -1.000000000000000000, -0.000000000000000000, -0.000000000000000000 ) ) ;
#5664=CIRCLE ( 'NONE', #16837, 27.60000000002759890 ) ;
#5668=ORIENTED_EDGE ( 'NONE', *, *, #3531, .T. ) ;
#5676=CARTESIAN_POINT ( 'NONE',  ( 0.000000000000000000, -56.42118728228132341, -32.77318456705499017 ) ) ;
#5677=VERTEX_POINT ( 'NONE', #14557 ) ;
#5680=DIRECTION ( 'NONE',  ( -1.000000000000000000, -0.000000000000000000, 0.000000000000000000 ) ) ;
#5681=ORIENTED_EDGE ( 'NONE', *, *, #13908, .T. ) ;
#5682=DIRECTION ( 'NONE',  ( 0.000000000000000000, -0.3984010898462296835, -0.9172113015054581542 ) ) ;
#5688=DIRECTION ( 'NONE',  ( 0.000000000000000000, -0.1361666490962331333, -0.9906859460363326431 ) ) ;
#5690=EDGE_CURVE ( 'NONE', #12410, #18310, #16782, .T. ) ;
#5691=ORIENTED_EDGE ( 'NONE', *, *, #10428, .F. ) ;
#5692=ORIENTED_EDGE ( 'NONE', *, *, #7126, .T. ) ;
#5695=FACE_OUTER_BOUND ( 'NONE', #18, .T. ) ;
#5696=CARTESIAN_POINT ( 'NONE',  ( -10.00000000000000000, 0.000000000000000000, 0.000000000000000000 ) ) ;
#5697=ADVANCED_FACE ( 'NONE', ( #16241 ), #14753, .T. ) ;
#5705=VERTEX_POINT ( 'NONE', #3315 ) ;
#5706=CARTESIAN_POINT ( 'NONE',  ( 0.000000000000000000, 0.000000000000000000, 0.000000000000000000 ) ) ;
#5709=VERTEX_POINT ( 'NONE', #18243 ) ;
#5713=CARTESIAN_POINT ( 'NONE',  ( 0.000000000000000000, 70.68211945903209426, -13.71269443944134458 ) ) ;
#5716=ORIENTED_EDGE ( 'NONE', *, *, #14562, .T. ) ;
#5717=VERTEX_POINT ( 'NONE', #5204 ) ;
#5719=ADVANCED_FACE ( 'NONE', ( #18035 ), #3708, .T. ) ;
#5721=DIRECTION ( 'NONE',  ( 1.000000000000000000, 0.000000000000000000, -0.000000000000000000 ) ) ;
#5722=CARTESIAN_POINT ( 'NONE',  ( 19.99999999999999645, 28.84646472442454979, 58.52617768068444093 ) ) ;
#5724=DIRECTION ( 'NONE',  ( 0.000000000000000000, 0.000000000000000000, 1.000000000000000000 ) ) ;
#5725=FACE_OUTER_BOUND ( 'NONE', #6417, .T. ) ;
#5726=ADVANCED_FACE ( 'NONE', ( #10183 ), #9870, .T. ) ;
#5730=CIRCLE ( 'NONE', #13536, 27.60000000002759890 ) ;
#5733=DIRECTION ( 'NONE',  ( 0.000000000000000000, 0.000000000000000000, 1.000000000000000000 ) ) ;
#5737=ORIENTED_EDGE ( 'NONE', *, *, #19216, .F. ) ;
#5738=DIRECTION ( 'NONE',  ( 0.000000000000000000, 0.000000000000000000, 1.000000000000000000 ) ) ;
#5739=ORIENTED_EDGE ( 'NONE', *, *, #12695, .F. ) ;
#5740=DIRECTION ( 'NONE',  ( -1.000000000000000000, 0.000000000000000000, 0.000000000000000000 ) ) ;
#5741=DIRECTION ( 'NONE',  ( -1.000000000000000000, -0.000000000000000000, -0.000000000000000000 ) ) ;
#5742=CARTESIAN_POINT ( 'NONE',  ( 19.99999999999999645, 0.000000000000000000, 0.000000000000000000 ) ) ;
#5744=ORIENTED_EDGE ( 'NONE', *, *, #5844, .T. ) ;
#5746=DIRECTION ( 'NONE',  ( -1.000000000000000000, -0.000000000000000000, 0.000000000000000000 ) ) ;
#5749=DIRECTION ( 'NONE',  ( 0.000000000000000000, 0.5195839500354287877, 0.8544194045464914566 ) ) ;
#5752=CARTESIAN_POINT ( 'NONE',  ( 19.99999999999999645, 0.9548212943365497196, 71.99366858485716136 ) ) ;
#5754=AXIS2_PLACEMENT_3D ( 'NONE', #9894, #8200, #353 ) ;
#5757=EDGE_LOOP ( 'NONE', ( #12689, #1251, #6437, #10079 ) ) ;
#5761=VERTEX_POINT ( 'NONE', #5096 ) ;
#5766=ORIENTED_EDGE ( 'NONE', *, *, #7546, .T. ) ;
#5776=ORIENTED_EDGE ( 'NONE', *, *, #9616, .F. ) ;
#5777=FACE_OUTER_BOUND ( 'NONE', #14057, .T. ) ;
#5783=DIRECTION ( 'NONE',  ( -1.000000000000000000, 0.000000000000000000, -0.000000000000000000 ) ) ;
#5784=ORIENTED_EDGE ( 'NONE', *, *, #14654, .F. ) ;
#5786=CARTESIAN_POINT ( 'NONE',  ( 19.99999999999999645, 0.000000000000000000, 0.000000000000000000 ) ) ;
#5787=VECTOR ( 'NONE', #7320, 1000.000000000000000 ) ;
#5795=DIRECTION ( 'NONE',  ( 0.000000000000000000, 0.9790840876823234673, -0.2034560130526309185 ) ) ;
#5802=VECTOR ( 'NONE', #9942, 1000.000000000000000 ) ;
#5819=ORIENTED_EDGE ( 'NONE', *, *, #12489, .T. ) ;
#5823=CARTESIAN_POINT ( 'NONE',  ( 0.000000000000000000, 0.000000000000000000, 0.000000000000000000 ) ) ;
#5827=CARTESIAN_POINT ( 'NONE',  ( 0.000000000000000000, -64.79224928664389438, -2.456263514198281150 ) ) ;
#5828=CYLINDRICAL_SURFACE ( 'NONE', #7556, 65.24900000006525147 ) ;
#5829=CIRCLE ( 'NONE', #15652, 27.60000000002760245 ) ;
#5833=AXIS2_PLACEMENT_3D ( 'NONE', #3752, #19660, #16495 ) ;
#5836=EDGE_CURVE ( 'NONE', #11468, #17275, #14444, .T. ) ;
#5838=CIRCLE ( 'NONE', #13982, 27.60000000002759890 ) ;
#5839=CARTESIAN_POINT ( 'NONE',  ( 19.99999999999999645, 27.62776854598936538, -58.65812137498974721 ) ) ;
#5840=CARTESIAN_POINT ( 'NONE',  ( 9.999999999999998224, 71.89099403602354244, -3.960426305689050075 ) ) ;
#5844=EDGE_CURVE ( 'NONE', #2530, #16859, #18482, .T. ) ;
#5848=CIRCLE ( 'NONE', #15668, 27.60000000002759890 ) ;
#5850=VECTOR ( 'NONE', #2702, 1000.000000000000000 ) ;
#5851=DIRECTION ( 'NONE',  ( 0.000000000000000000, 0.000000000000000000, -1.000000000000000000 ) ) ;
#5854=DIRECTION ( 'NONE',  ( -1.000000000000000000, -0.000000000000000000, 0.000000000000000000 ) ) ;
#5857=ORIENTED_EDGE ( 'NONE', *, *, #9463, .F. ) ;
#5858=CARTESIAN_POINT ( 'NONE',  ( 19.99999999999999645, -46.01927912072559224, 45.67597560296373871 ) ) ;
#5859=ADVANCED_FACE ( 'NONE', ( #16755 ), #7200, .T. ) ;
#5860=AXIS2_PLACEMENT_3D ( 'NONE', #10962, #4285, #19018 ) ;
#5864=AXIS2_PLACEMENT_3D ( 'NONE', #18345, #16959, #3921 ) ;
#5865=EDGE_CURVE ( 'NONE', #5564, #15624, #8004, .T. ) ;
#5870=FACE_OUTER_BOUND ( 'NONE', #10343, .T. ) ;
#5874=CARTESIAN_POINT ( 'NONE',  ( 19.99999999999999645, 38.69327817041845918, -52.53819777490596010 ) ) ;
#5875=CARTESIAN_POINT ( 'NONE',  ( 0.000000000000000000, -59.36728637278046961, 40.73727173906768684 ) ) ;
#5876=ADVANCED_FACE ( 'NONE', ( #20022 ), #3917, .T. ) ;
#5883=VECTOR ( 'NONE', #19979, 1000.000000000000000 ) ;
#5887=DIRECTION ( 'NONE',  ( -1.000000000000000000, -0.000000000000000000, -0.000000000000000000 ) ) ;
#5888=EDGE_LOOP ( 'NONE', ( #7301, #10862, #14835, #19480 ) ) ;
#5891=CIRCLE ( 'NONE', #1517, 72.00000000007199219 ) ;
#5892=DIRECTION ( 'NONE',  ( 0.000000000000000000, 0.000000000000000000, 1.000000000000000000 ) ) ;
#5894=DIRECTION ( 'NONE',  ( 0.000000000000000000, 0.000000000000000000, 1.000000000000000000 ) ) ;
#5897=CARTESIAN_POINT ( 'NONE',  ( -10.00000000000000000, 0.000000000000000000, 0.000000000000000000 ) ) ;
#5903=FACE_OUTER_BOUND ( 'NONE', #15020, .T. ) ;
#5904=VERTEX_POINT ( 'NONE', #9020 ) ;
#5906=DIRECTION ( 'NONE',  ( -1.000000000000000000, 0.000000000000000000, 0.000000000000000000 ) ) ;
#5914=CARTESIAN_POINT ( 'NONE',  ( 0.000000000000000000, 11.98658579560587789, 64.13855129306472236 ) ) ;
#5918=DIRECTION ( 'NONE',  ( -1.000000000000000000, 0.000000000000000000, 0.000000000000000000 ) ) ;
#5924=CARTESIAN_POINT ( 'NONE',  ( 19.99999999999999645, 29.55812890832068973, -65.65300461859658299 ) ) ;
#5926=CARTESIAN_POINT ( 'NONE',  ( 85.00002539999999840, 3.872983346207417021, -1.000000000000000000 ) ) ;
#5930=DIRECTION ( 'NONE',  ( 0.000000000000000000, 0.000000000000000000, 1.000000000000000000 ) ) ;
#5933=ORIENTED_EDGE ( 'NONE', *, *, #7636, .F. ) ;
#5935=ORIENTED_EDGE ( 'NONE', *, *, #6120, .F. ) ;
#5937=DIRECTION ( 'NONE',  ( -1.000000000000000000, 0.000000000000000000, 0.000000000000000000 ) ) ;
#5940=DIRECTION ( 'NONE',  ( 0.000000000000000000, 0.000000000000000000, 1.000000000000000000 ) ) ;
#5941=CARTESIAN_POINT ( 'NONE',  ( 0.000000000000000000, 63.85430960833490843, 16.34407078397899582 ) ) ;
#5945=FACE_OUTER_BOUND ( 'NONE', #18607, .T. ) ;
#5948=ORIENTED_EDGE ( 'NONE', *, *, #18287, .T. ) ;
#5952=LINE ( 'NONE', #12647, #15041 ) ;
#5956=EDGE_LOOP ( 'NONE', ( #6829, #19969, #20262, #8114 ) ) ;
#5959=DIRECTION ( 'NONE',  ( -1.000000000000000000, -0.000000000000000000, 0.000000000000000000 ) ) ;
#5962=DIRECTION ( 'NONE',  ( 0.000000000000000000, 0.8878852184023732219, 0.4600650377311559791 ) ) ;
#5964=ADVANCED_FACE ( 'NONE', ( #8790 ), #13686, .T. ) ;
#5966=CARTESIAN_POINT ( 'NONE',  ( 19.99999999999999645, 64.79224928664392280, 25.14373648582975918 ) ) ;
#5971=ORIENTED_EDGE ( 'NONE', *, *, #16157, .F. ) ;
#5976=CARTESIAN_POINT ( 'NONE',  ( 19.99999999999999645, 0.000000000000000000, 0.000000000000000000 ) ) ;
#5979=CARTESIAN_POINT ( 'NONE',  ( 19.99999999999999645, 0.000000000000000000, 0.000000000000000000 ) ) ;
#5983=CARTESIAN_POINT ( 'NONE',  ( 19.99999999999999645, -36.59093685910587368, -62.00889726308066940 ) ) ;
#5984=DIRECTION ( 'NONE',  ( -1.000000000000000000, 0.000000000000000000, -0.000000000000000000 ) ) ;
#5985=ORIENTED_EDGE ( 'NONE', *, *, #13835, .F. ) ;
#5987=CARTESIAN_POINT ( 'NONE',  ( -65.00002539999999840, 3.872983346207417021, -1.000000000000000000 ) ) ;
#5990=DIRECTION ( 'NONE',  ( 0.000000000000000000, 1.000000000000000000, -0.000000000000000000 ) ) ;
#5991=AXIS2_PLACEMENT_3D ( 'NONE', #18008, #19387, #13038 ) ;
#5994=AXIS2_PLACEMENT_3D ( 'NONE', #5138, #5854, #7336 ) ;
#5995=ADVANCED_FACE ( 'NONE', ( #18885 ), #12412, .T. ) ;
#5998=VECTOR ( 'NONE', #19078, 1000.000000000000000 ) ;
#6003=DIRECTION ( 'NONE',  ( -1.000000000000000000, 0.000000000000000000, 0.000000000000000000 ) ) ;
#6006=VECTOR ( 'NONE', #7188, 1000.000000000000000 ) ;
#6010=ORIENTED_EDGE ( 'NONE', *, *, #13798, .F. ) ;
#6022=LINE ( 'NONE', #15769, #13437 ) ;
#6024=CARTESIAN_POINT ( 'NONE',  ( 19.99999999999999645, 10.77748419466696284, 63.93680186330476545 ) ) ;
#6025=DIRECTION ( 'NONE',  ( 0.000000000000000000, 0.000000000000000000, 1.000000000000000000 ) ) ;
#6026=LINE ( 'NONE', #14511, #12610 ) ;
#6034=ORIENTED_EDGE ( 'NONE', *, *, #17781, .F. ) ;
#6037=LINE ( 'NONE', #12509, #2615 ) ;
#6042=CARTESIAN_POINT ( 'NONE',  ( 19.99999999999999645, 0.000000000000000000, 0.000000000000000000 ) ) ;
#6051=CARTESIAN_POINT ( 'NONE',  ( 19.99999999999999645, 23.08379033237351052, 61.02926039941442582 ) ) ;
#6053=CARTESIAN_POINT ( 'NONE',  ( 0.000000000000000000, 27.80658314415319055, -66.41380830714092554 ) ) ;
#6058=LINE ( 'NONE', #12532, #3212 ) ;
#6060=DIRECTION ( 'NONE',  ( 1.000000000000000000, -0.000000000000000000, -0.000000000000000000 ) ) ;
#6062=CARTESIAN_POINT ( 'NONE',  ( 0.000000000000000000, 54.08351995568756365, -35.76369202524444546 ) ) ;
#6063=CYLINDRICAL_SURFACE ( 'NONE', #9071, 27.60000000002759890 ) ;
#6064=DIRECTION ( 'NONE',  ( 1.000000000000000000, 0.000000000000000000, 0.000000000000000000 ) ) ;
#6067=DIRECTION ( 'NONE',  ( 0.000000000000000000, 0.000000000000000000, 1.000000000000000000 ) ) ;
#6068=CARTESIAN_POINT ( 'NONE',  ( 19.99999999999999645, -38.22257254261781867, 61.01667762370124137 ) ) ;
#6069=DIRECTION ( 'NONE',  ( 0.000000000000000000, 0.1361666490962400722, 0.9906859460363316439 ) ) ;
#6072=CARTESIAN_POINT ( 'NONE',  ( 19.99999999999999645, 38.69327817041775575, 52.53819777490647880 ) ) ;
#6077=DIRECTION ( 'NONE',  ( -1.000000000000000000, 0.000000000000000000, -0.000000000000000000 ) ) ;
#6078=EDGE_CURVE ( 'NONE', #8357, #18441, #19283, .T. ) ;
#6079=VERTEX_POINT ( 'NONE', #9441 ) ;
#6082=CARTESIAN_POINT ( 'NONE',  ( 19.99999999999999645, 0.000000000000000000, 0.000000000000000000 ) ) ;
#6086=DIRECTION ( 'NONE',  ( -1.000000000000000000, -0.000000000000000000, -0.000000000000000000 ) ) ;
#6090=DIRECTION ( 'NONE',  ( -1.000000000000000000, 0.000000000000000000, 0.000000000000000000 ) ) ;
#6093=ORIENTED_EDGE ( 'NONE', *, *, #8322, .T. ) ;
#6094=DIRECTION ( 'NONE',  ( -1.000000000000000000, 0.000000000000000000, 0.000000000000000000 ) ) ;
#6096=ORIENTED_EDGE ( 'NONE', *, *, #16474, .T. ) ;
#6098=EDGE_CURVE ( 'NONE', #12564, #3220, #16147, .T. ) ;
#6100=EDGE_CURVE ( 'NONE', #6425, #8357, #13089, .T. ) ;
#6104=ORIENTED_EDGE ( 'NONE', *, *, #19458, .T. ) ;
#6108=VECTOR ( 'NONE', #4587, 1000.000000000000000 ) ;
#6110=CARTESIAN_POINT ( 'NONE',  ( 0.000000000000000000, 29.55812890832068973, -65.65300461859658299 ) ) ;
#6113=EDGE_LOOP ( 'NONE', ( #18219, #15998, #11005, #16724 ) ) ;
#6116=CIRCLE ( 'NONE', #17973, 7.500000000000000000 ) ;
#6117=DIRECTION ( 'NONE',  ( 1.000000000000000000, 0.000000000000000000, 0.000000000000000000 ) ) ;
#6118=CARTESIAN_POINT ( 'NONE',  ( 0.000000000000000000, 10.74906464462217848, -71.19310085447958159 ) ) ;
#6120=EDGE_CURVE ( 'NONE', #1182, #3247, #20870, .T. ) ;
#6124=CIRCLE ( 'NONE', #17978, 27.60000000002760245 ) ;
#6126=DIRECTION ( 'NONE',  ( -1.000000000000000000, 0.000000000000000000, 0.000000000000000000 ) ) ;
#6128=ADVANCED_FACE ( 'NONE', ( #1801 ), #8254, .T. ) ;
#6129=CARTESIAN_POINT ( 'NONE',  ( 19.99999999999999645, -63.05226888949880504, -15.11556105343524514 ) ) ;
#6132=FACE_OUTER_BOUND ( 'NONE', #17937, .T. ) ;
#6135=EDGE_LOOP ( 'NONE', ( #16412, #5737, #3915, #15562 ) ) ;
#6145=AXIS2_PLACEMENT_3D ( 'NONE', #9760, #17718, #7965 ) ;
#6146=DIRECTION ( 'NONE',  ( 0.000000000000000000, 0.8878852184023764416, -0.4600650377311500394 ) ) ;
#6147=DIRECTION ( 'NONE',  ( -1.000000000000000000, -0.000000000000000000, -0.000000000000000000 ) ) ;
#6151=CARTESIAN_POINT ( 'NONE',  ( 0.000000000000000000, 65.23577793412344761, -1.313498510941930153 ) ) ;
#6152=AXIS2_PLACEMENT_3D ( 'NONE', #3680, #2312, #5475 ) ;
#6159=CARTESIAN_POINT ( 'NONE',  ( 19.99999999999999645, 36.59093685910711002, -62.00889726307995176 ) ) ;
#6160=ORIENTED_EDGE ( 'NONE', *, *, #19954, .T. ) ;
#6161=CARTESIAN_POINT ( 'NONE',  ( 9.999999999999998224, -18.50424539729892714, 69.58155576219110117 ) ) ;
#6166=EDGE_CURVE ( 'NONE', #2187, #1411, #8683, .T. ) ;
#6169=CIRCLE ( 'NONE', #19700, 27.60000000002759890 ) ;
#6172=DIRECTION ( 'NONE',  ( -1.000000000000000000, 0.000000000000000000, 0.000000000000000000 ) ) ;
#6180=VERTEX_POINT ( 'NONE', #18115 ) ;
#6184=AXIS2_PLACEMENT_3D ( 'NONE', #1594, #12614, #19076 ) ;
#6185=VECTOR ( 'NONE', #14010, 1000.000000000000000 ) ;
#6188=CIRCLE ( 'NONE', #6513, 65.24900000006525147 ) ;
#6189=DIRECTION ( 'NONE',  ( -1.000000000000000000, -0.000000000000000000, -0.000000000000000000 ) ) ;
#6191=ORIENTED_EDGE ( 'NONE', *, *, #4642, .T. ) ;
#6192=FACE_OUTER_BOUND ( 'NONE', #5757, .T. ) ;
#6193=ORIENTED_EDGE ( 'NONE', *, *, #6478, .T. ) ;
#6194=CARTESIAN_POINT ( 'NONE',  ( 19.99999999999999645, 23.08379033237438094, -61.02926039941409897 ) ) ;
#6196=VERTEX_POINT ( 'NONE', #308 ) ;
#6197=CYLINDRICAL_SURFACE ( 'NONE', #5331, 65.24900000006525147 ) ;
#6204=ORIENTED_EDGE ( 'NONE', *, *, #5540, .T. ) ;
#6206=DIRECTION ( 'NONE',  ( -1.000000000000000000, 0.000000000000000000, 0.000000000000000000 ) ) ;
#6208=AXIS2_PLACEMENT_3D ( 'NONE', #20458, #5937, #12408 ) ;
#6211=DIRECTION ( 'NONE',  ( 1.000000000000000000, -0.000000000000000000, -0.000000000000000000 ) ) ;
#6212=AXIS2_PLACEMENT_3D ( 'NONE', #2126, #19714, #743 ) ;
#6213=ORIENTED_EDGE ( 'NONE', *, *, #14819, .F. ) ;
#6214=DIRECTION ( 'NONE',  ( 0.000000000000000000, 0.000000000000000000, 1.000000000000000000 ) ) ;
#6215=ORIENTED_EDGE ( 'NONE', *, *, #15063, .T. ) ;
#6220=VERTEX_POINT ( 'NONE', #3377 ) ;
#6221=CARTESIAN_POINT ( 'NONE',  ( 19.99999999999999645, -64.52323195238632536, 6.389157729492951354 ) ) ;
#6222=CIRCLE ( 'NONE', #16376, 27.60000000002759890 ) ;
#6223=EDGE_CURVE ( 'NONE', #2292, #7786, #5068, .T. ) ;
#6225=EDGE_CURVE ( 'NONE', #12867, #5525, #11733, .T. ) ;
#6226=DIRECTION ( 'NONE',  ( 0.000000000000000000, 0.000000000000000000, -1.000000000000000000 ) ) ;
#6227=DIRECTION ( 'NONE',  ( -1.000000000000000000, -0.000000000000000000, -0.000000000000000000 ) ) ;
#6233=EDGE_CURVE ( 'NONE', #5196, #7047, #13768, .T. ) ;
#6237=DIRECTION ( 'NONE',  ( -1.000000000000000000, -0.000000000000000000, -0.000000000000000000 ) ) ;
#6239=VERTEX_POINT ( 'NONE', #16522 ) ;
#6240=CARTESIAN_POINT ( 'NONE',  ( 19.99999999999999645, -36.54710069451017063, -54.05313526368150434 ) ) ;
#6243=EDGE_LOOP ( 'NONE', ( #223, #15604, #16970, #12922 ) ) ;
#6245=DIRECTION ( 'NONE',  ( -1.000000000000000000, -0.000000000000000000, 0.000000000000000000 ) ) ;
#6247=AXIS2_PLACEMENT_3D ( 'NONE', #16635, #8782, #12085 ) ;
#6248=CARTESIAN_POINT ( 'NONE',  ( 19.99999999999999645, -64.79224928664389438, -2.456263514198281150 ) ) ;
#6257=EDGE_CURVE ( 'NONE', #9751, #10364, #18427, .T. ) ;
#6263=CARTESIAN_POINT ( 'NONE',  ( 0.000000000000000000, -43.56693332842751687, -48.57318520917550586 ) ) ;
#6264=DIRECTION ( 'NONE',  ( 0.000000000000000000, -0.8169698930104470902, 0.5766803221148600889 ) ) ;
#6269=CARTESIAN_POINT ( 'NONE',  ( 19.99999999999999645, 43.56693332842851873, -48.57318520917461058 ) ) ;
#6270=PRODUCT_DEFINITION_FORMATION_WITH_SPECIFIED_SOURCE ( 'ANY', '', #6770, .NOT_KNOWN. ) ;
#6274=VERTEX_POINT ( 'NONE', #18537 ) ;
#6278=VERTEX_POINT ( 'NONE', #18631 ) ;
#6280=AXIS2_PLACEMENT_3D ( 'NONE', #17542, #4801, #1114 ) ;
#6284=EDGE_LOOP ( 'NONE', ( #365, #19352, #3238, #8745 ) ) ;
#6285=DIRECTION ( 'NONE',  ( 1.000000000000000000, 0.000000000000000000, 0.000000000000000000 ) ) ;
#6288=CARTESIAN_POINT ( 'NONE',  ( 19.99999999999999645, 0.000000000000000000, 0.000000000000000000 ) ) ;
#6289=EDGE_LOOP ( 'NONE', ( #3729, #12474, #997, #9876 ) ) ;
#6290=DIRECTION ( 'NONE',  ( -1.000000000000000000, 0.000000000000000000, 0.000000000000000000 ) ) ;
#6292=AXIS2_PLACEMENT_3D ( 'NONE', #19291, #4775, #17720 ) ;
#6293=ORIENTED_EDGE ( 'NONE', *, *, #15852, .F. ) ;
#6295=DIRECTION ( 'NONE',  ( 0.000000000000000000, 0.000000000000000000, 1.000000000000000000 ) ) ;
#6302=AXIS2_PLACEMENT_3D ( 'NONE', #18140, #8279, #3403 ) ;
#6305=VECTOR ( 'NONE', #12807, 1000.000000000000000 ) ;
#6306=DIRECTION ( 'NONE',  ( -1.000000000000000000, 0.000000000000000000, -0.000000000000000000 ) ) ;
#6310=CARTESIAN_POINT ( 'NONE',  ( 0.000000000000000000, 63.05226888949912478, -15.11556105343395906 ) ) ;
#6312=AXIS2_PLACEMENT_3D ( 'NONE', #8813, #7337, #8613 ) ;
#6313=DIRECTION ( 'NONE',  ( 0.000000000000000000, 0.3984010898462361783, 0.9172113015054552676 ) ) ;
#6314=ORIENTED_EDGE ( 'NONE', *, *, #2347, .T. ) ;
#6316=AXIS2_PLACEMENT_3D ( 'NONE', #5645, #8935, #1000 ) ;
#6317=CIRCLE ( 'NONE', #12772, 27.60000000002760245 ) ;
#6320=AXIS2_PLACEMENT_3D ( 'NONE', #16457, #14571, #17951 ) ;
#6327=CARTESIAN_POINT ( 'NONE',  ( 19.99999999999999645, 14.55863677812122425, 63.60407295269110506 ) ) ;
#6334=CARTESIAN_POINT ( 'NONE',  ( 19.99999999999999645, 48.70996102988739551, -42.79495875147724604 ) ) ;
#6340=LINE ( 'NONE', #12502, #260 ) ;
#6345=ORIENTED_EDGE ( 'NONE', *, *, #6166, .F. ) ;
#6346=DIRECTION ( 'NONE',  ( -1.000000000000000000, 0.000000000000000000, 0.000000000000000000 ) ) ;
#6348=ADVANCED_FACE ( 'NONE', ( #18220 ), #10158, .T. ) ;
#6350=CARTESIAN_POINT ( 'NONE',  ( 150.0000507999999968, 0.000000000000000000, 0.000000000000000000 ) ) ;
#6351=EDGE_LOOP ( 'NONE', ( #3020, #11830, #6676, #13411 ) ) ;
#6353=ORIENTED_EDGE ( 'NONE', *, *, #10920, .F. ) ;
#6354=LINE ( 'NONE', #6659, #5802 ) ;
#6355=LINE ( 'NONE', #14528, #2138 ) ;
#6359=ADVANCED_FACE ( 'NONE', ( #12065 ), #2105, .T. ) ;
#6361=CARTESIAN_POINT ( 'NONE',  ( 19.99999999999999645, 15.58726123847937828, -62.93731870009387563 ) ) ;
#6364=ADVANCED_FACE ( 'NONE', ( #16726 ), #13658, .T. ) ;
#6366=DIRECTION ( 'NONE',  ( -1.000000000000000000, 0.000000000000000000, -0.000000000000000000 ) ) ;
#6367=CARTESIAN_POINT ( 'NONE',  ( 0.000000000000000000, -64.44931368725514176, -10.18420179740675380 ) ) ;
#6369=EDGE_CURVE ( 'NONE', #4779, #6220, #3282, .T. ) ;
#6370=ORIENTED_EDGE ( 'NONE', *, *, #3890, .F. ) ;
#6373=ORIENTED_EDGE ( 'NONE', *, *, #13687, .T. ) ;
#6375=DIRECTION ( 'NONE',  ( 0.000000000000000000, 0.2697967711570248839, -0.9629172873477991335 ) ) ;
#6376=ORIENTED_EDGE ( 'NONE', *, *, #1459, .T. ) ;
#6377=FACE_OUTER_BOUND ( 'NONE', #8718, .T. ) ;
#6379=DIRECTION ( 'NONE',  ( -1.000000000000000000, -0.000000000000000000, 0.000000000000000000 ) ) ;
#6380=CARTESIAN_POINT ( 'NONE',  ( 19.99999999999999645, 0.000000000000000000, 0.000000000000000000 ) ) ;
#6386=CARTESIAN_POINT ( 'NONE',  ( 9.999999999999998224, 46.17500197033132281, -55.24372537266351912 ) ) ;
#6387=ADVANCED_FACE ( 'NONE', ( #16932 ), #8875, .T. ) ;
#6388=ORIENTED_EDGE ( 'NONE', *, *, #8388, .T. ) ;
#6392=ORIENTED_EDGE ( 'NONE', *, *, #13835, .T. ) ;
#6394=CARTESIAN_POINT ( 'NONE',  ( 0.000000000000000000, 0.000000000000000000, 0.000000000000000000 ) ) ;
#6398=CARTESIAN_POINT ( 'NONE',  ( 0.000000000000000000, 0.000000000000000000, 0.000000000000000000 ) ) ;
#6399=DIRECTION ( 'NONE',  ( -1.000000000000000000, 0.000000000000000000, 0.000000000000000000 ) ) ;
#6400=ORIENTED_EDGE ( 'NONE', *, *, #2403, .T. ) ;
#6403=DIRECTION ( 'NONE',  ( 0.000000000000000000, 0.000000000000000000, 1.000000000000000000 ) ) ;
#6404=ORIENTED_EDGE ( 'NONE', *, *, #6822, .F. ) ;
#6405=DIRECTION ( 'NONE',  ( -1.000000000000000000, 0.000000000000000000, -0.000000000000000000 ) ) ;
#6406=CARTESIAN_POINT ( 'NONE',  ( 19.99999999999999645, 6.872116855664026858, -64.47358224882410127 ) ) ;
#6409=CARTESIAN_POINT ( 'NONE',  ( 19.99999999999999645, -27.80658314415179078, -66.41380830714150818 ) ) ;
#6416=AXIS2_PLACEMENT_3D ( 'NONE', #8015, #11097, #7593 ) ;
#6417=EDGE_LOOP ( 'NONE', ( #19331, #2057, #16028, #4385 ) ) ;
#6418=DIRECTION ( 'NONE',  ( 1.000000000000000000, 0.000000000000000000, 0.000000000000000000 ) ) ;
#6419=CARTESIAN_POINT ( 'NONE',  ( 19.99999999999999645, 0.000000000000000000, 0.000000000000000000 ) ) ;
#6421=DIRECTION ( 'NONE',  ( -1.000000000000000000, 0.000000000000000000, 0.000000000000000000 ) ) ;
#6423=DIRECTION ( 'NONE',  ( 0.000000000000000000, 0.000000000000000000, 1.000000000000000000 ) ) ;
#6424=EDGE_CURVE ( 'NONE', #2180, #14573, #6317, .T. ) ;
#6425=VERTEX_POINT ( 'NONE', #9099 ) ;
#6427=DIRECTION ( 'NONE',  ( 0.000000000000000000, -0.5195839500354404450, 0.8544194045464844622 ) ) ;
#6428=CARTESIAN_POINT ( 'NONE',  ( 0.000000000000000000, -63.85430960833482317, 16.34407078397855528 ) ) ;
#6431=ORIENTED_EDGE ( 'NONE', *, *, #15767, .F. ) ;
#6436=VECTOR ( 'NONE', #16562, 1000.000000000000000 ) ;
#6437=ORIENTED_EDGE ( 'NONE', *, *, #3653, .T. ) ;
#6442=CARTESIAN_POINT ( 'NONE',  ( 19.99999999999999645, 23.08379033237438094, -61.02926039941409897 ) ) ;
#6446=EDGE_CURVE ( 'NONE', #18079, #17770, #6022, .T. ) ;
#6447=VECTOR ( 'NONE', #10326, 1000.000000000000000 ) ;
#6456=DIRECTION ( 'NONE',  ( -1.000000000000000000, -0.000000000000000000, 0.000000000000000000 ) ) ;
#6459=CARTESIAN_POINT ( 'NONE',  ( 0.000000000000000000, -27.80658314415272514, 66.41380830714115291 ) ) ;
#6462=ORIENTED_EDGE ( 'NONE', *, *, #10399, .F. ) ;
#6463=CARTESIAN_POINT ( 'NONE',  ( 0.000000000000000000, 54.08351995568706627, 35.76369202524519864 ) ) ;
#6473=ORIENTED_EDGE ( 'NONE', *, *, #12086, .F. ) ;
#6474=VERTEX_POINT ( 'NONE', #20736 ) ;
#6476=DIRECTION ( 'NONE',  ( 1.000000000000000000, 0.000000000000000000, 0.000000000000000000 ) ) ;
#6477=AXIS2_PLACEMENT_3D ( 'NONE', #951, #5481, #12166 ) ;
#6478=EDGE_CURVE ( 'NONE', #9154, #1772, #15803, .T. ) ;
#6479=EDGE_CURVE ( 'NONE', #19715, #12410, #18954, .T. ) ;
#6480=CARTESIAN_POINT ( 'NONE',  ( 19.99999999999999645, -59.31169354540720207, -27.19476070466916795 ) ) ;
#6486=EDGE_CURVE ( 'NONE', #5273, #20260, #5310, .T. ) ;
#6489=CARTESIAN_POINT ( 'NONE',  ( 0.000000000000000000, 64.52323195238639642, -6.389157729492497495 ) ) ;
#6491=CARTESIAN_POINT ( 'NONE',  ( 0.000000000000000000, -55.05624179291956466, -35.01774179823839717 ) ) ;
#6493=DIRECTION ( 'NONE',  ( 0.000000000000000000, 0.1361666490962468723, -0.9906859460363307557 ) ) ;
#6495=ORIENTED_EDGE ( 'NONE', *, *, #10802, .F. ) ;
#6499=DIRECTION ( 'NONE',  ( -1.000000000000000000, -0.000000000000000000, 0.000000000000000000 ) ) ;
#6500=AXIS2_PLACEMENT_3D ( 'NONE', #2433, #7306, #15371 ) ;
#6505=DIRECTION ( 'NONE',  ( 0.000000000000000000, 0.000000000000000000, -1.000000000000000000 ) ) ;
#6507=VECTOR ( 'NONE', #5918, 1000.000000000000000 ) ;
#6512=CARTESIAN_POINT ( 'NONE',  ( 0.000000000000000000, 51.96384592647199696, 49.83732252579633126 ) ) ;
#6513=AXIS2_PLACEMENT_3D ( 'NONE', #8352, #18000, #5164 ) ;
#6514=ORIENTED_EDGE ( 'NONE', *, *, #4005, .T. ) ;
#6515=FACE_OUTER_BOUND ( 'NONE', #946, .T. ) ;
#6520=VERTEX_POINT ( 'NONE', #5914 ) ;
#6523=CIRCLE ( 'NONE', #7184, 4.000000000000000000 ) ;
#6530=CARTESIAN_POINT ( 'NONE',  ( 19.99999999999999645, 64.52323195238639642, -6.389157729492497495 ) ) ;
#6531=CARTESIAN_POINT ( 'NONE',  ( 19.99999999999999645, 36.59093685910629290, 62.00889726308042782 ) ) ;
#6535=AXIS2_PLACEMENT_3D ( 'NONE', #5308, #5405, #10186 ) ;
#6537=CARTESIAN_POINT ( 'NONE',  ( 19.99999999999999645, 55.05624179291979914, 35.01774179823801347 ) ) ;
#6539=LINE ( 'NONE', #17990, #14165 ) ;
#6540=CIRCLE ( 'NONE', #18396, 27.60000000002759890 ) ;
#6542=ADVANCED_FACE ( 'NONE', ( #10797 ), #17258, .T. ) ;
#6544=ORIENTED_EDGE ( 'NONE', *, *, #10240, .F. ) ;
#6545=CYLINDRICAL_SURFACE ( 'NONE', #9578, 27.60000000002760245 ) ;
#6546=CYLINDRICAL_SURFACE ( 'NONE', #19539, 65.24900000006525147 ) ;
#6548=ORIENTED_EDGE ( 'NONE', *, *, #1722, .F. ) ;
#6554=EDGE_LOOP ( 'NONE', ( #7550, #7063, #20786, #5857 ) ) ;
#6557=AXIS2_PLACEMENT_3D ( 'NONE', #893, #20271, #17106 ) ;
#6564=VECTOR ( 'NONE', #16676, 1000.000000000000000 ) ;
#6567=CIRCLE ( 'NONE', #1181, 65.24900000006525147 ) ;
#6569=DIRECTION ( 'NONE',  ( 0.000000000000000000, 0.000000000000000000, 1.000000000000000000 ) ) ;
#6572=FACE_OUTER_BOUND ( 'NONE', #11665, .T. ) ;
#6580=VERTEX_POINT ( 'NONE', #19663 ) ;
#6581=ORIENTED_EDGE ( 'NONE', *, *, #10428, .T. ) ;
#6582=CARTESIAN_POINT ( 'NONE',  ( 19.99999999999999645, -42.42902769288503606, -49.02903636734241388 ) ) ;
#6589=CARTESIAN_POINT ( 'NONE',  ( 9.999999999999998224, -68.15657073222450890, 23.20952102120258331 ) ) ;
#6590=CARTESIAN_POINT ( 'NONE',  ( 19.99999999999999645, 0.000000000000000000, 0.000000000000000000 ) ) ;
#6593=DIRECTION ( 'NONE',  ( -1.000000000000000000, -0.000000000000000000, 0.000000000000000000 ) ) ;
#6594=ORIENTED_EDGE ( 'NONE', *, *, #13605, .F. ) ;
#6596=LINE ( 'NONE', #8297, #13008 ) ;
#6599=DIRECTION ( 'NONE',  ( 0.000000000000000000, 0.000000000000000000, 1.000000000000000000 ) ) ;
#6601=VECTOR ( 'NONE', #1330, 1000.000000000000000 ) ;
#6603=ADVANCED_FACE ( 'NONE', ( #16193 ), #3355, .T. ) ;
#6606=DIRECTION ( 'NONE',  ( -1.000000000000000000, 0.000000000000000000, -0.000000000000000000 ) ) ;
#6607=VECTOR ( 'NONE', #1321, 1000.000000000000000 ) ;
#6612=CARTESIAN_POINT ( 'NONE',  ( 0.000000000000000000, 0.000000000000000000, 0.000000000000000000 ) ) ;
#6615=EDGE_CURVE ( 'NONE', #14502, #17420, #13785, .T. ) ;
#6619=EDGE_CURVE ( 'NONE', #5352, #2775, #1929, .T. ) ;
#6629=DIRECTION ( 'NONE',  ( -1.000000000000000000, -0.000000000000000000, 0.000000000000000000 ) ) ;
#6631=ADVANCED_FACE ( 'NONE', ( #14510 ), #19361, .T. ) ;
#6633=DIRECTION ( 'NONE',  ( -1.000000000000000000, 0.000000000000000000, -0.000000000000000000 ) ) ;
#6634=AXIS2_PLACEMENT_3D ( 'NONE', #3204, #1922, #13058 ) ;
#6638=ORIENTED_EDGE ( 'NONE', *, *, #3058, .T. ) ;
#6639=AXIS2_PLACEMENT_3D ( 'NONE', #6862, #3290, #8257 ) ;
#6642=CARTESIAN_POINT ( 'NONE',  ( 19.99999999999999645, 0.000000000000000000, 0.000000000000000000 ) ) ;
#6644=VECTOR ( 'NONE', #11438, 1000.000000000000000 ) ;
#6650=ORIENTED_EDGE ( 'NONE', *, *, #962, .F. ) ;
#6651=FACE_OUTER_BOUND ( 'NONE', #20921, .T. ) ;
#6657=DIRECTION ( 'NONE',  ( -1.000000000000000000, 0.000000000000000000, 0.000000000000000000 ) ) ;
#6659=CARTESIAN_POINT ( 'NONE',  ( 19.99999999999999645, -64.80702306891100761, 7.581672767546201008 ) ) ;
#6660=DIRECTION ( 'NONE',  ( 0.000000000000000000, 0.2697967711570248839, -0.9629172873477991335 ) ) ;
#6667=FACE_OUTER_BOUND ( 'NONE', #9037, .T. ) ;
#6673=DIRECTION ( 'NONE',  ( -1.000000000000000000, 0.000000000000000000, 0.000000000000000000 ) ) ;
#6675=CIRCLE ( 'NONE', #1621, 72.00000000007199219 ) ;
#6676=ORIENTED_EDGE ( 'NONE', *, *, #3985, .T. ) ;
#6680=CARTESIAN_POINT ( 'NONE',  ( 0.000000000000000000, 0.000000000000000000, 0.000000000000000000 ) ) ;
#6681=ORIENTED_EDGE ( 'NONE', *, *, #15852, .T. ) ;
#6684=DIRECTION ( 'NONE',  ( 0.000000000000000000, -0.8169698930104470902, 0.5766803221148600889 ) ) ;
#6693=CARTESIAN_POINT ( 'NONE',  ( 0.000000000000000000, 46.17500197033132991, -55.24372537266351912 ) ) ;
#6695=ORIENTED_EDGE ( 'NONE', *, *, #1090, .F. ) ;
#6696=CARTESIAN_POINT ( 'NONE',  ( 19.99999999999999645, 71.76067541710850151, 5.865617076724869428 ) ) ;
#6698=CARTESIAN_POINT ( 'NONE',  ( 0.000000000000000000, 45.48683723007212620, 46.78012013466234720 ) ) ;
#6701=VERTEX_POINT ( 'NONE', #14600 ) ;
#6707=ORIENTED_EDGE ( 'NONE', *, *, #18678, .F. ) ;
#6710=DIRECTION ( 'NONE',  ( -1.000000000000000000, 0.000000000000000000, 0.000000000000000000 ) ) ;
#6711=VERTEX_POINT ( 'NONE', #13016 ) ;
#6712=EDGE_CURVE ( 'NONE', #8080, #17681, #11749, .T. ) ;
#6716=EDGE_CURVE ( 'NONE', #20034, #17803, #2184, .T. ) ;
#6718=CARTESIAN_POINT ( 'NONE',  ( 0.000000000000000000, -23.08379033237394395, 61.02926039941428371 ) ) ;
#6719=CARTESIAN_POINT ( 'NONE',  ( 19.99999999999999645, 0.000000000000000000, 0.000000000000000000 ) ) ;
#6726=EDGE_CURVE ( 'NONE', #2919, #1411, #5454, .T. ) ;
#6730=ORIENTED_EDGE ( 'NONE', *, *, #19226, .F. ) ;
#6733=VERTEX_POINT ( 'NONE', #10555 ) ;
#6740=DIRECTION ( 'NONE',  ( 0.000000000000000000, 0.3984010898462422290, -0.9172113015054527141 ) ) ;
#6748=ORIENTED_EDGE ( 'NONE', *, *, #5865, .F. ) ;
#6753=FACE_OUTER_BOUND ( 'NONE', #12506, .T. ) ;
#6757=ORIENTED_EDGE ( 'NONE', *, *, #7368, .F. ) ;
#6758=ADVANCED_FACE ( 'NONE', ( #13630 ), #10135, .T. ) ;
#6762=CYLINDRICAL_SURFACE ( 'NONE', #910, 27.60000000002759890 ) ;
#6763=CARTESIAN_POINT ( 'NONE',  ( 0.000000000000000000, 60.35829202194874910, 24.78524934717571426 ) ) ;
#6770=PRODUCT ( 'spur gear_iso_ISO - Spur gear 3M 46T 20PA 20FW ---S46C15H150L8.0S1', 'spur gear_iso_ISO - Spur gear 3M 46T 20PA 20FW ---S46C15H150L8.0S1', '', ( #10137 ) ) ;
#6774=FACE_OUTER_BOUND ( 'NONE', #19923, .T. ) ;
#6785=ORIENTED_EDGE ( 'NONE', *, *, #2323, .T. ) ;
#6787=DIRECTION ( 'NONE',  ( 0.000000000000000000, 0.000000000000000000, 1.000000000000000000 ) ) ;
#6788=CARTESIAN_POINT ( 'NONE',  ( 19.99999999999999645, 0.000000000000000000, 0.000000000000000000 ) ) ;
#6791=CIRCLE ( 'NONE', #9518, 27.60000000002760245 ) ;
#6792=DIRECTION ( 'NONE',  ( -1.000000000000000000, -0.000000000000000000, 0.000000000000000000 ) ) ;
#6793=DIRECTION ( 'NONE',  ( 0.000000000000000000, 0.9976687691905389288, 0.06824241336467461172 ) ) ;
#6795=ORIENTED_EDGE ( 'NONE', *, *, #17282, .F. ) ;
#6800=DIRECTION ( 'NONE',  ( -1.000000000000000000, 0.000000000000000000, -0.000000000000000000 ) ) ;
#6811=CARTESIAN_POINT ( 'NONE',  ( -10.00000000000000000, 0.000000000000000000, 0.000000000000000000 ) ) ;
#6816=CARTESIAN_POINT ( 'NONE',  ( 19.99999999999999645, 64.79224928664392280, 25.14373648582975918 ) ) ;
#6820=AXIS2_PLACEMENT_3D ( 'NONE', #14023, #13910, #20358 ) ;
#6822=EDGE_CURVE ( 'NONE', #12431, #10201, #7341, .T. ) ;
#6826=DIRECTION ( 'NONE',  ( -1.000000000000000000, 0.000000000000000000, -0.000000000000000000 ) ) ;
#6828=DIRECTION ( 'NONE',  ( 1.000000000000000000, -0.000000000000000000, -0.000000000000000000 ) ) ;
#6829=ORIENTED_EDGE ( 'NONE', *, *, #16526, .T. ) ;
#6830=EDGE_CURVE ( 'NONE', #19485, #17488, #7001, .T. ) ;
#6832=CARTESIAN_POINT ( 'NONE',  ( 19.99999999999999645, -46.17500197033096754, 55.24372537266381045 ) ) ;
#6833=ORIENTED_EDGE ( 'NONE', *, *, #16620, .T. ) ;
#6834=DIRECTION ( 'NONE',  ( -1.000000000000000000, -0.000000000000000000, 0.000000000000000000 ) ) ;
#6835=VECTOR ( 'NONE', #20543, 1000.000000000000000 ) ;
#6836=VECTOR ( 'NONE', #14949, 1000.000000000000000 ) ;
#6837=LINE ( 'NONE', #1982, #4840 ) ;
#6848=CIRCLE ( 'NONE', #20732, 27.60000000002759890 ) ;
#6851=EDGE_LOOP ( 'NONE', ( #11813, #14875, #8634, #2168 ) ) ;
#6859=VERTEX_POINT ( 'NONE', #20189 ) ;
#6862=CARTESIAN_POINT ( 'NONE',  ( 19.99999999999999645, -10.77748419466740692, 63.93680186330469439 ) ) ;
#6863=DIRECTION ( 'NONE',  ( 1.000000000000000000, 0.000000000000000000, 0.000000000000000000 ) ) ;
#6873=AXIS2_PLACEMENT_3D ( 'NONE', #11477, #20915, #4805 ) ;
#6874=CARTESIAN_POINT ( 'NONE',  ( 19.99999999999999645, 0.000000000000000000, 0.000000000000000000 ) ) ;
#6875=DIRECTION ( 'NONE',  ( -1.000000000000000000, 0.000000000000000000, 0.000000000000000000 ) ) ;
#6878=CIRCLE ( 'NONE', #14014, 27.60000000002759890 ) ;
#6882=DIRECTION ( 'NONE',  ( -1.000000000000000000, -0.000000000000000000, -0.000000000000000000 ) ) ;
#6883=CIRCLE ( 'NONE', #15354, 65.24900000006525147 ) ;
#6884=ORIENTED_EDGE ( 'NONE', *, *, #9604, .F. ) ;
#6889=DIRECTION ( 'NONE',  ( 1.000000000000000000, 0.000000000000000000, 0.000000000000000000 ) ) ;
#6893=ORIENTED_EDGE ( 'NONE', *, *, #10528, .T. ) ;
#6900=CARTESIAN_POINT ( 'NONE',  ( 9.999999999999998224, 59.36728637278075382, -40.73727173906726762 ) ) ;
#6903=DIRECTION ( 'NONE',  ( -1.000000000000000000, 0.000000000000000000, 0.000000000000000000 ) ) ;
#6910=DIRECTION ( 'NONE',  ( -1.000000000000000000, -0.000000000000000000, 0.000000000000000000 ) ) ;
#6918=ADVANCED_FACE ( 'NONE', ( #2707 ), #2613, .T. ) ;
#6924=EDGE_CURVE ( 'NONE', #5449, #18310, #9175, .T. ) ;
#6935=CARTESIAN_POINT ( 'NONE',  ( 0.000000000000000000, 0.000000000000000000, 0.000000000000000000 ) ) ;
#6940=ORIENTED_EDGE ( 'NONE', *, *, #6098, .F. ) ;
#6945=AXIS2_PLACEMENT_3D ( 'NONE', #10537, #16898, #2373 ) ;
#6947=ADVANCED_FACE ( 'NONE', ( #2813 ), #6197, .T. ) ;
#6948=CARTESIAN_POINT ( 'NONE',  ( 19.99999999999999645, 64.80702306891095077, 7.581672767546655756 ) ) ;
#6950=ORIENTED_EDGE ( 'NONE', *, *, #16069, .T. ) ;
#6954=AXIS2_PLACEMENT_3D ( 'NONE', #10749, #8815, #15508 ) ;
#6957=ORIENTED_EDGE ( 'NONE', *, *, #8210, .F. ) ;
#6961=PLANE ( 'NONE',  #8891 ) ;
#6965=EDGE_LOOP ( 'NONE', ( #11081, #12832, #9268, #4993 ) ) ;
#6966=VERTEX_POINT ( 'NONE', #4193 ) ;
#6972=CIRCLE ( 'NONE', #16805, 27.60000000002759535 ) ;
#6973=CIRCLE ( 'NONE', #18843, 72.00000000007199219 ) ;
#6980=DIRECTION ( 'NONE',  ( 0.000000000000000000, 0.5195839500354345608, -0.8544194045464879039 ) ) ;
#6981=AXIS2_PLACEMENT_3D ( 'NONE', #721, #838, #8668 ) ;
#6982=ORIENTED_EDGE ( 'NONE', *, *, #18463, .F. ) ;
#6983=DIRECTION ( 'NONE',  ( 0.000000000000000000, -0.5195839500354227924, -0.8544194045464950094 ) ) ;
#6991=AXIS2_PLACEMENT_3D ( 'NONE', #12483, #7806, #7483 ) ;
#6993=DIRECTION ( 'NONE',  ( 0.000000000000000000, 0.000000000000000000, 1.000000000000000000 ) ) ;
#6996=ORIENTED_EDGE ( 'NONE', *, *, #6166, .T. ) ;
#6997=ORIENTED_EDGE ( 'NONE', *, *, #1858, .T. ) ;
#6999=CIRCLE ( 'NONE', #18869, 27.60000000002759890 ) ;
#7000=FACE_OUTER_BOUND ( 'NONE', #3836, .T. ) ;
#7001=CIRCLE ( 'NONE', #20196, 27.60000000002760245 ) ;
#7002=CARTESIAN_POINT ( 'NONE',  ( 19.99999999999999645, 46.01927912072591198, -45.67597560296339765 ) ) ;
#7009=CARTESIAN_POINT ( 'NONE',  ( 19.99999999999999645, 0.000000000000000000, 0.000000000000000000 ) ) ;
#7010=CARTESIAN_POINT ( 'NONE',  ( 19.99999999999999645, 71.89099403602354244, 3.960426305689046522 ) ) ;
#7011=DIRECTION ( 'NONE',  ( 0.000000000000000000, 0.7308359642781205867, 0.6825531432186576763 ) ) ;
#7014=EDGE_LOOP ( 'NONE', ( #14656, #10736, #12393, #9522 ) ) ;
#7025=ORIENTED_EDGE ( 'NONE', *, *, #88, .T. ) ;
#7031=EDGE_CURVE ( 'NONE', #19744, #10678, #18533, .T. ) ;
#7037=VERTEX_POINT ( 'NONE', #11489 ) ;
#7039=VERTEX_POINT ( 'NONE', #12795 ) ;
#7045=ORIENTED_EDGE ( 'NONE', *, *, #5836, .T. ) ;
#7046=DIRECTION ( 'NONE',  ( 0.000000000000000000, 0.2697967711570183891, 0.9629172873478009098 ) ) ;
#7047=VERTEX_POINT ( 'NONE', #16169 ) ;
#7050=DIRECTION ( 'NONE',  ( 1.000000000000000000, 0.000000000000000000, 0.000000000000000000 ) ) ;
#7053=ORIENTED_EDGE ( 'NONE', *, *, #14911, .T. ) ;
#7055=ORIENTED_EDGE ( 'NONE', *, *, #1484, .T. ) ;
#7056=CARTESIAN_POINT ( 'NONE',  ( 19.99999999999999645, 20.60847369613070512, -61.90898814327692889 ) ) ;
#7058=DIRECTION ( 'NONE',  ( -1.000000000000000000, 0.000000000000000000, 0.000000000000000000 ) ) ;
#7063=ORIENTED_EDGE ( 'NONE', *, *, #8532, .T. ) ;
#7071=DIRECTION ( 'NONE',  ( 0.000000000000000000, 0.000000000000000000, 1.000000000000000000 ) ) ;
#7076=CARTESIAN_POINT ( 'NONE',  ( 0.000000000000000000, 0.000000000000000000, 0.000000000000000000 ) ) ;
#7081=EDGE_LOOP ( 'NONE', ( #13646, #20132, #3224, #17676 ) ) ;
#7082=EDGE_CURVE ( 'NONE', #20014, #19780, #17193, .T. ) ;
#7083=DIRECTION ( 'NONE',  ( -1.000000000000000000, 0.000000000000000000, 0.000000000000000000 ) ) ;
#7086=EDGE_LOOP ( 'NONE', ( #13540, #16, #12934, #5681 ) ) ;
#7087=CARTESIAN_POINT ( 'NONE',  ( 19.99999999999999645, -54.08351995568681048, -35.76369202524558233 ) ) ;
#7088=VECTOR ( 'NONE', #8972, 1000.000000000000000 ) ;
#7093=ORIENTED_EDGE ( 'NONE', *, *, #5354, .T. ) ;
#7096=AXIS2_PLACEMENT_3D ( 'NONE', #8289, #18047, #14761 ) ;
#7097=SURFACE_STYLE_FILL_AREA ( #15266 ) ;
#7099=CARTESIAN_POINT ( 'NONE',  ( 19.99999999999999645, -10.77748419466740692, 63.93680186330469439 ) ) ;
#7101=CIRCLE ( 'NONE', #16933, 72.00000000007199219 ) ;
#7103=DIRECTION ( 'NONE',  ( 0.000000000000000000, -0.9976687691905384847, -0.06824241336468166164 ) ) ;
#7111=CIRCLE ( 'NONE', #9157, 65.24900000006525147 ) ;
#7115=PRODUCT_DEFINITION_SHAPE ( 'NONE', 'NONE',  #17783 ) ;
#7117=DIRECTION ( 'NONE',  ( 0.000000000000000000, 0.000000000000000000, -1.000000000000000000 ) ) ;
#7118=ORIENTED_EDGE ( 'NONE', *, *, #8845, .F. ) ;
#7124=CYLINDRICAL_SURFACE ( 'NONE', #16387, 65.24900000006525147 ) ;
#7125=FACE_OUTER_BOUND ( 'NONE', #1973, .T. ) ;
#7126=EDGE_CURVE ( 'NONE', #18161, #10180, #261, .T. ) ;
#7130=ORIENTED_EDGE ( 'NONE', *, *, #14164, .T. ) ;
#7132=ORIENTED_EDGE ( 'NONE', *, *, #14649, .F. ) ;
#7134=CARTESIAN_POINT ( 'NONE',  ( 0.000000000000000000, 0.000000000000000000, 0.000000000000000000 ) ) ;
#7138=CARTESIAN_POINT ( 'NONE',  ( 0.000000000000000000, 0.000000000000000000, 0.000000000000000000 ) ) ;
#7139=ORIENTED_EDGE ( 'NONE', *, *, #10070, .F. ) ;
#7141=CIRCLE ( 'NONE', #19657, 65.24900000006526568 ) ;
#7142=ORIENTED_EDGE ( 'NONE', *, *, #9798, .T. ) ;
#7143=CARTESIAN_POINT ( 'NONE',  ( 19.99999999999999645, 46.01927912072526539, 45.67597560296404424 ) ) ;
#7144=EDGE_CURVE ( 'NONE', #10526, #10560, #5659, .T. ) ;
#7145=ADVANCED_FACE ( 'NONE', ( #16062 ), #14379, .T. ) ;
#7147=AXIS2_PLACEMENT_3D ( 'NONE', #20314, #10697, #17159 ) ;
#7149=ADVANCED_FACE ( 'NONE', ( #1750 ), #11182, .T. ) ;
#7154=CIRCLE ( 'NONE', #1083, 72.00000000007199219 ) ;
#7156=LINE ( 'NONE', #5263, #5883 ) ;
#7157=AXIS2_PLACEMENT_3D ( 'NONE', #198, #5166, #1603 ) ;
#7159=CARTESIAN_POINT ( 'NONE',  ( 19.99999999999999645, 0.000000000000000000, 0.000000000000000000 ) ) ;
#7162=CIRCLE ( 'NONE', #9880, 65.24900000006526568 ) ;
#7163=ADVANCED_FACE ( 'NONE', ( #8408 ), #14880, .T. ) ;
#7167=ORIENTED_EDGE ( 'NONE', *, *, #601, .F. ) ;
#7171=VERTEX_POINT ( 'NONE', #3532 ) ;
#7172=CYLINDRICAL_SURFACE ( 'NONE', #2770, 72.00000000007199219 ) ;
#7175=CIRCLE ( 'NONE', #19042, 27.60000000002759890 ) ;
#7176=VERTEX_POINT ( 'NONE', #8506 ) ;
#7178=CARTESIAN_POINT ( 'NONE',  ( 19.99999999999999645, 0.000000000000000000, 0.000000000000000000 ) ) ;
#7179=CYLINDRICAL_SURFACE ( 'NONE', #9889, 72.00000000007199219 ) ;
#7182=DIRECTION ( 'NONE',  ( -1.000000000000000000, 0.000000000000000000, 0.000000000000000000 ) ) ;
#7184=AXIS2_PLACEMENT_3D ( 'NONE', #11728, #16503, #2077 ) ;
#7188=DIRECTION ( 'NONE',  ( -1.000000000000000000, -0.000000000000000000, 0.000000000000000000 ) ) ;
#7189=EDGE_LOOP ( 'NONE', ( #16532, #19662, #15425, #17651 ) ) ;
#7192=DIRECTION ( 'NONE',  ( 0.000000000000000000, 0.1361666490962400444, 0.9906859460363315328 ) ) ;
#7195=VERTEX_POINT ( 'NONE', #3839 ) ;
#7196=DIRECTION ( 'NONE',  ( 0.000000000000000000, 0.000000000000000000, 1.000000000000000000 ) ) ;
#7200=CYLINDRICAL_SURFACE ( 'NONE', #16130, 27.60000000002760245 ) ;
#7202=CIRCLE ( 'NONE', #1820, 72.00000000007199219 ) ;
#7205=CARTESIAN_POINT ( 'NONE',  ( 0.000000000000000000, -3.141410481201534211, 65.17333458706185922 ) ) ;
#7206=AXIS2_PLACEMENT_3D ( 'NONE', #15972, #8030, #6423 ) ;
#7208=CARTESIAN_POINT ( 'NONE',  ( 0.000000000000000000, -63.17103598352137794, 16.33561182745118501 ) ) ;
#7211=CIRCLE ( 'NONE', #10954, 65.24900000006526568 ) ;
#7212=LINE ( 'NONE', #655, #3073 ) ;
#7220=ORIENTED_EDGE ( 'NONE', *, *, #16816, .T. ) ;
#7222=EDGE_LOOP ( 'NONE', ( #16749, #15082, #16852, #20913 ) ) ;
#7228=CARTESIAN_POINT ( 'NONE',  ( 19.99999999999999645, -1.971042061627920727, -64.80882494896108881 ) ) ;
#7230=VECTOR ( 'NONE', #650, 1000.000000000000000 ) ;
#7235=ORIENTED_EDGE ( 'NONE', *, *, #14025, .F. ) ;
#7241=EDGE_CURVE ( 'NONE', #13498, #7037, #9066, .T. ) ;
#7242=ORIENTED_EDGE ( 'NONE', *, *, #9744, .T. ) ;
#7250=AXIS2_PLACEMENT_3D ( 'NONE', #12854, #9963, #9859 ) ;
#7262=VECTOR ( 'NONE', #4928, 1000.000000000000000 ) ;
#7264=VERTEX_POINT ( 'NONE', #18478 ) ;
#7265=DIRECTION ( 'NONE',  ( -1.000000000000000000, 0.000000000000000000, 0.000000000000000000 ) ) ;
#7268=ADVANCED_FACE ( 'NONE', ( #13505 ), #780, .T. ) ;
#7269=FACE_OUTER_BOUND ( 'NONE', #19043, .T. ) ;
#7279=DIRECTION ( 'NONE',  ( 1.000000000000000000, 0.000000000000000000, 0.000000000000000000 ) ) ;
#7281=ORIENTED_EDGE ( 'NONE', *, *, #14533, .F. ) ;
#7284=CYLINDRICAL_SURFACE ( 'NONE', #17322, 27.60000000002760245 ) ;
#7287=EDGE_CURVE ( 'NONE', #3334, #14868, #268, .T. ) ;
#7292=VECTOR ( 'NONE', #19307, 1000.000000000000000 ) ;
#7296=CIRCLE ( 'NONE', #14754, 27.60000000002759535 ) ;
#7299=EDGE_CURVE ( 'NONE', #20061, #20910, #4272, .T. ) ;
#7300=DIRECTION ( 'NONE',  ( 0.000000000000000000, 0.000000000000000000, 1.000000000000000000 ) ) ;
#7301=ORIENTED_EDGE ( 'NONE', *, *, #17537, .F. ) ;
#7305=EDGE_LOOP ( 'NONE', ( #3253, #16436, #15370, #20735 ) ) ;
#7306=DIRECTION ( 'NONE',  ( -1.000000000000000000, -0.000000000000000000, -0.000000000000000000 ) ) ;
#7307=ORIENTED_EDGE ( 'NONE', *, *, #6478, .F. ) ;
#7308=DIRECTION ( 'NONE',  ( 1.000000000000000000, 0.000000000000000000, -0.000000000000000000 ) ) ;
#7310=ORIENTED_EDGE ( 'NONE', *, *, #13385, .T. ) ;
#7313=CIRCLE ( 'NONE', #1903, 27.60000000002760245 ) ;
#7315=CIRCLE ( 'NONE', #4288, 65.24900000006525147 ) ;
#7317=CIRCLE ( 'NONE', #18549, 72.00000000007199219 ) ;
#7320=DIRECTION ( 'NONE',  ( 1.000000000000000000, 0.000000000000000000, -0.000000000000000000 ) ) ;
#7321=CYLINDRICAL_SURFACE ( 'NONE', #2722, 27.60000000002759535 ) ;
#7323=DIRECTION ( 'NONE',  ( 0.000000000000000000, 0.000000000000000000, 1.000000000000000000 ) ) ;
#7328=ORIENTED_EDGE ( 'NONE', *, *, #1872, .F. ) ;
#7333=DIRECTION ( 'NONE',  ( -1.000000000000000000, 0.000000000000000000, -0.000000000000000000 ) ) ;
#7334=VERTEX_POINT ( 'NONE', #10529 ) ;
#7336=DIRECTION ( 'NONE',  ( 0.000000000000000000, 0.000000000000000000, 1.000000000000000000 ) ) ;
#7337=DIRECTION ( 'NONE',  ( 1.000000000000000000, 0.000000000000000000, 0.000000000000000000 ) ) ;
#7338=EDGE_CURVE ( 'NONE', #10026, #5060, #10751, .T. ) ;
#7341=CIRCLE ( 'NONE', #17512, 27.60000000002759890 ) ;
#7345=VECTOR ( 'NONE', #3348, 1000.000000000000000 ) ;
#7359=ORIENTED_EDGE ( 'NONE', *, *, #2330, .F. ) ;
#7362=VERTEX_POINT ( 'NONE', #20486 ) ;
#7363=DIRECTION ( 'NONE',  ( -1.000000000000000000, -0.000000000000000000, 0.000000000000000000 ) ) ;
#7364=EDGE_CURVE ( 'NONE', #3116, #15567, #17158, .T. ) ;
#7365=ORIENTED_EDGE ( 'NONE', *, *, #9843, .T. ) ;
#7367=CARTESIAN_POINT ( 'NONE',  ( 19.99999999999999645, 1.971042061628357933, 64.80882494896107460 ) ) ;
#7368=EDGE_CURVE ( 'NONE', #7828, #9385, #1963, .T. ) ;
#7371=ORIENTED_EDGE ( 'NONE', *, *, #16216, .F. ) ;
#7375=CARTESIAN_POINT ( 'NONE',  ( 9.999999999999998224, 0.9548212943365428362, 71.99366858485716136 ) ) ;
#7377=CARTESIAN_POINT ( 'NONE',  ( 19.99999999999999645, 0.000000000000000000, 0.000000000000000000 ) ) ;
#7378=CARTESIAN_POINT ( 'NONE',  ( 19.99999999999999645, 0.000000000000000000, 0.000000000000000000 ) ) ;
#7379=EDGE_LOOP ( 'NONE', ( #7167, #1017, #16050, #3409 ) ) ;
#7382=ORIENTED_EDGE ( 'NONE', *, *, #19816, .F. ) ;
#7385=CARTESIAN_POINT ( 'NONE',  ( 19.99999999999999645, -49.77519642624036322, 42.18840861821767163 ) ) ;
#7387=ORIENTED_EDGE ( 'NONE', *, *, #4642, .F. ) ;
#7388=ORIENTED_EDGE ( 'NONE', *, *, #20685, .T. ) ;
#7390=ADVANCED_FACE ( 'NONE', ( #15404 ), #1109, .T. ) ;
#7393=CARTESIAN_POINT ( 'NONE',  ( 0.000000000000000000, -10.74906464462166866, 71.19310085447965264 ) ) ;
#7397=EDGE_CURVE ( 'NONE', #1369, #10946, #20231, .T. ) ;
#7399=ADVANCED_FACE ( 'NONE', ( #12543 ), #7443, .T. ) ;
#7410=ORIENTED_EDGE ( 'NONE', *, *, #3170, .T. ) ;
#7412=CARTESIAN_POINT ( 'NONE',  ( -10.00000000000000000, 0.000000000000000000, 0.000000000000000000 ) ) ;
#7413=ORIENTED_EDGE ( 'NONE', *, *, #9840, .F. ) ;
#7415=DIRECTION ( 'NONE',  ( 0.000000000000000000, 0.000000000000000000, 1.000000000000000000 ) ) ;
#7424=CARTESIAN_POINT ( 'NONE',  ( 19.99999999999999645, 45.48683723007275148, -46.78012013466171481 ) ) ;
#7431=ORIENTED_EDGE ( 'NONE', *, *, #2294, .F. ) ;
#7436=CARTESIAN_POINT ( 'NONE',  ( 19.99999999999999645, 59.31169354540738681, 27.19476070466876649 ) ) ;
#7437=ORIENTED_EDGE ( 'NONE', *, *, #16966, .T. ) ;
#7439=CYLINDRICAL_SURFACE ( 'NONE', #16150, 27.60000000002759535 ) ;
#7440=CARTESIAN_POINT ( 'NONE',  ( 19.99999999999999645, -35.35772184876915958, 54.34979580218180928 ) ) ;
#7443=CYLINDRICAL_SURFACE ( 'NONE', #11110, 27.60000000002759890 ) ;
#7447=VECTOR ( 'NONE', #16997, 1000.000000000000000 ) ;
#7452=ORIENTED_EDGE ( 'NONE', *, *, #7287, .T. ) ;
#7455=VERTEX_POINT ( 'NONE', #2007 ) ;
#7457=DIRECTION ( 'NONE',  ( -1.000000000000000000, 0.000000000000000000, 0.000000000000000000 ) ) ;
#7459=ORIENTED_EDGE ( 'NONE', *, *, #1796, .F. ) ;
#7466=AXIS2_PLACEMENT_3D ( 'NONE', #6062, #6379, #15713 ) ;
#7467=CARTESIAN_POINT ( 'NONE',  ( 19.99999999999999645, -63.17103598352115057, -16.33561182745204476 ) ) ;
#7469=DIRECTION ( 'NONE',  ( 0.000000000000000000, 0.000000000000000000, -1.000000000000000000 ) ) ;
#7472=VERTEX_POINT ( 'NONE', #14240 ) ;
#7473=ADVANCED_FACE ( 'NONE', ( #18010 ), #20686, .T. ) ;
#7474=DIRECTION ( 'NONE',  ( -1.000000000000000000, -0.000000000000000000, 0.000000000000000000 ) ) ;
#7475=EDGE_LOOP ( 'NONE', ( #18876, #1476, #5638, #13612 ) ) ;
#7476=CARTESIAN_POINT ( 'NONE',  ( 9.999999999999998224, -63.48283426024829623, -33.96954156735433372 ) ) ;
#7477=AXIS2_PLACEMENT_3D ( 'NONE', #13539, #18413, #19893 ) ;
#7483=DIRECTION ( 'NONE',  ( 0.000000000000000000, 0.000000000000000000, 1.000000000000000000 ) ) ;
#7485=VERTEX_POINT ( 'NONE', #1704 ) ;
#7487=DIRECTION ( 'NONE',  ( -1.000000000000000000, 0.000000000000000000, 0.000000000000000000 ) ) ;
#7493=CIRCLE ( 'NONE', #14618, 27.60000000002759890 ) ;
#7496=FACE_OUTER_BOUND ( 'NONE', #19942, .T. ) ;
#7502=LINE ( 'NONE', #5487, #10407 ) ;
#7506=EDGE_CURVE ( 'NONE', #17111, #10885, #13766, .T. ) ;
#7508=CARTESIAN_POINT ( 'NONE',  ( 19.99999999999999645, -71.89099403602351401, -3.960426305689549675 ) ) ;
#7512=AXIS2_PLACEMENT_3D ( 'NONE', #10816, #9118, #15787 ) ;
#7513=ORIENTED_EDGE ( 'NONE', *, *, #15191, .T. ) ;
#7516=CARTESIAN_POINT ( 'NONE',  ( 19.99999999999999645, 45.48683723007212620, 46.78012013466234720 ) ) ;
#7523=VECTOR ( 'NONE', #19998, 1000.000000000000000 ) ;
#7526=LINE ( 'NONE', #14220, #6185 ) ;
#7532=DIRECTION ( 'NONE',  ( -1.000000000000000000, -0.000000000000000000, 0.000000000000000000 ) ) ;
#7540=DIRECTION ( 'NONE',  ( -1.000000000000000000, 0.000000000000000000, 0.000000000000000000 ) ) ;
#7543=AXIS2_PLACEMENT_3D ( 'NONE', #19481, #4966, #4861 ) ;
#7544=DIRECTION ( 'NONE',  ( -1.000000000000000000, -0.000000000000000000, -0.000000000000000000 ) ) ;
#7545=ORIENTED_EDGE ( 'NONE', *, *, #9952, .F. ) ;
#7546=EDGE_CURVE ( 'NONE', #16499, #18514, #7317, .T. ) ;
#7550=ORIENTED_EDGE ( 'NONE', *, *, #9843, .F. ) ;
#7551=CARTESIAN_POINT ( 'NONE',  ( 19.99999999999999645, -51.81019761368347787, 38.98425606966041101 ) ) ;
#7556=AXIS2_PLACEMENT_3D ( 'NONE', #15584, #1079, #14118 ) ;
#7557=CARTESIAN_POINT ( 'NONE',  ( 0.000000000000000000, 0.000000000000000000, 0.000000000000000000 ) ) ;
#7558=AXIS2_PLACEMENT_3D ( 'NONE', #13606, #10650, #5749 ) ;
#7562=ADVANCED_FACE ( 'NONE', ( #1900 ), #5281, .T. ) ;
#7565=ORIENTED_EDGE ( 'NONE', *, *, #14542, .T. ) ;
#7568=ORIENTED_EDGE ( 'NONE', *, *, #15695, .F. ) ;
#7575=CIRCLE ( 'NONE', #11300, 72.00000000007199219 ) ;
#7577=ORIENTED_EDGE ( 'NONE', *, *, #19816, .T. ) ;
#7578=CARTESIAN_POINT ( 'NONE',  ( -10.00000000000000000, 0.000000000000000000, 0.000000000000000000 ) ) ;
#7580=CIRCLE ( 'NONE', #8236, 72.00000000007199219 ) ;
#7582=CIRCLE ( 'NONE', #16383, 27.60000000002759890 ) ;
#7583=ADVANCED_FACE ( 'NONE', ( #6667 ), #6762, .T. ) ;
#7587=AXIS2_PLACEMENT_3D ( 'NONE', #2477, #12014, #18480 ) ;
#7589=VERTEX_POINT ( 'NONE', #13241 ) ;
#7590=CARTESIAN_POINT ( 'NONE',  ( 19.99999999999999645, -58.44960523466222213, -28.06621538408651872 ) ) ;
#7591=ORIENTED_EDGE ( 'NONE', *, *, #13412, .T. ) ;
#7592=CIRCLE ( 'NONE', #10300, 72.00000000007199219 ) ;
#7593=DIRECTION ( 'NONE',  ( 0.000000000000000000, 0.6310879443260539734, -0.7757112907044189098 ) ) ;
#7595=VECTOR ( 'NONE', #7540, 1000.000000000000000 ) ;
#7603=EDGE_CURVE ( 'NONE', #254, #4449, #14779, .T. ) ;
#7607=ORIENTED_EDGE ( 'NONE', *, *, #19855, .T. ) ;
#7609=LINE ( 'NONE', #4220, #8176 ) ;
#7615=ORIENTED_EDGE ( 'NONE', *, *, #20832, .T. ) ;
#7616=CARTESIAN_POINT ( 'NONE',  ( 19.99999999999999645, -46.01927912072559224, 45.67597560296373871 ) ) ;
#7617=DIRECTION ( 'NONE',  ( 0.000000000000000000, 0.000000000000000000, 1.000000000000000000 ) ) ;
#7621=VECTOR ( 'NONE', #19227, 1000.000000000000000 ) ;
#7622=ORIENTED_EDGE ( 'NONE', *, *, #12066, .F. ) ;
#7626=EDGE_LOOP ( 'NONE', ( #20449, #13200, #4691, #10653 ) ) ;
#7627=CARTESIAN_POINT ( 'NONE',  ( 0.000000000000000000, 51.96384592647267908, -49.83732252579563493 ) ) ;
#7628=ORIENTED_EDGE ( 'NONE', *, *, #6830, .F. ) ;
#7632=VERTEX_POINT ( 'NONE', #3584 ) ;
#7634=AXIS2_PLACEMENT_3D ( 'NONE', #7718, #9719, #19567 ) ;
#7636=EDGE_CURVE ( 'NONE', #17663, #1747, #16815, .T. ) ;
#7637=CARTESIAN_POINT ( 'NONE',  ( 0.000000000000000000, 63.48283426024899256, -33.96954156735303343 ) ) ;
#7638=EDGE_CURVE ( 'NONE', #6274, #12091, #3278, .T. ) ;
#7639=AXIS2_PLACEMENT_3D ( 'NONE', #20299, #3796, #17142 ) ;
#7647=FACE_OUTER_BOUND ( 'NONE', #1010, .T. ) ;
#7653=CIRCLE ( 'NONE', #5616, 27.60000000002759890 ) ;
#7654=ORIENTED_EDGE ( 'NONE', *, *, #20226, .F. ) ;
#7658=CARTESIAN_POINT ( 'NONE',  ( 19.99999999999999645, -0.9548212943360466776, -71.99366858485716136 ) ) ;
#7661=AXIS2_PLACEMENT_3D ( 'NONE', #20838, #354, #18163 ) ;
#7662=CARTESIAN_POINT ( 'NONE',  ( 19.99999999999999645, 0.000000000000000000, 0.000000000000000000 ) ) ;
#7663=CARTESIAN_POINT ( 'NONE',  ( 9.999999999999998224, 44.69367065308645692, 56.44887778834763026 ) ) ;
#7665=EDGE_CURVE ( 'NONE', #2235, #3334, #10478, .T. ) ;
#7668=EDGE_CURVE ( 'NONE', #17731, #13498, #10385, .T. ) ;
#7669=DIRECTION ( 'NONE',  ( 0.000000000000000000, -0.2697967711570115057, -0.9629172873478027972 ) ) ;
#7670=ORIENTED_EDGE ( 'NONE', *, *, #1161, .F. ) ;
#7672=AXIS2_PLACEMENT_3D ( 'NONE', #796, #5662, #17118 ) ;
#7673=LINE ( 'NONE', #11070, #5579 ) ;
#7675=ADVANCED_FACE ( 'NONE', ( #3784 ), #10373, .T. ) ;
#7676=DIRECTION ( 'NONE',  ( -1.000000000000000000, -0.000000000000000000, -0.000000000000000000 ) ) ;
#7678=DIRECTION ( 'NONE',  ( -1.000000000000000000, 0.000000000000000000, 0.000000000000000000 ) ) ;
#7679=CARTESIAN_POINT ( 'NONE',  ( 0.000000000000000000, 48.70996102988739551, -42.79495875147724604 ) ) ;
#7686=CARTESIAN_POINT ( 'NONE',  ( 19.99999999999999645, -48.70996102988709708, 42.79495875147758710 ) ) ;
#7687=VECTOR ( 'NONE', #11850, 1000.000000000000000 ) ;
#7690=VECTOR ( 'NONE', #4073, 1000.000000000000000 ) ;
#7695=AXIS2_PLACEMENT_3D ( 'NONE', #13468, #13671, #16738 ) ;
#7697=ADVANCED_FACE ( 'NONE', ( #2317 ), #4221, .T. ) ;
#7701=ORIENTED_EDGE ( 'NONE', *, *, #4494, .T. ) ;
#7704=CARTESIAN_POINT ( 'NONE',  ( 19.99999999999999645, 45.48683723007212620, 46.78012013466234720 ) ) ;
#7705=ORIENTED_EDGE ( 'NONE', *, *, #17169, .T. ) ;
#7709=AXIS2_PLACEMENT_3D ( 'NONE', #18817, #10767, #17228 ) ;
#7712=VERTEX_POINT ( 'NONE', #16730 ) ;
#7716=ORIENTED_EDGE ( 'NONE', *, *, #5865, .T. ) ;
#7718=CARTESIAN_POINT ( 'NONE',  ( 0.000000000000000000, -48.70996102988652154, -42.79495875147824790 ) ) ;
#7729=VERTEX_POINT ( 'NONE', #18540 ) ;
#7730=DIRECTION ( 'NONE',  ( 0.000000000000000000, -0.5195839500354404450, 0.8544194045464844622 ) ) ;
#7733=EDGE_LOOP ( 'NONE', ( #14127, #10474, #9065, #18002 ) ) ;
#7734=DIRECTION ( 'NONE',  ( 0.000000000000000000, 0.000000000000000000, 1.000000000000000000 ) ) ;
#7738=CARTESIAN_POINT ( 'NONE',  ( 19.99999999999999645, -64.44931368725528387, 10.18420179740584608 ) ) ;
#7739=ORIENTED_EDGE ( 'NONE', *, *, #5210, .F. ) ;
#7741=DIRECTION ( 'NONE',  ( -1.000000000000000000, 0.000000000000000000, 0.000000000000000000 ) ) ;
#7744=ORIENTED_EDGE ( 'NONE', *, *, #20074, .F. ) ;
#7746=FACE_OUTER_BOUND ( 'NONE', #20510, .T. ) ;
#7750=ADVANCED_FACE ( 'NONE', ( #2209 ), #15239, .T. ) ;
#7754=ORIENTED_EDGE ( 'NONE', *, *, #16966, .F. ) ;
#7761=CARTESIAN_POINT ( 'NONE',  ( 0.000000000000000000, 42.42902769288603082, -49.02903636734153281 ) ) ;
#7770=DIRECTION ( 'NONE',  ( -1.000000000000000000, 0.000000000000000000, 0.000000000000000000 ) ) ;
#7776=DIRECTION ( 'NONE',  ( -1.000000000000000000, -0.000000000000000000, 0.000000000000000000 ) ) ;
#7778=ADVANCED_FACE ( 'NONE', ( #5695 ), #8991, .T. ) ;
#7779=ORIENTED_EDGE ( 'NONE', *, *, #1446, .F. ) ;
#7786=VERTEX_POINT ( 'NONE', #7393 ) ;
#7789=VERTEX_POINT ( 'NONE', #10799 ) ;
#7790=ADVANCED_FACE ( 'NONE', ( #10999 ), #13979, .T. ) ;
#7792=DIRECTION ( 'NONE',  ( 1.000000000000000000, -0.000000000000000000, -0.000000000000000000 ) ) ;
#7793=AXIS2_PLACEMENT_3D ( 'NONE', #6129, #11008, #12199 ) ;
#7797=DIRECTION ( 'NONE',  ( -1.000000000000000000, -0.000000000000000000, -0.000000000000000000 ) ) ;
#7801=LINE ( 'NONE', #9497, #2414 ) ;
#7802=DIRECTION ( 'NONE',  ( 0.000000000000000000, 0.000000000000000000, 1.000000000000000000 ) ) ;
#7803=EDGE_CURVE ( 'NONE', #19780, #14868, #8180, .T. ) ;
#7804=ORIENTED_EDGE ( 'NONE', *, *, #10571, .F. ) ;
#7806=DIRECTION ( 'NONE',  ( -1.000000000000000000, -0.000000000000000000, 0.000000000000000000 ) ) ;
#7811=CARTESIAN_POINT ( 'NONE',  ( 0.000000000000000000, 67.51707036274413554, 25.00890260772400708 ) ) ;
#7814=ORIENTED_EDGE ( 'NONE', *, *, #5389, .T. ) ;
#7822=AXIS2_PLACEMENT_3D ( 'NONE', #16952, #2435, #15790 ) ;
#7827=CARTESIAN_POINT ( 'NONE',  ( 19.99999999999999645, 54.08351995568706627, 35.76369202524519864 ) ) ;
#7828=VERTEX_POINT ( 'NONE', #1162 ) ;
#7829=CARTESIAN_POINT ( 'NONE',  ( 0.000000000000000000, 0.000000000000000000, 0.000000000000000000 ) ) ;
#7833=AXIS2_PLACEMENT_3D ( 'NONE', #2320, #7182, #20003 ) ;
#7837=DIRECTION ( 'NONE',  ( 0.000000000000000000, -0.1361666490962539222, 0.9906859460363298675 ) ) ;
#7840=AXIS2_PLACEMENT_3D ( 'NONE', #19792, #7279, #13759 ) ;
#7843=EDGE_CURVE ( 'NONE', #2697, #17420, #2095, .T. ) ;
#7845=AXIS2_PLACEMENT_3D ( 'NONE', #6024, #13767, #15551 ) ;
#7854=CARTESIAN_POINT ( 'NONE',  ( 19.99999999999999645, 20.60847369612982405, 61.90898814327722732 ) ) ;
#7856=ORIENTED_EDGE ( 'NONE', *, *, #2345, .F. ) ;
#7862=DIRECTION ( 'NONE',  ( 0.000000000000000000, 0.000000000000000000, 1.000000000000000000 ) ) ;
#7863=ORIENTED_EDGE ( 'NONE', *, *, #19224, .T. ) ;
#7864=DIRECTION ( 'NONE',  ( -1.000000000000000000, 0.000000000000000000, -0.000000000000000000 ) ) ;
#7868=DIRECTION ( 'NONE',  ( -1.000000000000000000, 0.000000000000000000, -0.000000000000000000 ) ) ;
#7869=AXIS2_PLACEMENT_3D ( 'NONE', #2734, #2416, #15351 ) ;
#7881=CARTESIAN_POINT ( 'NONE',  ( 19.99999999999999645, -46.01927912072495275, -45.67597560296436399 ) ) ;
#7882=CIRCLE ( 'NONE', #20041, 65.24900000006525147 ) ;
#7883=CIRCLE ( 'NONE', #16010, 27.60000000002759890 ) ;
#7887=DIRECTION ( 'NONE',  ( -1.000000000000000000, 0.000000000000000000, -0.000000000000000000 ) ) ;
#7891=DIRECTION ( 'NONE',  ( 0.000000000000000000, -0.5195839500354404450, 0.8544194045464843512 ) ) ;
#7894=ORIENTED_EDGE ( 'NONE', *, *, #5592, .F. ) ;
#7895=VECTOR ( 'NONE', #19928, 1000.000000000000000 ) ;
#7903=EDGE_CURVE ( 'NONE', #20609, #125, #20007, .T. ) ;
#7904=ORIENTED_EDGE ( 'NONE', *, *, #11314, .T. ) ;
#7905=CYLINDRICAL_SURFACE ( 'NONE', #15070, 27.60000000002759535 ) ;
#7915=VECTOR ( 'NONE', #6060, 1000.000000000000000 ) ;
#7921=DIRECTION ( 'NONE',  ( 0.000000000000000000, 0.000000000000000000, 1.000000000000000000 ) ) ;
#7925=DIRECTION ( 'NONE',  ( 0.000000000000000000, -0.5195839500354229035, -0.8544194045464950094 ) ) ;
#7927=EDGE_CURVE ( 'NONE', #14524, #11622, #4458, .T. ) ;
#7932=CIRCLE ( 'NONE', #9948, 65.24900000006523726 ) ;
#7939=DIRECTION ( 'NONE',  ( -1.000000000000000000, 0.000000000000000000, 0.000000000000000000 ) ) ;
#7943=LINE ( 'NONE', #11221, #11909 ) ;
#7945=DIRECTION ( 'NONE',  ( -1.000000000000000000, -0.000000000000000000, 0.000000000000000000 ) ) ;
#7946=ORIENTED_EDGE ( 'NONE', *, *, #2872, .T. ) ;
#7951=DIRECTION ( 'NONE',  ( 0.000000000000000000, 0.3984010898462422290, -0.9172113015054527141 ) ) ;
#7952=ORIENTED_EDGE ( 'NONE', *, *, #15009, .T. ) ;
#7961=EDGE_CURVE ( 'NONE', #12996, #9191, #2385, .T. ) ;
#7965=DIRECTION ( 'NONE',  ( 0.000000000000000000, -0.9790840876823249106, 0.2034560130526240906 ) ) ;
#7966=FACE_OUTER_BOUND ( 'NONE', #14045, .T. ) ;
#7968=ORIENTED_EDGE ( 'NONE', *, *, #20864, .T. ) ;
#7972=CARTESIAN_POINT ( 'NONE',  ( 0.000000000000000000, -45.48683723007244595, 46.78012013466202035 ) ) ;
#7976=ORIENTED_EDGE ( 'NONE', *, *, #7299, .F. ) ;
#7980=ORIENTED_EDGE ( 'NONE', *, *, #6615, .T. ) ;
#7981=CARTESIAN_POINT ( 'NONE',  ( 0.000000000000000000, 20.34307325858884141, -69.06634035770285607 ) ) ;
#7987=CARTESIAN_POINT ( 'NONE',  ( 9.999999999999998224, 67.51707036274449081, -25.00890260772307627 ) ) ;
#7991=LINE ( 'NONE', #2800, #3838 ) ;
#7993=VECTOR ( 'NONE', #4318, 1000.000000000000000 ) ;
#7996=CARTESIAN_POINT ( 'NONE',  ( 19.99999999999999645, 63.17103598352149874, -16.33561182745074447 ) ) ;
#7998=CARTESIAN_POINT ( 'NONE',  ( 19.99999999999999645, 0.000000000000000000, 0.000000000000000000 ) ) ;
#8001=ORIENTED_EDGE ( 'NONE', *, *, #10493, .F. ) ;
#8004=CIRCLE ( 'NONE', #19833, 72.00000000007199219 ) ;
#8007=CIRCLE ( 'NONE', #10724, 27.60000000002760601 ) ;
#8008=CARTESIAN_POINT ( 'NONE',  ( 19.99999999999999645, 51.81019761368321497, 38.98425606966075918 ) ) ;
#8010=ORIENTED_EDGE ( 'NONE', *, *, #8959, .F. ) ;
#8013=DIRECTION ( 'NONE',  ( 0.000000000000000000, 0.000000000000000000, 1.000000000000000000 ) ) ;
#8015=CARTESIAN_POINT ( 'NONE',  ( 0.000000000000000000, 0.000000000000000000, 0.000000000000000000 ) ) ;
#8024=CARTESIAN_POINT ( 'NONE',  ( 9.999999999999998224, -29.55812890832026341, 65.65300461859676773 ) ) ;
#8028=FACE_OUTER_BOUND ( 'NONE', #8804, .T. ) ;
#8029=DIRECTION ( 'NONE',  ( 0.000000000000000000, 0.2697967711570182225, 0.9629172873478010208 ) ) ;
#8030=DIRECTION ( 'NONE',  ( -1.000000000000000000, -0.000000000000000000, -0.000000000000000000 ) ) ;
#8032=ORIENTED_EDGE ( 'NONE', *, *, #5592, .T. ) ;
#8035=CARTESIAN_POINT ( 'NONE',  ( 0.000000000000000000, 0.000000000000000000, 0.000000000000000000 ) ) ;
#8039=CIRCLE ( 'NONE', #4666, 27.60000000002759535 ) ;
#8042=CARTESIAN_POINT ( 'NONE',  ( 9.999999999999998224, 27.80658314415319055, -66.41380830714092554 ) ) ;
#8048=DIRECTION ( 'NONE',  ( 0.000000000000000000, -0.9790840876823205807, -0.2034560130526446575 ) ) ;
#8051=CYLINDRICAL_SURFACE ( 'NONE', #9046, 27.60000000002760245 ) ;
#8052=ORIENTED_EDGE ( 'NONE', *, *, #15416, .F. ) ;
#8053=EDGE_CURVE ( 'NONE', #9946, #645, #58, .T. ) ;
#8059=ADVANCED_FACE ( 'NONE', ( #17650 ), #20924, .T. ) ;
#8062=CARTESIAN_POINT ( 'NONE',  ( 0.000000000000000000, 0.000000000000000000, 0.000000000000000000 ) ) ;
#8063=ADVANCED_FACE ( 'NONE', ( #17336 ), #4611, .T. ) ;
#8072=DIRECTION ( 'NONE',  ( -1.000000000000000000, 0.000000000000000000, 0.000000000000000000 ) ) ;
#8073=DIRECTION ( 'NONE',  ( 0.000000000000000000, 0.000000000000000000, 1.000000000000000000 ) ) ;
#8074=EDGE_CURVE ( 'NONE', #4217, #18949, #3437, .T. ) ;
#8075=ORIENTED_EDGE ( 'NONE', *, *, #20744, .F. ) ;
#8077=VERTEX_POINT ( 'NONE', #14375 ) ;
#8080=VERTEX_POINT ( 'NONE', #6194 ) ;
#8090=FACE_OUTER_BOUND ( 'NONE', #20009, .T. ) ;
#8095=DIRECTION ( 'NONE',  ( 0.000000000000000000, 0.000000000000000000, -1.000000000000000000 ) ) ;
#8099=DIRECTION ( 'NONE',  ( 0.000000000000000000, -0.3984010898462296835, -0.9172113015054581542 ) ) ;
#8101=DIRECTION ( 'NONE',  ( 0.000000000000000000, 0.8878852184023731109, 0.4600650377311562012 ) ) ;
#8108=EDGE_CURVE ( 'NONE', #19446, #16924, #20708, .T. ) ;
#8114=ORIENTED_EDGE ( 'NONE', *, *, #11936, .T. ) ;
#8117=DIRECTION ( 'NONE',  ( -1.000000000000000000, 0.000000000000000000, 0.000000000000000000 ) ) ;
#8118=CIRCLE ( 'NONE', #326, 27.60000000002759180 ) ;
#8119=ORIENTED_EDGE ( 'NONE', *, *, #12338, .T. ) ;
#8122=DIRECTION ( 'NONE',  ( 0.000000000000000000, -0.8169698930104469792, 0.5766803221148600889 ) ) ;
#8127=EDGE_CURVE ( 'NONE', #1793, #19110, #19140, .T. ) ;
#8128=LINE ( 'NONE', #14601, #3451 ) ;
#8131=ORIENTED_EDGE ( 'NONE', *, *, #2354, .F. ) ;
#8132=AXIS2_PLACEMENT_3D ( 'NONE', #10851, #15836, #1331 ) ;
#8133=DIRECTION ( 'NONE',  ( 0.000000000000000000, 0.000000000000000000, 1.000000000000000000 ) ) ;
#8136=CARTESIAN_POINT ( 'NONE',  ( -10.00000000000000000, 0.000000000000000000, 0.000000000000000000 ) ) ;
#8138=EDGE_LOOP ( 'NONE', ( #8537, #14214, #15435, #14509 ) ) ;
#8139=FACE_OUTER_BOUND ( 'NONE', #18382, .T. ) ;
#8142=ORIENTED_EDGE ( 'NONE', *, *, #19706, .F. ) ;
#8143=CARTESIAN_POINT ( 'NONE',  ( 19.99999999999999645, -55.05624179291956466, -35.01774179823839717 ) ) ;
#8148=ORIENTED_EDGE ( 'NONE', *, *, #4230, .F. ) ;
#8149=ORIENTED_EDGE ( 'NONE', *, *, #1632, .F. ) ;
#8154=DIRECTION ( 'NONE',  ( -1.000000000000000000, 0.000000000000000000, 0.000000000000000000 ) ) ;
#8155=CARTESIAN_POINT ( 'NONE',  ( -10.00000000000000000, 0.000000000000000000, 0.000000000000000000 ) ) ;
#8159=ADVANCED_FACE ( 'NONE', ( #1130 ), #9388, .T. ) ;
#8161=DIRECTION ( 'NONE',  ( -1.000000000000000000, 0.000000000000000000, -0.000000000000000000 ) ) ;
#8165=DIRECTION ( 'NONE',  ( 1.000000000000000000, 0.000000000000000000, 0.000000000000000000 ) ) ;
#8167=CYLINDRICAL_SURFACE ( 'NONE', #11991, 27.60000000002759890 ) ;
#8168=AXIS2_PLACEMENT_3D ( 'NONE', #17071, #15259, #6993 ) ;
#8173=LINE ( 'NONE', #13792, #723 ) ;
#8175=ORIENTED_EDGE ( 'NONE', *, *, #17652, .T. ) ;
#8176=VECTOR ( 'NONE', #9101, 1000.000000000000000 ) ;
#8180=CIRCLE ( 'NONE', #9197, 72.00000000007199219 ) ;
#8183=AXIS2_PLACEMENT_3D ( 'NONE', #15545, #7487, #14191 ) ;
#8185=EDGE_CURVE ( 'NONE', #1607, #12002, #1774, .T. ) ;
#8186=CARTESIAN_POINT ( 'NONE',  ( 19.99999999999999645, 42.42902769288603082, -49.02903636734153281 ) ) ;
#8189=CIRCLE ( 'NONE', #15632, 65.24900000006525147 ) ;
#8190=CARTESIAN_POINT ( 'NONE',  ( 9.999999999999998224, 70.29359119158506530, -15.58239511117214704 ) ) ;
#8191=LINE ( 'NONE', #2453, #2509 ) ;
#8194=EDGE_CURVE ( 'NONE', #5437, #8657, #310, .T. ) ;
#8196=CARTESIAN_POINT ( 'NONE',  ( 19.99999999999999645, -1.971042061628798470, 64.80882494896106039 ) ) ;
#8199=ORIENTED_EDGE ( 'NONE', *, *, #19482, .T. ) ;
#8200=DIRECTION ( 'NONE',  ( -1.000000000000000000, 0.000000000000000000, 0.000000000000000000 ) ) ;
#8201=VERTEX_POINT ( 'NONE', #3686 ) ;
#8202=DIRECTION ( 'NONE',  ( 0.000000000000000000, 0.000000000000000000, 1.000000000000000000 ) ) ;
#8204=LINE ( 'NONE', #11805, #14342 ) ;
#8207=AXIS2_PLACEMENT_3D ( 'NONE', #12679, #17231, #15739 ) ;
#8210=EDGE_CURVE ( 'NONE', #14524, #7039, #16145, .T. ) ;
#8214=CARTESIAN_POINT ( 'NONE',  ( 19.99999999999999645, 49.77519642624064744, -42.18840861821734478 ) ) ;
#8218=CIRCLE ( 'NONE', #10643, 27.60000000002759890 ) ;
#8219=VERTEX_POINT ( 'NONE', #6763 ) ;
#8224=AXIS2_PLACEMENT_3D ( 'NONE', #14058, #255, #11280 ) ;
#8225=CARTESIAN_POINT ( 'NONE',  ( 19.99999999999999645, 59.36728637278074672, -40.73727173906726051 ) ) ;
#8227=VERTEX_POINT ( 'NONE', #5482 ) ;
#8231=AXIS2_PLACEMENT_3D ( 'NONE', #6042, #20564, #17498 ) ;
#8236=AXIS2_PLACEMENT_3D ( 'NONE', #13691, #16651, #8909 ) ;
#8243=DIRECTION ( 'NONE',  ( -1.000000000000000000, 0.000000000000000000, 0.000000000000000000 ) ) ;
#8247=CIRCLE ( 'NONE', #17046, 27.60000000002759890 ) ;
#8250=DIRECTION ( 'NONE',  ( -1.000000000000000000, 0.000000000000000000, 0.000000000000000000 ) ) ;
#8252=ORIENTED_EDGE ( 'NONE', *, *, #17325, .F. ) ;
#8254=CYLINDRICAL_SURFACE ( 'NONE', #5991, 27.60000000002759535 ) ;
#8255=AXIS2_PLACEMENT_3D ( 'NONE', #6788, #13273, #16547 ) ;
#8257=DIRECTION ( 'NONE',  ( 0.000000000000000000, 0.8169698930104392076, 0.5766803221148710801 ) ) ;
#8259=CARTESIAN_POINT ( 'NONE',  ( 0.000000000000000000, -14.55863677812078016, -63.60407295269120453 ) ) ;
#8266=FACE_OUTER_BOUND ( 'NONE', #17954, .T. ) ;
#8267=CIRCLE ( 'NONE', #10301, 7.500000000000000000 ) ;
#8269=DIRECTION ( 'NONE',  ( 0.000000000000000000, 0.000000000000000000, 1.000000000000000000 ) ) ;
#8276=DIRECTION ( 'NONE',  ( -1.000000000000000000, -0.000000000000000000, 0.000000000000000000 ) ) ;
#8277=ORIENTED_EDGE ( 'NONE', *, *, #4688, .F. ) ;
#8279=DIRECTION ( 'NONE',  ( -1.000000000000000000, 0.000000000000000000, 0.000000000000000000 ) ) ;
#8282=AXIS2_PLACEMENT_3D ( 'NONE', #16068, #17053, #18638 ) ;
#8283=LINE ( 'NONE', #6386, #11624 ) ;
#8286=ORIENTED_EDGE ( 'NONE', *, *, #6822, .T. ) ;
#8289=CARTESIAN_POINT ( 'NONE',  ( -10.00000000000000000, 0.000000000000000000, 0.000000000000000000 ) ) ;
#8292=CARTESIAN_POINT ( 'NONE',  ( 19.99999999999999645, 49.77519642624064744, -42.18840861821734478 ) ) ;
#8293=ORIENTED_EDGE ( 'NONE', *, *, #3492, .T. ) ;
#8297=CARTESIAN_POINT ( 'NONE',  ( 19.99999999999999645, -65.23577793412346182, 1.313498510941474740 ) ) ;
#8300=ORIENTED_EDGE ( 'NONE', *, *, #4818, .T. ) ;
#8301=VECTOR ( 'NONE', #4379, 1000.000000000000000 ) ;
#8305=EDGE_CURVE ( 'NONE', #11056, #19208, #19037, .T. ) ;
#8307=CIRCLE ( 'NONE', #13735, 27.60000000002759890 ) ;
#8308=ADVANCED_FACE ( 'NONE', ( #19906 ), #20437, .T. ) ;
#8311=ORIENTED_EDGE ( 'NONE', *, *, #15439, .F. ) ;
#8312=AXIS2_PLACEMENT_3D ( 'NONE', #16422, #19503, #6264 ) ;
#8313=CARTESIAN_POINT ( 'NONE',  ( 0.000000000000000000, 56.63599015375672963, 31.56633360682482703 ) ) ;
#8315=ORIENTED_EDGE ( 'NONE', *, *, #15312, .F. ) ;
#8316=CARTESIAN_POINT ( 'NONE',  ( 19.99999999999999645, -70.29359119158495162, 15.58239511117263554 ) ) ;
#8318=DIRECTION ( 'NONE',  ( -1.000000000000000000, -0.000000000000000000, 0.000000000000000000 ) ) ;
#8319=CARTESIAN_POINT ( 'NONE',  ( 0.000000000000000000, 51.81019761368321497, 38.98425606966075918 ) ) ;
#8321=EDGE_CURVE ( 'NONE', #19744, #13592, #722, .T. ) ;
#8322=EDGE_CURVE ( 'NONE', #8201, #13929, #11583, .T. ) ;
#8323=ORIENTED_EDGE ( 'NONE', *, *, #17713, .F. ) ;
#8328=AXIS2_PLACEMENT_3D ( 'NONE', #8319, #18278, #9910 ) ;
#8331=ORIENTED_EDGE ( 'NONE', *, *, #15673, .T. ) ;
#8334=CYLINDRICAL_SURFACE ( 'NONE', #2814, 27.60000000002759535 ) ;
#8339=AXIS2_PLACEMENT_3D ( 'NONE', #15348, #15040, #16613 ) ;
#8340=DIRECTION ( 'NONE',  ( -1.000000000000000000, 0.000000000000000000, 0.000000000000000000 ) ) ;
#8342=VECTOR ( 'NONE', #1693, 1000.000000000000000 ) ;
#8347=DIRECTION ( 'NONE',  ( 0.000000000000000000, 0.000000000000000000, 1.000000000000000000 ) ) ;
#8349=CARTESIAN_POINT ( 'NONE',  ( 19.99999999999999645, 43.56693332842851873, -48.57318520917461058 ) ) ;
#8351=ORIENTED_EDGE ( 'NONE', *, *, #14218, .T. ) ;
#8352=CARTESIAN_POINT ( 'NONE',  ( 0.000000000000000000, 0.000000000000000000, 0.000000000000000000 ) ) ;
#8356=AXIS2_PLACEMENT_3D ( 'NONE', #6530, #16088, #7925 ) ;
#8357=VERTEX_POINT ( 'NONE', #15240 ) ;
#8359=CARTESIAN_POINT ( 'NONE',  ( 19.99999999999999645, 0.000000000000000000, 0.000000000000000000 ) ) ;
#8361=CIRCLE ( 'NONE', #9055, 72.00000000007199219 ) ;
#8362=CARTESIAN_POINT ( 'NONE',  ( 19.99999999999999645, -64.79224928664389438, -2.456263514198281150 ) ) ;
#8363=CARTESIAN_POINT ( 'NONE',  ( 9.999999999999998224, 44.69367065308723141, -56.44887778834701919 ) ) ;
#8366=UNCERTAINTY_MEASURE_WITH_UNIT (LENGTH_MEASURE( 1.000000000000000082E-05 ), #2274, 'distance_accuracy_value', 'NONE');
#8370=CIRCLE ( 'NONE', #15472, 72.00000000007199219 ) ;
#8373=CYLINDRICAL_SURFACE ( 'NONE', #11051, 27.60000000002759890 ) ;
#8374=ORIENTED_EDGE ( 'NONE', *, *, #9135, .T. ) ;
#8379=CARTESIAN_POINT ( 'NONE',  ( 9.999999999999998224, -64.36139404985944168, -32.27399814043940296 ) ) ;
#8383=VERTEX_POINT ( 'NONE', #3893 ) ;
#8387=DIRECTION ( 'NONE',  ( 1.000000000000000000, -0.000000000000000000, 0.000000000000000000 ) ) ;
#8388=EDGE_CURVE ( 'NONE', #4471, #5326, #10699, .T. ) ;
#8389=CYLINDRICAL_SURFACE ( 'NONE', #8255, 65.24900000006525147 ) ;
#8396=EDGE_CURVE ( 'NONE', #15688, #15450, #6169, .T. ) ;
#8398=DIRECTION ( 'NONE',  ( -1.000000000000000000, -0.000000000000000000, -0.000000000000000000 ) ) ;
#8402=ORIENTED_EDGE ( 'NONE', *, *, #6712, .F. ) ;
#8405=DIRECTION ( 'NONE',  ( -1.000000000000000000, -0.000000000000000000, -0.000000000000000000 ) ) ;
#8406=DIRECTION ( 'NONE',  ( -1.000000000000000000, 0.000000000000000000, -0.000000000000000000 ) ) ;
#8408=FACE_OUTER_BOUND ( 'NONE', #7086, .T. ) ;
#8409=CARTESIAN_POINT ( 'NONE',  ( 19.99999999999999645, 0.000000000000000000, 0.000000000000000000 ) ) ;
#8421=DIRECTION ( 'NONE',  ( -1.000000000000000000, 0.000000000000000000, 0.000000000000000000 ) ) ;
#8426=ORIENTED_EDGE ( 'NONE', *, *, #18463, .T. ) ;
#8427=CARTESIAN_POINT ( 'NONE',  ( 19.99999999999999645, 0.000000000000000000, 0.000000000000000000 ) ) ;
#8428=EDGE_LOOP ( 'NONE', ( #13307, #3952, #19825, #4639 ) ) ;
#8429=CARTESIAN_POINT ( 'NONE',  ( 19.99999999999999645, 6.872116855663142232, 64.47358224882421496 ) ) ;
#8430=CARTESIAN_POINT ( 'NONE',  ( 19.99999999999999645, -38.22257254261699444, -61.01667762370177428 ) ) ;
#8434=ORIENTED_EDGE ( 'NONE', *, *, #175, .F. ) ;
#8435=CARTESIAN_POINT ( 'NONE',  ( 19.99999999999999645, -38.69327817041739337, -52.53819777490673459 ) ) ;
#8436=VERTEX_POINT ( 'NONE', #18636 ) ;
#8438=EDGE_CURVE ( 'NONE', #14260, #19110, #14089, .T. ) ;
#8441=EDGE_CURVE ( 'NONE', #14303, #19485, #16935, .T. ) ;
#8449=DIRECTION ( 'NONE',  ( 0.000000000000000000, 0.000000000000000000, 1.000000000000000000 ) ) ;
#8453=ORIENTED_EDGE ( 'NONE', *, *, #14459, .F. ) ;
#8459=ADVANCED_FACE ( 'NONE', ( #7496 ), #7179, .T. ) ;
#8463=CARTESIAN_POINT ( 'NONE',  ( 19.99999999999999645, 0.000000000000000000, 0.000000000000000000 ) ) ;
#8464=CARTESIAN_POINT ( 'NONE',  ( 19.99999999999999645, -44.69367065308607323, -56.44887778834792158 ) ) ;
#8469=DIRECTION ( 'NONE',  ( -1.000000000000000000, 0.000000000000000000, 0.000000000000000000 ) ) ;
#8470=VERTEX_POINT ( 'NONE', #10585 ) ;
#8476=EDGE_CURVE ( 'NONE', #20364, #11776, #752, .T. ) ;
#8478=CIRCLE ( 'NONE', #19983, 72.00000000007199219 ) ;
#8481=CARTESIAN_POINT ( 'NONE',  ( 19.99999999999999645, -64.79224928664393701, 2.456263514197400077 ) ) ;
#8482=DIRECTION ( 'NONE',  ( 0.000000000000000000, 0.000000000000000000, 1.000000000000000000 ) ) ;
#8486=DIRECTION ( 'NONE',  ( -1.000000000000000000, 0.000000000000000000, 0.000000000000000000 ) ) ;
#8487=LINE ( 'NONE', #11378, #14709 ) ;
#8488=DIRECTION ( 'NONE',  ( 0.000000000000000000, 0.000000000000000000, 1.000000000000000000 ) ) ;
#8492=DIRECTION ( 'NONE',  ( -1.000000000000000000, 0.000000000000000000, 0.000000000000000000 ) ) ;
#8496=EDGE_CURVE ( 'NONE', #17681, #15210, #17343, .T. ) ;
#8499=CARTESIAN_POINT ( 'NONE',  ( 19.99999999999999645, -64.79224928664393701, 2.456263514197400077 ) ) ;
#8502=ORIENTED_EDGE ( 'NONE', *, *, #4511, .F. ) ;
#8503=CIRCLE ( 'NONE', #18038, 65.24900000006526568 ) ;
#8505=CIRCLE ( 'NONE', #7840, 7.500000000000000000 ) ;
#8506=CARTESIAN_POINT ( 'NONE',  ( 0.000000000000000000, 0.9548212943375558037, -71.99366858485714715 ) ) ;
#8513=LINE ( 'NONE', #18179, #3407 ) ;
#8515=AXIS2_PLACEMENT_3D ( 'NONE', #20436, #20738, #6025 ) ;
#8516=DIRECTION ( 'NONE',  ( 0.000000000000000000, 0.000000000000000000, 1.000000000000000000 ) ) ;
#8528=AXIS2_PLACEMENT_3D ( 'NONE', #6334, #16090, #3052 ) ;
#8532=EDGE_CURVE ( 'NONE', #11409, #10935, #2113, .T. ) ;
#8534=AXIS2_PLACEMENT_3D ( 'NONE', #9745, #16208, #2310 ) ;
#8535=SHAPE_DEFINITION_REPRESENTATION ( #7115, #13064 ) ;
#8537=ORIENTED_EDGE ( 'NONE', *, *, #9240, .F. ) ;
#8538=DIRECTION ( 'NONE',  ( -1.000000000000000000, 0.000000000000000000, 0.000000000000000000 ) ) ;
#8539=VECTOR ( 'NONE', #8538, 1000.000000000000000 ) ;
#8540=EDGE_CURVE ( 'NONE', #10147, #12530, #6026, .T. ) ;
#8545=AXIS2_PLACEMENT_3D ( 'NONE', #4754, #9642, #8048 ) ;
#8546=ORIENTED_EDGE ( 'NONE', *, *, #12672, .T. ) ;
#8550=CIRCLE ( 'NONE', #2135, 27.60000000002759535 ) ;
#8553=DIRECTION ( 'NONE',  ( -1.000000000000000000, 0.000000000000000000, 0.000000000000000000 ) ) ;
#8560=AXIS2_PLACEMENT_3D ( 'NONE', #12631, #11134, #3076 ) ;
#8562=ADVANCED_FACE ( 'NONE', ( #9626 ), #19164, .T. ) ;
#8570=EDGE_CURVE ( 'NONE', #1429, #12585, #12962, .T. ) ;
#8578=EDGE_LOOP ( 'NONE', ( #5739, #4623, #6997, #502 ) ) ;
#8582=EDGE_CURVE ( 'NONE', #7729, #4144, #8128, .T. ) ;
#8583=ORIENTED_EDGE ( 'NONE', *, *, #2989, .T. ) ;
#8584=EDGE_CURVE ( 'NONE', #6966, #7729, #5829, .T. ) ;
#8588=DIRECTION ( 'NONE',  ( 0.000000000000000000, 0.000000000000000000, 1.000000000000000000 ) ) ;
#8590=ORIENTED_EDGE ( 'NONE', *, *, #12846, .T. ) ;
#8591=ORIENTED_EDGE ( 'NONE', *, *, #14818, .T. ) ;
#8593=EDGE_CURVE ( 'NONE', #14998, #281, #17693, .T. ) ;
#8596=DIRECTION ( 'NONE',  ( 0.000000000000000000, -0.9422609221188167350, -0.3348796121709969875 ) ) ;
#8597=AXIS2_PLACEMENT_3D ( 'NONE', #16154, #20914, #6793 ) ;
#8603=DIRECTION ( 'NONE',  ( -1.000000000000000000, 0.000000000000000000, 0.000000000000000000 ) ) ;
#8604=VERTEX_POINT ( 'NONE', #6428 ) ;
#8606=ORIENTED_EDGE ( 'NONE', *, *, #20737, .F. ) ;
#8611=ORIENTED_EDGE ( 'NONE', *, *, #19095, .T. ) ;
#8613=DIRECTION ( 'NONE',  ( 0.000000000000000000, 0.000000000000000000, 1.000000000000000000 ) ) ;
#8614=ORIENTED_EDGE ( 'NONE', *, *, #10669, .F. ) ;
#8620=CARTESIAN_POINT ( 'NONE',  ( 9.999999999999998224, 71.89099403602354244, 3.960426305689050075 ) ) ;
#8622=ORIENTED_EDGE ( 'NONE', *, *, #5367, .T. ) ;
#8623=LINE ( 'NONE', #18073, #7262 ) ;
#8624=EDGE_CURVE ( 'NONE', #1644, #10081, #4849, .T. ) ;
#8626=VERTEX_POINT ( 'NONE', #2842 ) ;
#8629=VERTEX_POINT ( 'NONE', #6118 ) ;
#8631=CYLINDRICAL_SURFACE ( 'NONE', #9731, 27.60000000002759890 ) ;
#8634=ORIENTED_EDGE ( 'NONE', *, *, #12491, .F. ) ;
#8635=DIRECTION ( 'NONE',  ( -1.000000000000000000, 0.000000000000000000, -0.000000000000000000 ) ) ;
#8636=AXIS2_PLACEMENT_3D ( 'NONE', #14399, #3251, #1676 ) ;
#8638=CARTESIAN_POINT ( 'NONE',  ( 19.99999999999999645, 0.000000000000000000, 0.000000000000000000 ) ) ;
#8640=( GEOMETRIC_REPRESENTATION_CONTEXT ( 3 ) GLOBAL_UNCERTAINTY_ASSIGNED_CONTEXT ( ( #8366 ) ) GLOBAL_UNIT_ASSIGNED_CONTEXT ( ( #2274, #5652, #15613 ) ) REPRESENTATION_CONTEXT ( 'NONE', 'WORKASPACE' ) );
#8649=AXIS2_PLACEMENT_3D ( 'NONE', #5858, #15605, #377 ) ;
#8650=DIRECTION ( 'NONE',  ( -1.000000000000000000, -0.000000000000000000, 0.000000000000000000 ) ) ;
#8652=CIRCLE ( 'NONE', #3969, 65.24900000006525147 ) ;
#8657=VERTEX_POINT ( 'NONE', #17685 ) ;
#8659=ORIENTED_EDGE ( 'NONE', *, *, #7603, .T. ) ;
#8663=AXIS2_PLACEMENT_3D ( 'NONE', #4087, #4736, #11696 ) ;
#8665=ORIENTED_EDGE ( 'NONE', *, *, #8053, .T. ) ;
#8666=DIRECTION ( 'NONE',  ( 0.000000000000000000, 0.000000000000000000, 1.000000000000000000 ) ) ;
#8668=DIRECTION ( 'NONE',  ( 0.000000000000000000, 0.000000000000000000, 1.000000000000000000 ) ) ;
#8670=AXIS2_PLACEMENT_3D ( 'NONE', #4808, #11079, #9273 ) ;
#8677=VECTOR ( 'NONE', #11667, 1000.000000000000000 ) ;
#8683=CIRCLE ( 'NONE', #9367, 72.00000000007199219 ) ;
#8684=EDGE_CURVE ( 'NONE', #1182, #17144, #12283, .T. ) ;
#8686=DIRECTION ( 'NONE',  ( -1.000000000000000000, -0.000000000000000000, -0.000000000000000000 ) ) ;
#8691=DIRECTION ( 'NONE',  ( 0.000000000000000000, 0.000000000000000000, 1.000000000000000000 ) ) ;
#8692=DIRECTION ( 'NONE',  ( -1.000000000000000000, 0.000000000000000000, 0.000000000000000000 ) ) ;
#8694=EDGE_CURVE ( 'NONE', #18360, #10009, #6523, .T. ) ;
#8697=VERTEX_POINT ( 'NONE', #10238 ) ;
#8702=EDGE_CURVE ( 'NONE', #8788, #10906, #13986, .T. ) ;
#8708=DIRECTION ( 'NONE',  ( 1.000000000000000000, -0.000000000000000000, -0.000000000000000000 ) ) ;
#8710=EDGE_CURVE ( 'NONE', #11468, #13959, #6837, .T. ) ;
#8718=EDGE_LOOP ( 'NONE', ( #17413, #13145, #2068, #12130 ) ) ;
#8721=EDGE_CURVE ( 'NONE', #4150, #4451, #18376, .T. ) ;
#8735=VERTEX_POINT ( 'NONE', #6948 ) ;
#8737=ORIENTED_EDGE ( 'NONE', *, *, #3770, .F. ) ;
#8740=CYLINDRICAL_SURFACE ( 'NONE', #227, 27.60000000002759535 ) ;
#8741=VERTEX_POINT ( 'NONE', #8430 ) ;
#8742=CARTESIAN_POINT ( 'NONE',  ( 9.999999999999998224, -29.55812890831937167, -65.65300461859717984 ) ) ;
#8745=ORIENTED_EDGE ( 'NONE', *, *, #4652, .T. ) ;
#8746=CARTESIAN_POINT ( 'NONE',  ( 0.000000000000000000, 0.000000000000000000, 0.000000000000000000 ) ) ;
#8748=ORIENTED_EDGE ( 'NONE', *, *, #11799, .T. ) ;
#8750=DIRECTION ( 'NONE',  ( 0.000000000000000000, -0.9790840876823249106, 0.2034560130526240906 ) ) ;
#8757=CARTESIAN_POINT ( 'NONE',  ( -65.00002539999999840, 0.000000000000000000, 0.000000000000000000 ) ) ;
#8759=DIRECTION ( 'NONE',  ( -1.000000000000000000, -0.000000000000000000, 0.000000000000000000 ) ) ;
#8762=DIRECTION ( 'NONE',  ( -1.000000000000000000, 0.000000000000000000, 0.000000000000000000 ) ) ;
#8766=ADVANCED_FACE ( 'NONE', ( #9818 ), #11828, .T. ) ;
#8768=ORIENTED_EDGE ( 'NONE', *, *, #648, .F. ) ;
#8776=DIRECTION ( 'NONE',  ( 1.000000000000000000, 0.000000000000000000, -0.000000000000000000 ) ) ;
#8778=CARTESIAN_POINT ( 'NONE',  ( 0.000000000000000000, 58.26603306962022089, -42.29739224042413781 ) ) ;
#8782=DIRECTION ( 'NONE',  ( -1.000000000000000000, -0.000000000000000000, -0.000000000000000000 ) ) ;
#8784=CARTESIAN_POINT ( 'NONE',  ( 0.000000000000000000, 0.000000000000000000, 0.000000000000000000 ) ) ;
#8786=DIRECTION ( 'NONE',  ( -1.000000000000000000, -0.000000000000000000, -0.000000000000000000 ) ) ;
#8788=VERTEX_POINT ( 'NONE', #6531 ) ;
#8789=ORIENTED_EDGE ( 'NONE', *, *, #18227, .T. ) ;
#8790=FACE_OUTER_BOUND ( 'NONE', #13197, .T. ) ;
#8799=CARTESIAN_POINT ( 'NONE',  ( 0.000000000000000000, -6.872116855662673274, -64.47358224882424338 ) ) ;
#8800=CARTESIAN_POINT ( 'NONE',  ( 9.999999999999998224, -51.96384592647235934, 49.83732252579596889 ) ) ;
#8804=EDGE_LOOP ( 'NONE', ( #14233, #5043, #8789, #16723 ) ) ;
#8808=VERTEX_POINT ( 'NONE', #10035 ) ;
#8812=DIRECTION ( 'NONE',  ( 0.000000000000000000, 0.000000000000000000, 1.000000000000000000 ) ) ;
#8813=CARTESIAN_POINT ( 'NONE',  ( 20.00000000000000355, 0.000000000000000000, 0.000000000000000000 ) ) ;
#8814=ORIENTED_EDGE ( 'NONE', *, *, #11594, .F. ) ;
#8815=DIRECTION ( 'NONE',  ( -1.000000000000000000, 0.000000000000000000, 0.000000000000000000 ) ) ;
#8817=CARTESIAN_POINT ( 'NONE',  ( 0.000000000000000000, 42.42902769288536291, 49.02903636734212967 ) ) ;
#8820=ADVANCED_FACE ( 'NONE', ( #9921 ), #8334, .T. ) ;
#8823=CIRCLE ( 'NONE', #10534, 72.00000000007199219 ) ;
#8825=ORIENTED_EDGE ( 'NONE', *, *, #16526, .F. ) ;
#8834=DIRECTION ( 'NONE',  ( -1.000000000000000000, -0.000000000000000000, 0.000000000000000000 ) ) ;
#8838=CYLINDRICAL_SURFACE ( 'NONE', #10594, 27.60000000002760245 ) ;
#8845=EDGE_CURVE ( 'NONE', #6733, #9385, #3146, .T. ) ;
#8853=AXIS2_PLACEMENT_3D ( 'NONE', #14168, #3023, #15742 ) ;
#8854=AXIS2_PLACEMENT_3D ( 'NONE', #10196, #10309, #15078 ) ;
#8856=CARTESIAN_POINT ( 'NONE',  ( 19.99999999999999645, 0.000000000000000000, 0.000000000000000000 ) ) ;
#8857=AXIS2_PLACEMENT_3D ( 'NONE', #15479, #1291, #4349 ) ;
#8859=CARTESIAN_POINT ( 'NONE',  ( 19.99999999999999645, 14.55863677812212131, -63.60407295269091321 ) ) ;
#8862=VERTEX_POINT ( 'NONE', #20289 ) ;
#8868=ORIENTED_EDGE ( 'NONE', *, *, #18120, .F. ) ;
#8869=DIRECTION ( 'NONE',  ( 0.000000000000000000, 0.000000000000000000, 1.000000000000000000 ) ) ;
#8875=CYLINDRICAL_SURFACE ( 'NONE', #1255, 72.00000000007199219 ) ;
#8877=CARTESIAN_POINT ( 'NONE',  ( 19.99999999999999645, 36.54710069451126486, -54.05313526368077248 ) ) ;
#8879=AXIS2_PLACEMENT_3D ( 'NONE', #15751, #12252, #9401 ) ;
#8886=AXIS2_PLACEMENT_3D ( 'NONE', #1692, #19272, #3169 ) ;
#8888=CIRCLE ( 'NONE', #14329, 27.60000000002759535 ) ;
#8891=AXIS2_PLACEMENT_3D ( 'NONE', #3575, #16830, #19898 ) ;
#8898=CYLINDRICAL_SURFACE ( 'NONE', #7512, 72.00000000007199219 ) ;
#8899=VERTEX_POINT ( 'NONE', #13737 ) ;
#8903=EDGE_LOOP ( 'NONE', ( #16245, #3912, #19509, #1184 ) ) ;
#8905=VECTOR ( 'NONE', #13093, 1000.000000000000000 ) ;
#8906=AXIS2_PLACEMENT_3D ( 'NONE', #14373, #9072, #1016 ) ;
#8909=DIRECTION ( 'NONE',  ( 0.000000000000000000, 0.000000000000000000, 1.000000000000000000 ) ) ;
#8915=DIRECTION ( 'NONE',  ( 0.000000000000000000, 0.000000000000000000, 1.000000000000000000 ) ) ;
#8927=ORIENTED_EDGE ( 'NONE', *, *, #10493, .T. ) ;
#8928=FACE_OUTER_BOUND ( 'NONE', #9369, .T. ) ;
#8934=AXIS2_PLACEMENT_3D ( 'NONE', #1509, #16220, #10064 ) ;
#8935=DIRECTION ( 'NONE',  ( 1.000000000000000000, 0.000000000000000000, 0.000000000000000000 ) ) ;
#8937=AXIS2_PLACEMENT_3D ( 'NONE', #13803, #20250, #553 ) ;
#8944=CYLINDRICAL_SURFACE ( 'NONE', #15750, 7.500000000000000000 ) ;
#8945=CARTESIAN_POINT ( 'NONE',  ( 19.99999999999999645, 0.000000000000000000, 0.000000000000000000 ) ) ;
#8951=DIRECTION ( 'NONE',  ( 0.000000000000000000, 0.1361666490962466225, -0.9906859460363307557 ) ) ;
#8954=EDGE_CURVE ( 'NONE', #8604, #20034, #10251, .T. ) ;
#8955=CYLINDRICAL_SURFACE ( 'NONE', #10236, 65.24900000006525147 ) ;
#8956=ORIENTED_EDGE ( 'NONE', *, *, #7397, .T. ) ;
#8957=CIRCLE ( 'NONE', #2533, 65.24900000006525147 ) ;
#8959=EDGE_CURVE ( 'NONE', #2251, #4710, #11597, .T. ) ;
#8960=ORIENTED_EDGE ( 'NONE', *, *, #16354, .F. ) ;
#8961=EDGE_CURVE ( 'NONE', #9123, #12996, #5848, .T. ) ;
#8969=DIRECTION ( 'NONE',  ( 1.000000000000000000, 0.000000000000000000, 0.000000000000000000 ) ) ;
#8970=ORIENTED_EDGE ( 'NONE', *, *, #20769, .F. ) ;
#8972=DIRECTION ( 'NONE',  ( 1.000000000000000000, -0.000000000000000000, -0.000000000000000000 ) ) ;
#8979=CARTESIAN_POINT ( 'NONE',  ( 19.99999999999999645, 51.43306257653143376, 40.15061736769582268 ) ) ;
#8983=EDGE_LOOP ( 'NONE', ( #5006, #4825, #5362, #13818 ) ) ;
#8988=ORIENTED_EDGE ( 'NONE', *, *, #12489, .F. ) ;
#8990=DIRECTION ( 'NONE',  ( -1.000000000000000000, -0.000000000000000000, 0.000000000000000000 ) ) ;
#8991=CYLINDRICAL_SURFACE ( 'NONE', #6477, 27.60000000002760245 ) ;
#8996=AXIS2_PLACEMENT_3D ( 'NONE', #8427, #15286, #20049 ) ;
#8997=DIRECTION ( 'NONE',  ( 0.000000000000000000, 0.000000000000000000, -1.000000000000000000 ) ) ;
#9002=EDGE_CURVE ( 'NONE', #6180, #3647, #17341, .T. ) ;
#9006=CARTESIAN_POINT ( 'NONE',  ( 19.99999999999999645, -63.17103598352137794, 16.33561182745118501 ) ) ;
#9007=ORIENTED_EDGE ( 'NONE', *, *, #14780, .F. ) ;
#9010=CARTESIAN_POINT ( 'NONE',  ( 9.999999999999998224, 70.29359119158485214, 15.58239511117312226 ) ) ;
#9011=ORIENTED_EDGE ( 'NONE', *, *, #20584, .T. ) ;
#9012=DIRECTION ( 'NONE',  ( 0.000000000000000000, 0.000000000000000000, -1.000000000000000000 ) ) ;
#9015=CARTESIAN_POINT ( 'NONE',  ( 0.000000000000000000, -5.762283366690708952, -64.99406197038678101 ) ) ;
#9017=VERTEX_POINT ( 'NONE', #9489 ) ;
#9020=CARTESIAN_POINT ( 'NONE',  ( 19.99999999999999645, -68.15657073222419626, -23.20952102120349991 ) ) ;
#9021=VECTOR ( 'NONE', #16379, 1000.000000000000000 ) ;
#9022=CIRCLE ( 'NONE', #2250, 27.60000000002759535 ) ;
#9026=CARTESIAN_POINT ( 'NONE',  ( 150.0000507999999968, 4.898587196589412829E-16, -4.000000000000000000 ) ) ;
#9031=CARTESIAN_POINT ( 'NONE',  ( 19.99999999999999645, -35.35772184876843482, -54.34979580218228534 ) ) ;
#9032=CARTESIAN_POINT ( 'NONE',  ( 19.99999999999999645, 11.98658579560678206, -64.13855129306456604 ) ) ;
#9036=CYLINDRICAL_SURFACE ( 'NONE', #2768, 72.00000000007199219 ) ;
#9037=EDGE_LOOP ( 'NONE', ( #5344, #168, #14809, #4094 ) ) ;
#9039=CARTESIAN_POINT ( 'NONE',  ( 9.999999999999998224, -58.26603306961992956, 42.29739224042451440 ) ) ;
#9040=ORIENTED_EDGE ( 'NONE', *, *, #3026, .T. ) ;
#9041=CARTESIAN_POINT ( 'NONE',  ( 0.000000000000000000, -39.37110852956848817, 51.51683813304857296 ) ) ;
#9044=DIRECTION ( 'NONE',  ( 0.000000000000000000, 0.000000000000000000, 1.000000000000000000 ) ) ;
#9046=AXIS2_PLACEMENT_3D ( 'NONE', #7616, #11335, #16923 ) ;
#9048=DIRECTION ( 'NONE',  ( -1.000000000000000000, 0.000000000000000000, -0.000000000000000000 ) ) ;
#9049=ADVANCED_FACE ( 'NONE', ( #14381 ), #11090, .T. ) ;
#9054=AXIS2_PLACEMENT_3D ( 'NONE', #9810, #3143, #5039 ) ;
#9055=AXIS2_PLACEMENT_3D ( 'NONE', #8463, #5390, #2118 ) ;
#9057=EDGE_CURVE ( 'NONE', #7334, #6474, #10938, .T. ) ;
#9061=ORIENTED_EDGE ( 'NONE', *, *, #18922, .F. ) ;
#9062=AXIS2_PLACEMENT_3D ( 'NONE', #20727, #19748, #16081 ) ;
#9065=ORIENTED_EDGE ( 'NONE', *, *, #13558, .T. ) ;
#9066=CIRCLE ( 'NONE', #20905, 65.24900000006525147 ) ;
#9071=AXIS2_PLACEMENT_3D ( 'NONE', #20588, #12537, #17622 ) ;
#9072=DIRECTION ( 'NONE',  ( -1.000000000000000000, -0.000000000000000000, -0.000000000000000000 ) ) ;
#9075=EDGE_LOOP ( 'NONE', ( #9359, #6431, #7739, #19746 ) ) ;
#9080=EDGE_CURVE ( 'NONE', #5761, #7195, #11184, .T. ) ;
#9082=EDGE_CURVE ( 'NONE', #17178, #16888, #10870, .T. ) ;
#9089=ADVANCED_FACE ( 'NONE', ( #14174 ), #2816, .T. ) ;
#9091=CARTESIAN_POINT ( 'NONE',  ( 19.99999999999999645, -64.79224928664389438, -2.456263514198281150 ) ) ;
#9095=CARTESIAN_POINT ( 'NONE',  ( 19.99999999999999645, -60.35829202194859278, -24.78524934717612282 ) ) ;
#9097=ORIENTED_EDGE ( 'NONE', *, *, #8710, .F. ) ;
#9098=ORIENTED_EDGE ( 'NONE', *, *, #2612, .F. ) ;
#9099=CARTESIAN_POINT ( 'NONE',  ( 19.99999999999999645, -28.84646472442415543, -58.52617768068463278 ) ) ;
#9101=DIRECTION ( 'NONE',  ( 1.000000000000000000, -0.000000000000000000, -0.000000000000000000 ) ) ;
#9111=EDGE_CURVE ( 'NONE', #3661, #20364, #117, .T. ) ;
#9116=DIRECTION ( 'NONE',  ( -1.000000000000000000, 0.000000000000000000, -0.000000000000000000 ) ) ;
#9118=DIRECTION ( 'NONE',  ( -1.000000000000000000, -0.000000000000000000, -0.000000000000000000 ) ) ;
#9119=ORIENTED_EDGE ( 'NONE', *, *, #11699, .T. ) ;
#9121=DIRECTION ( 'NONE',  ( -1.000000000000000000, -0.000000000000000000, 0.000000000000000000 ) ) ;
#9123=VERTEX_POINT ( 'NONE', #20516 ) ;
#9127=FACE_OUTER_BOUND ( 'NONE', #10253, .T. ) ;
#9131=CARTESIAN_POINT ( 'NONE',  ( 19.99999999999999645, 0.000000000000000000, 0.000000000000000000 ) ) ;
#9133=CARTESIAN_POINT ( 'NONE',  ( 0.000000000000000000, -5.762283366691622000, 64.99406197038668154 ) ) ;
#9134=ORIENTED_EDGE ( 'NONE', *, *, #18959, .T. ) ;
#9135=EDGE_CURVE ( 'NONE', #20910, #12110, #9263, .T. ) ;
#9136=FACE_OUTER_BOUND ( 'NONE', #7475, .T. ) ;
#9139=CARTESIAN_POINT ( 'NONE',  ( 19.99999999999999645, 0.000000000000000000, 0.000000000000000000 ) ) ;
#9141=EDGE_LOOP ( 'NONE', ( #14870, #2222, #1045, #9580 ) ) ;
#9142=DIRECTION ( 'NONE',  ( 1.000000000000000000, 0.000000000000000000, 0.000000000000000000 ) ) ;
#9146=DIRECTION ( 'NONE',  ( -1.000000000000000000, 0.000000000000000000, 0.000000000000000000 ) ) ;
#9149=DIRECTION ( 'NONE',  ( 1.000000000000000000, 0.000000000000000000, 0.000000000000000000 ) ) ;
#9151=CARTESIAN_POINT ( 'NONE',  ( 19.99999999999999645, 10.77748419466696284, 63.93680186330476545 ) ) ;
#9152=VECTOR ( 'NONE', #3216, 1000.000000000000000 ) ;
#9153=CARTESIAN_POINT ( 'NONE',  ( 0.000000000000000000, -38.22257254261699444, -61.01667762370178139 ) ) ;
#9154=VERTEX_POINT ( 'NONE', #16170 ) ;
#9155=SURFACE_SIDE_STYLE ('',( #10758 ) ) ;
#9157=AXIS2_PLACEMENT_3D ( 'NONE', #2034, #6903, #17084 ) ;
#9159=DIRECTION ( 'NONE',  ( 0.000000000000000000, 0.000000000000000000, 1.000000000000000000 ) ) ;
#9160=FACE_OUTER_BOUND ( 'NONE', #7379, .T. ) ;
#9165=CYLINDRICAL_SURFACE ( 'NONE', #15778, 65.24900000006525147 ) ;
#9166=CARTESIAN_POINT ( 'NONE',  ( 0.000000000000000000, 45.48683723007275148, -46.78012013466171481 ) ) ;
#9169=ORIENTED_EDGE ( 'NONE', *, *, #1882, .F. ) ;
#9170=CARTESIAN_POINT ( 'NONE',  ( 9.999999999999998224, -18.50424539729797146, -69.58155576219135696 ) ) ;
#9173=VECTOR ( 'NONE', #9447, 1000.000000000000000 ) ;
#9175=LINE ( 'NONE', #7467, #14494 ) ;
#9178=ORIENTED_EDGE ( 'NONE', *, *, #5598, .F. ) ;
#9179=FACE_OUTER_BOUND ( 'NONE', #16798, .T. ) ;
#9180=ORIENTED_EDGE ( 'NONE', *, *, #14275, .T. ) ;
#9185=CIRCLE ( 'NONE', #13582, 65.24900000006525147 ) ;
#9186=CARTESIAN_POINT ( 'NONE',  ( 19.99999999999999645, -5.762283366690708064, -64.99406197038676680 ) ) ;
#9188=CYLINDRICAL_SURFACE ( 'NONE', #17164, 27.60000000002759890 ) ;
#9191=VERTEX_POINT ( 'NONE', #11595 ) ;
#9192=EDGE_CURVE ( 'NONE', #19322, #17178, #1805, .T. ) ;
#9194=LINE ( 'NONE', #7385, #1425 ) ;
#9197=AXIS2_PLACEMENT_3D ( 'NONE', #9200, #12495, #12387 ) ;
#9199=LINE ( 'NONE', #2840, #2778 ) ;
#9200=CARTESIAN_POINT ( 'NONE',  ( 0.000000000000000000, 0.000000000000000000, 0.000000000000000000 ) ) ;
#9217=AXIS2_PLACEMENT_3D ( 'NONE', #7087, #325, #10080 ) ;
#9218=ORIENTED_EDGE ( 'NONE', *, *, #4688, .T. ) ;
#9223=CARTESIAN_POINT ( 'NONE',  ( 0.000000000000000000, -36.54710069451090959, 54.05313526368099986 ) ) ;
#9226=EDGE_LOOP ( 'NONE', ( #7387, #2372, #20863, #18884 ) ) ;
#9228=EDGE_CURVE ( 'NONE', #18900, #2782, #13644, .T. ) ;
#9229=( NAMED_UNIT ( * ) SI_UNIT ( $, .STERADIAN. ) SOLID_ANGLE_UNIT ( ) );
#9236=CIRCLE ( 'NONE', #99, 27.60000000002759890 ) ;
#9237=EDGE_CURVE ( 'NONE', #13848, #4671, #4924, .T. ) ;
#9240=EDGE_CURVE ( 'NONE', #12110, #12459, #8204, .T. ) ;
#9242=CARTESIAN_POINT ( 'NONE',  ( 9.999999999999998224, -71.76067541710854414, 5.865617076724380041 ) ) ;
#9245=LINE ( 'NONE', #1095, #7595 ) ;
#9247=ORIENTED_EDGE ( 'NONE', *, *, #11428, .F. ) ;
#9249=CARTESIAN_POINT ( 'NONE',  ( 19.99999999999999645, -10.74906464462167577, 71.19310085447963843 ) ) ;
#9257=CIRCLE ( 'NONE', #4851, 27.60000000002759890 ) ;
#9263=CIRCLE ( 'NONE', #18733, 27.60000000002760245 ) ;
#9264=AXIS2_PLACEMENT_3D ( 'NONE', #14550, #224, #3396 ) ;
#9267=DIRECTION ( 'NONE',  ( -1.000000000000000000, -0.000000000000000000, -0.000000000000000000 ) ) ;
#9268=ORIENTED_EDGE ( 'NONE', *, *, #19593, .T. ) ;
#9270=CARTESIAN_POINT ( 'NONE',  ( 0.000000000000000000, 67.51707036274449081, -25.00890260772307627 ) ) ;
#9273=DIRECTION ( 'NONE',  ( 0.000000000000000000, 0.000000000000000000, 1.000000000000000000 ) ) ;
#9274=DIRECTION ( 'NONE',  ( -1.000000000000000000, 0.000000000000000000, -0.000000000000000000 ) ) ;
#9276=VERTEX_POINT ( 'NONE', #13297 ) ;
#9279=ORIENTED_EDGE ( 'NONE', *, *, #15416, .T. ) ;
#9283=CIRCLE ( 'NONE', #2518, 27.60000000002759890 ) ;
#9286=DIRECTION ( 'NONE',  ( -1.000000000000000000, 0.000000000000000000, -0.000000000000000000 ) ) ;
#9289=CARTESIAN_POINT ( 'NONE',  ( 19.99999999999999645, -64.44931368725514176, -10.18420179740675380 ) ) ;
#9297=VERTEX_POINT ( 'NONE', #10114 ) ;
#9300=ORIENTED_EDGE ( 'NONE', *, *, #18528, .T. ) ;
#9315=DIRECTION ( 'NONE',  ( -1.000000000000000000, 0.000000000000000000, 0.000000000000000000 ) ) ;
#9316=ADVANCED_FACE ( 'NONE', ( #1958 ), #14990, .T. ) ;
#9324=ORIENTED_EDGE ( 'NONE', *, *, #19442, .F. ) ;
#9325=CARTESIAN_POINT ( 'NONE',  ( 19.99999999999999645, 62.46228066917787203, 18.86519267363478036 ) ) ;
#9327=DIRECTION ( 'NONE',  ( 0.000000000000000000, 0.000000000000000000, -1.000000000000000000 ) ) ;
#9330=ORIENTED_EDGE ( 'NONE', *, *, #16474, .F. ) ;
#9335=CIRCLE ( 'NONE', #8312, 65.24900000006525147 ) ;
#9336=CARTESIAN_POINT ( 'NONE',  ( 19.99999999999999645, 59.31169354540775629, -27.19476070466793871 ) ) ;
#9342=DIRECTION ( 'NONE',  ( 0.000000000000000000, 0.000000000000000000, 1.000000000000000000 ) ) ;
#9352=DIRECTION ( 'NONE',  ( 0.000000000000000000, 0.000000000000000000, 1.000000000000000000 ) ) ;
#9354=ORIENTED_EDGE ( 'NONE', *, *, #8694, .T. ) ;
#9355=AXIS2_PLACEMENT_3D ( 'NONE', #5391, #11859, #12258 ) ;
#9356=CARTESIAN_POINT ( 'NONE',  ( 19.99999999999999645, 20.60847369613070512, -61.90898814327692889 ) ) ;
#9359=ORIENTED_EDGE ( 'NONE', *, *, #19111, .T. ) ;
#9366=AXIS2_PLACEMENT_3D ( 'NONE', #5233, #11700, #19948 ) ;
#9367=AXIS2_PLACEMENT_3D ( 'NONE', #14730, #4874, #3474 ) ;
#9369=EDGE_LOOP ( 'NONE', ( #5067, #2026, #14520, #12219 ) ) ;
#9371=AXIS2_PLACEMENT_3D ( 'NONE', #9477, #19235, #14476 ) ;
#9375=CARTESIAN_POINT ( 'NONE',  ( 19.99999999999999645, 0.000000000000000000, 0.000000000000000000 ) ) ;
#9378=DIRECTION ( 'NONE',  ( 0.000000000000000000, -0.2697967711570115057, -0.9629172873478029082 ) ) ;
#9379=EDGE_CURVE ( 'NONE', #19446, #12867, #2143, .T. ) ;
#9382=AXIS2_PLACEMENT_3D ( 'NONE', #15577, #7741, #2864 ) ;
#9383=LINE ( 'NONE', #3222, #17503 ) ;
#9385=VERTEX_POINT ( 'NONE', #784 ) ;
#9386=CARTESIAN_POINT ( 'NONE',  ( 19.99999999999999645, 0.000000000000000000, 0.000000000000000000 ) ) ;
#9388=CYLINDRICAL_SURFACE ( 'NONE', #3115, 27.60000000002759535 ) ;
#9391=AXIS2_PLACEMENT_3D ( 'NONE', #16513, #8759, #5682 ) ;
#9394=EDGE_CURVE ( 'NONE', #13762, #16945, #14007, .T. ) ;
#9401=DIRECTION ( 'NONE',  ( 0.000000000000000000, -0.6310879443260433153, -0.7757112907044274586 ) ) ;
#9405=DIRECTION ( 'NONE',  ( 0.000000000000000000, -0.8878852184023793281, 0.4600650377311439887 ) ) ;
#9417=ORIENTED_EDGE ( 'NONE', *, *, #1722, .T. ) ;
#9418=DIRECTION ( 'NONE',  ( -1.000000000000000000, 0.000000000000000000, 0.000000000000000000 ) ) ;
#9419=CYLINDRICAL_SURFACE ( 'NONE', #7845, 27.60000000002760245 ) ;
#9426=DIRECTION ( 'NONE',  ( -1.000000000000000000, -0.000000000000000000, -0.000000000000000000 ) ) ;
#9435=LINE ( 'NONE', #6589, #10562 ) ;
#9438=CARTESIAN_POINT ( 'NONE',  ( 19.99999999999999645, 1.971042061629218356, -64.80882494896104618 ) ) ;
#9441=CARTESIAN_POINT ( 'NONE',  ( 0.000000000000000000, -65.23577793412346182, 1.313498510941474740 ) ) ;
#9442=CARTESIAN_POINT ( 'NONE',  ( 19.99999999999999645, -5.762283366691622000, 64.99406197038668154 ) ) ;
#9447=DIRECTION ( 'NONE',  ( 1.000000000000000000, -0.000000000000000000, -0.000000000000000000 ) ) ;
#9449=VERTEX_POINT ( 'NONE', #16677 ) ;
#9454=ORIENTED_EDGE ( 'NONE', *, *, #13428, .T. ) ;
#9455=CYLINDRICAL_SURFACE ( 'NONE', #14020, 72.00000000007199219 ) ;
#9456=ORIENTED_EDGE ( 'NONE', *, *, #10669, .T. ) ;
#9460=VERTEX_POINT ( 'NONE', #16783 ) ;
#9461=CARTESIAN_POINT ( 'NONE',  ( 0.000000000000000000, 46.01927912072526539, 45.67597560296404424 ) ) ;
#9462=ADVANCED_FACE ( 'NONE', ( #7125 ), #15512, .T. ) ;
#9463=EDGE_CURVE ( 'NONE', #12885, #273, #11304, .T. ) ;
#9469=AXIS2_PLACEMENT_3D ( 'NONE', #14997, #17878, #16271 ) ;
#9470=CARTESIAN_POINT ( 'NONE',  ( 0.000000000000000000, 70.29359119158506530, -15.58239511117215415 ) ) ;
#9474=CARTESIAN_POINT ( 'NONE',  ( -65.00002539999999840, 0.000000000000000000, 1.000000000000000000 ) ) ;
#9477=CARTESIAN_POINT ( 'NONE',  ( 0.000000000000000000, 0.000000000000000000, 0.000000000000000000 ) ) ;
#9479=VERTEX_POINT ( 'NONE', #18483 ) ;
#9481=CARTESIAN_POINT ( 'NONE',  ( 0.000000000000000000, -68.15657073222419626, -23.20952102120350347 ) ) ;
#9482=ORIENTED_EDGE ( 'NONE', *, *, #8582, .F. ) ;
#9489=CARTESIAN_POINT ( 'NONE',  ( 0.000000000000000000, -53.26727847779503833, -48.44168704307686113 ) ) ;
#9492=EDGE_LOOP ( 'NONE', ( #8315, #18711, #12702, #19518 ) ) ;
#9494=DIRECTION ( 'NONE',  ( 0.000000000000000000, 0.7308359642781252496, -0.6825531432186529024 ) ) ;
#9497=CARTESIAN_POINT ( 'NONE',  ( 19.99999999999999645, -64.44931368725514176, -10.18420179740675380 ) ) ;
#9501=EDGE_CURVE ( 'NONE', #1075, #8470, #19421, .T. ) ;
#9502=ORIENTED_EDGE ( 'NONE', *, *, #19562, .T. ) ;
#9518=AXIS2_PLACEMENT_3D ( 'NONE', #6248, #14002, #3067 ) ;
#9519=CARTESIAN_POINT ( 'NONE',  ( 19.99999999999999645, 28.84646472442533494, -58.52617768068405013 ) ) ;
#9522=ORIENTED_EDGE ( 'NONE', *, *, #7364, .F. ) ;
#9526=EDGE_LOOP ( 'NONE', ( #5422, #6193, #17558, #19256 ) ) ;
#9534=ORIENTED_EDGE ( 'NONE', *, *, #5097, .F. ) ;
#9546=CIRCLE ( 'NONE', #15308, 65.24900000006525147 ) ;
#9550=CYLINDRICAL_SURFACE ( 'NONE', #13287, 27.60000000002760245 ) ;
#9551=VERTEX_POINT ( 'NONE', #2691 ) ;
#9554=ORIENTED_EDGE ( 'NONE', *, *, #12244, .F. ) ;
#9557=CARTESIAN_POINT ( 'NONE',  ( 0.000000000000000000, 59.36728637278075382, -40.73727173906726762 ) ) ;
#9561=CARTESIAN_POINT ( 'NONE',  ( 19.99999999999999645, -28.84646472442495480, 58.52617768068423487 ) ) ;
#9564=AXIS2_PLACEMENT_3D ( 'NONE', #15333, #5680, #16600 ) ;
#9569=AXIS2_PLACEMENT_3D ( 'NONE', #15329, #611, #13637 ) ;
#9571=CARTESIAN_POINT ( 'NONE',  ( 19.99999999999999645, 49.77519642624007901, 42.18840861821802690 ) ) ;
#9573=ORIENTED_EDGE ( 'NONE', *, *, #19434, .F. ) ;
#9575=DIRECTION ( 'NONE',  ( 0.000000000000000000, -0.3984010898462297390, -0.9172113015054581542 ) ) ;
#9576=DIRECTION ( 'NONE',  ( 0.000000000000000000, -7.039457583666959814E-15, 1.000000000000000000 ) ) ;
#9578=AXIS2_PLACEMENT_3D ( 'NONE', #3061, #4552, #20753 ) ;
#9580=ORIENTED_EDGE ( 'NONE', *, *, #12903, .T. ) ;
#9582=CIRCLE ( 'NONE', #14237, 27.60000000002759535 ) ;
#9587=VERTEX_POINT ( 'NONE', #9153 ) ;
#9588=CARTESIAN_POINT ( 'NONE',  ( -10.00000000000000000, 0.000000000000000000, 0.000000000000000000 ) ) ;
#9589=ORIENTED_EDGE ( 'NONE', *, *, #4292, .F. ) ;
#9592=DIRECTION ( 'NONE',  ( 0.000000000000000000, 0.5195839500354344498, -0.8544194045464880150 ) ) ;
#9593=AXIS2_PLACEMENT_3D ( 'NONE', #8008, #20928, #15746 ) ;
#9599=LINE ( 'NONE', #1756, #13638 ) ;
#9600=ORIENTED_EDGE ( 'NONE', *, *, #16346, .T. ) ;
#9601=CIRCLE ( 'NONE', #10276, 72.00000000007199219 ) ;
#9603=CIRCLE ( 'NONE', #470, 27.60000000002760245 ) ;
#9604=EDGE_CURVE ( 'NONE', #1518, #15789, #7211, .T. ) ;
#9607=CARTESIAN_POINT ( 'NONE',  ( -10.00000000000000000, 0.000000000000000000, 0.000000000000000000 ) ) ;
#9608=CARTESIAN_POINT ( 'NONE',  ( 19.99999999999999645, -68.15657073222450890, 23.20952102120258331 ) ) ;
#9612=ORIENTED_EDGE ( 'NONE', *, *, #8721, .T. ) ;
#9616=EDGE_CURVE ( 'NONE', #16343, #13609, #16042, .T. ) ;
#9619=CARTESIAN_POINT ( 'NONE',  ( 19.99999999999999645, -20.34307325858738835, -69.06634035770328239 ) ) ;
#9624=VECTOR ( 'NONE', #18937, 1000.000000000000000 ) ;
#9626=FACE_OUTER_BOUND ( 'NONE', #5523, .T. ) ;
#9633=AXIS2_PLACEMENT_3D ( 'NONE', #11080, #5984, #14056 ) ;
#9635=CARTESIAN_POINT ( 'NONE',  ( 0.000000000000000000, -27.62776854598897813, 58.65812137498992485 ) ) ;
#9637=EDGE_CURVE ( 'NONE', #20917, #15524, #6883, .T. ) ;
#9639=AXIS2_PLACEMENT_3D ( 'NONE', #8481, #3504, #14558 ) ;
#9640=ADVANCED_FACE ( 'NONE', ( #5011 ), #8389, .T. ) ;
#9642=DIRECTION ( 'NONE',  ( -1.000000000000000000, -0.000000000000000000, 0.000000000000000000 ) ) ;
#9646=CARTESIAN_POINT ( 'NONE',  ( 19.99999999999999645, -61.72688495901628869, 19.84591825363989415 ) ) ;
#9663=DIRECTION ( 'NONE',  ( 0.000000000000000000, 0.000000000000000000, 1.000000000000000000 ) ) ;
#9665=DIRECTION ( 'NONE',  ( -1.000000000000000000, 0.000000000000000000, -0.000000000000000000 ) ) ;
#9670=CARTESIAN_POINT ( 'NONE',  ( 19.99999999999999645, -64.44931368725528387, 10.18420179740584608 ) ) ;
#9673=ADVANCED_FACE ( 'NONE', ( #16244 ), #2031, .T. ) ;
#9674=EDGE_LOOP ( 'NONE', ( #18128, #18626, #8611, #2879 ) ) ;
#9681=VERTEX_POINT ( 'NONE', #5099 ) ;
#9682=DIRECTION ( 'NONE',  ( 0.000000000000000000, -0.8169698930104469792, 0.5766803221148600889 ) ) ;
#9685=DIRECTION ( 'NONE',  ( -1.000000000000000000, 0.000000000000000000, 0.000000000000000000 ) ) ;
#9686=DIRECTION ( 'NONE',  ( 0.000000000000000000, 0.000000000000000000, 1.000000000000000000 ) ) ;
#9689=DIRECTION ( 'NONE',  ( 0.000000000000000000, 0.000000000000000000, 1.000000000000000000 ) ) ;
#9691=DIRECTION ( 'NONE',  ( 0.000000000000000000, 0.000000000000000000, 1.000000000000000000 ) ) ;
#9693=CYLINDRICAL_SURFACE ( 'NONE', #12975, 27.60000000002759890 ) ;
#9697=VERTEX_POINT ( 'NONE', #14966 ) ;
#9700=VECTOR ( 'NONE', #6910, 1000.000000000000000 ) ;
#9701=CIRCLE ( 'NONE', #20528, 65.24900000006525147 ) ;
#9705=DIRECTION ( 'NONE',  ( 0.000000000000000000, 0.000000000000000000, 1.000000000000000000 ) ) ;
#9706=VECTOR ( 'NONE', #16031, 1000.000000000000000 ) ;
#9708=EDGE_LOOP ( 'NONE', ( #4038, #18450, #7242, #11561 ) ) ;
#9714=CIRCLE ( 'NONE', #9391, 65.24900000006525147 ) ;
#9715=ORIENTED_EDGE ( 'NONE', *, *, #13859, .T. ) ;
#9716=DIRECTION ( 'NONE',  ( -1.000000000000000000, 0.000000000000000000, 0.000000000000000000 ) ) ;
#9719=DIRECTION ( 'NONE',  ( 1.000000000000000000, 0.000000000000000000, 0.000000000000000000 ) ) ;
#9726=EDGE_CURVE ( 'NONE', #10201, #15185, #8283, .T. ) ;
#9731=AXIS2_PLACEMENT_3D ( 'NONE', #11716, #19454, #276 ) ;
#9732=DIRECTION ( 'NONE',  ( -1.000000000000000000, -0.000000000000000000, -0.000000000000000000 ) ) ;
#9734=CARTESIAN_POINT ( 'NONE',  ( 19.99999999999999645, -63.48283426024828202, -33.96954156735433372 ) ) ;
#9736=ORIENTED_EDGE ( 'NONE', *, *, #17964, .F. ) ;
#9737=CIRCLE ( 'NONE', #15148, 65.24900000006525147 ) ;
#9743=VERTEX_POINT ( 'NONE', #19420 ) ;
#9744=EDGE_CURVE ( 'NONE', #13498, #13788, #5209, .T. ) ;
#9745=CARTESIAN_POINT ( 'NONE',  ( -10.00000000000000000, 0.000000000000000000, 0.000000000000000000 ) ) ;
#9746=AXIS2_PLACEMENT_3D ( 'NONE', #13128, #14607, #3563 ) ;
#9750=ORIENTED_EDGE ( 'NONE', *, *, #16747, .F. ) ;
#9751=VERTEX_POINT ( 'NONE', #6480 ) ;
#9757=DIRECTION ( 'NONE',  ( 0.000000000000000000, 0.000000000000000000, 1.000000000000000000 ) ) ;
#9760=CARTESIAN_POINT ( 'NONE',  ( 0.000000000000000000, 0.000000000000000000, 0.000000000000000000 ) ) ;
#9762=DIRECTION ( 'NONE',  ( -1.000000000000000000, 0.000000000000000000, 0.000000000000000000 ) ) ;
#9769=EDGE_CURVE ( 'NONE', #3604, #2557, #15022, .T. ) ;
#9771=ORIENTED_EDGE ( 'NONE', *, *, #4130, .F. ) ;
#9774=ORIENTED_EDGE ( 'NONE', *, *, #1665, .F. ) ;
#9778=DIRECTION ( 'NONE',  ( 1.000000000000000000, 0.000000000000000000, 0.000000000000000000 ) ) ;
#9780=VERTEX_POINT ( 'NONE', #7205 ) ;
#9782=EDGE_CURVE ( 'NONE', #10885, #788, #7580, .T. ) ;
#9784=LINE ( 'NONE', #8190, #2179 ) ;
#9786=ORIENTED_EDGE ( 'NONE', *, *, #20878, .T. ) ;
#9788=CARTESIAN_POINT ( 'NONE',  ( 19.99999999999999645, -38.69327817041812523, 52.53819777490620169 ) ) ;
#9789=CARTESIAN_POINT ( 'NONE',  ( 19.99999999999999645, -1.971042061627920727, -64.80882494896108881 ) ) ;
#9794=VERTEX_POINT ( 'NONE', #15381 ) ;
#9796=DIRECTION ( 'NONE',  ( 0.000000000000000000, -0.6310879443260433153, -0.7757112907044274586 ) ) ;
#9798=EDGE_CURVE ( 'NONE', #5332, #4217, #864, .T. ) ;
#9800=DIRECTION ( 'NONE',  ( -1.000000000000000000, 0.000000000000000000, 0.000000000000000000 ) ) ;
#9803=ORIENTED_EDGE ( 'NONE', *, *, #19952, .F. ) ;
#9810=CARTESIAN_POINT ( 'NONE',  ( 19.99999999999999645, -42.42902769288568976, 49.02903636734183124 ) ) ;
#9816=EDGE_LOOP ( 'NONE', ( #5935, #20859, #6373, #3332 ) ) ;
#9818=FACE_OUTER_BOUND ( 'NONE', #386, .T. ) ;
#9821=ORIENTED_EDGE ( 'NONE', *, *, #15598, .F. ) ;
#9822=VECTOR ( 'NONE', #2905, 1000.000000000000000 ) ;
#9828=EDGE_CURVE ( 'NONE', #10009, #10694, #18083, .T. ) ;
#9829=ORIENTED_EDGE ( 'NONE', *, *, #10645, .T. ) ;
#9830=CARTESIAN_POINT ( 'NONE',  ( 19.99999999999999645, -45.48683723007244595, 46.78012013466202035 ) ) ;
#9833=ORIENTED_EDGE ( 'NONE', *, *, #11702, .F. ) ;
#9834=FACE_OUTER_BOUND ( 'NONE', #18271, .T. ) ;
#9835=ORIENTED_EDGE ( 'NONE', *, *, #7636, .T. ) ;
#9840=EDGE_CURVE ( 'NONE', #17007, #7589, #1834, .T. ) ;
#9841=ORIENTED_EDGE ( 'NONE', *, *, #12625, .F. ) ;
#9843=EDGE_CURVE ( 'NONE', #11409, #12885, #2137, .T. ) ;
#9846=CARTESIAN_POINT ( 'NONE',  ( 0.000000000000000000, 62.46228066917814203, -18.86519267363391350 ) ) ;
#9852=CYLINDRICAL_SURFACE ( 'NONE', #2578, 27.60000000002759890 ) ;
#9853=EDGE_CURVE ( 'NONE', #125, #8080, #17066, .T. ) ;
#9859=DIRECTION ( 'NONE',  ( 0.000000000000000000, 0.2697967711570248839, -0.9629172873477991335 ) ) ;
#9861=ORIENTED_EDGE ( 'NONE', *, *, #3985, .F. ) ;
#9862=CYLINDRICAL_SURFACE ( 'NONE', #119, 72.00000000007199219 ) ;
#9864=DIRECTION ( 'NONE',  ( 0.000000000000000000, 0.000000000000000000, 1.000000000000000000 ) ) ;
#9866=EDGE_CURVE ( 'NONE', #11163, #6966, #16759, .T. ) ;
#9868=VECTOR ( 'NONE', #18895, 1000.000000000000000 ) ;
#9869=EDGE_LOOP ( 'NONE', ( #5948, #4078, #6376, #17956, #19355, #1417, #19658, #15034, #3493, #9835, #13753, #3831, #19340, #18274, #14948, #11860, #15630, #16275, #18844, #6757, #13377, #8927, #19977, #14594, #6191, #18451, #5766, #20332, #5651, #16608, #7701, #4122, #9454, #4896, #10057, #923, #6314, #13032, #20925, #9786, #7431, #13932, #3723, #6833, #1129, #10400, #603, #14873, #10109, #13422, #11999, #11255, #12356, #7413, #39, #16456, #2679, #737, #16955, #18007, #11149, #5583, #17948, #1896, #7716, #20649, #16197, #2882, #3045, #4080, #985, #16428, #3283, #1335, #29, #8199, #15258, #15167, #11484, #15299, #2004, #15548, #15443, #1503, #11599, #1044, #13142, #4741, #2512, #16377, #14804, #11948, #20185, #1968, #5378, #2681, #12267, #2154, #12481, #7130, #18726, #14745, #12511, #4608, #10131, #20763, #9612, #17472, #17994, #13435, #6893, #13309, #15318, #13586, #4090, #9456, #12698, #19569, #13855, #20683, #15396, #1457, #20397, #2264, #4171, #20360, #20765, #18289, #11610, #19423, #8300, #17500, #1500, #17613, #18713, #6950, #14385, #19025, #8583, #708, #7310, #7804, #17200, #20872, #1388, #13220, #3418, #2569, #4419, #4872, #17415, #20930, #8293, #18997, #5033, #3423, #13061, #6093, #8546, #6730, #11397, #3679, #7980, #19360, #9502, #10821, #7410, #3195, #14892, #15917, #15138, #11501, #5434, #10085, #2550, #8960, #5668, #8659, #4785, #13321, #320, #484, #1826, #14106, #3956, #12043, #12213, #11192, #11386 ) ) ;
#9870=CYLINDRICAL_SURFACE ( 'NONE', #1899, 72.00000000007199219 ) ;
#9872=CYLINDRICAL_SURFACE ( 'NONE', #20098, 27.60000000002759890 ) ;
#9873=CARTESIAN_POINT ( 'NONE',  ( 19.99999999999999645, 0.000000000000000000, 0.000000000000000000 ) ) ;
#9876=ORIENTED_EDGE ( 'NONE', *, *, #8584, .T. ) ;
#9877=EDGE_CURVE ( 'NONE', #18360, #19491, #18662, .T. ) ;
#9880=AXIS2_PLACEMENT_3D ( 'NONE', #2399, #15436, #18618 ) ;
#9881=DIRECTION ( 'NONE',  ( -1.000000000000000000, 0.000000000000000000, 0.000000000000000000 ) ) ;
#9884=DIRECTION ( 'NONE',  ( -1.000000000000000000, 0.000000000000000000, -0.000000000000000000 ) ) ;
#9885=EDGE_CURVE ( 'NONE', #11056, #9780, #7932, .T. ) ;
#9886=ORIENTED_EDGE ( 'NONE', *, *, #4709, .F. ) ;
#9889=AXIS2_PLACEMENT_3D ( 'NONE', #5696, #17162, #4101 ) ;
#9891=AXIS2_PLACEMENT_3D ( 'NONE', #4441, #15675, #10907 ) ;
#9894=CARTESIAN_POINT ( 'NONE',  ( 19.99999999999999645, 39.37110852956814000, 51.51683813304883586 ) ) ;
#9896=VECTOR ( 'NONE', #6245, 1000.000000000000000 ) ;
#9897=ORIENTED_EDGE ( 'NONE', *, *, #13269, .T. ) ;
#9899=DIRECTION ( 'NONE',  ( 1.000000000000000000, -0.000000000000000000, 0.000000000000000000 ) ) ;
#9904=CARTESIAN_POINT ( 'NONE',  ( 0.000000000000000000, 0.000000000000000000, 0.000000000000000000 ) ) ;
#9907=FACE_OUTER_BOUND ( 'NONE', #14644, .T. ) ;
#9908=VERTEX_POINT ( 'NONE', #5312 ) ;
#9910=DIRECTION ( 'NONE',  ( 0.000000000000000000, 0.8878852184023763305, -0.4600650377311499839 ) ) ;
#9921=FACE_OUTER_BOUND ( 'NONE', #15485, .T. ) ;
#9922=CIRCLE ( 'NONE', #5860, 65.24900000006525147 ) ;
#9924=ORIENTED_EDGE ( 'NONE', *, *, #8108, .F. ) ;
#9926=AXIS2_PLACEMENT_3D ( 'NONE', #19010, #18805, #10756 ) ;
#9928=CIRCLE ( 'NONE', #6212, 72.00000000007199219 ) ;
#9932=ADVANCED_FACE ( 'NONE', ( #13486 ), #2446, .T. ) ;
#9934=DIRECTION ( 'NONE',  ( -1.000000000000000000, -0.000000000000000000, 0.000000000000000000 ) ) ;
#9937=AXIS2_PLACEMENT_3D ( 'NONE', #7881, #11271, #4911 ) ;
#9939=CIRCLE ( 'NONE', #10279, 27.60000000002760245 ) ;
#9941=ORIENTED_EDGE ( 'NONE', *, *, #3453, .F. ) ;
#9942=DIRECTION ( 'NONE',  ( -1.000000000000000000, 0.000000000000000000, 0.000000000000000000 ) ) ;
#9943=DIRECTION ( 'NONE',  ( -1.000000000000000000, 0.000000000000000000, -0.000000000000000000 ) ) ;
#9945=VERTEX_POINT ( 'NONE', #15171 ) ;
#9946=VERTEX_POINT ( 'NONE', #4675 ) ;
#9948=AXIS2_PLACEMENT_3D ( 'NONE', #19829, #11877, #2563 ) ;
#9952=EDGE_CURVE ( 'NONE', #5576, #10231, #13677, .T. ) ;
#9958=CARTESIAN_POINT ( 'NONE',  ( 0.000000000000000000, -61.72688495901601158, -19.84591825364075746 ) ) ;
#9960=EDGE_LOOP ( 'NONE', ( #7863, #815, #19162, #6104 ) ) ;
#9963=DIRECTION ( 'NONE',  ( -1.000000000000000000, 0.000000000000000000, -0.000000000000000000 ) ) ;
#9970=EDGE_LOOP ( 'NONE', ( #2094, #8502, #3320, #2286 ) ) ;
#9972=DIRECTION ( 'NONE',  ( 0.000000000000000000, 0.000000000000000000, 1.000000000000000000 ) ) ;
#9975=LINE ( 'NONE', #16146, #13358 ) ;
#9976=EDGE_CURVE ( 'NONE', #17187, #8604, #8888, .T. ) ;
#9978=ADVANCED_FACE ( 'NONE', ( #15800 ), #20345, .T. ) ;
#9985=DIRECTION ( 'NONE',  ( -1.000000000000000000, 0.000000000000000000, -0.000000000000000000 ) ) ;
#9991=CARTESIAN_POINT ( 'NONE',  ( 19.99999999999999645, -62.46228066917775834, -18.86519267363519958 ) ) ;
#9992=DIRECTION ( 'NONE',  ( -1.000000000000000000, 0.000000000000000000, 0.000000000000000000 ) ) ;
#9995=ORIENTED_EDGE ( 'NONE', *, *, #12086, .T. ) ;
#9998=DIRECTION ( 'NONE',  ( 0.000000000000000000, -0.3984010898462486683, 0.9172113015054499385 ) ) ;
#10009=VERTEX_POINT ( 'NONE', #17401 ) ;
#10010=CIRCLE ( 'NONE', #6292, 27.60000000002759890 ) ;
#10013=EDGE_CURVE ( 'NONE', #3647, #14496, #7883, .T. ) ;
#10014=DIRECTION ( 'NONE',  ( 0.000000000000000000, 0.000000000000000000, 1.000000000000000000 ) ) ;
#10015=EDGE_LOOP ( 'NONE', ( #1786, #1156, #7025, #5744 ) ) ;
#10019=FACE_OUTER_BOUND ( 'NONE', #8983, .T. ) ;
#10023=VECTOR ( 'NONE', #11778, 1000.000000000000000 ) ;
#10026=VERTEX_POINT ( 'NONE', #9336 ) ;
#10029=CIRCLE ( 'NONE', #14764, 65.24900000006526568 ) ;
#10030=AXIS2_PLACEMENT_3D ( 'NONE', #18082, #6826, #13205 ) ;
#10034=AXIS2_PLACEMENT_3D ( 'NONE', #20589, #6064, #12538 ) ;
#10035=CARTESIAN_POINT ( 'NONE',  ( 0.000000000000000000, 8.857208570070804754, -71.45313048675076573 ) ) ;
#10053=EDGE_LOOP ( 'NONE', ( #10820, #8131, #15815, #1549 ) ) ;
#10057=ORIENTED_EDGE ( 'NONE', *, *, #7803, .T. ) ;
#10059=DIRECTION ( 'NONE',  ( 0.000000000000000000, -0.9422609221188237294, 0.3348796121709770590 ) ) ;
#10064=DIRECTION ( 'NONE',  ( 0.000000000000000000, -0.3984010898462486683, 0.9172113015054499385 ) ) ;
#10065=CARTESIAN_POINT ( 'NONE',  ( 0.000000000000000000, 58.26603306961963824, 42.29739224042492651 ) ) ;
#10070=EDGE_CURVE ( 'NONE', #15500, #15651, #7526, .T. ) ;
#10073=DIRECTION ( 'NONE',  ( 0.000000000000000000, 0.000000000000000000, 1.000000000000000000 ) ) ;
#10074=AXIS2_PLACEMENT_3D ( 'NONE', #1378, #9426, #3056 ) ;
#10076=CARTESIAN_POINT ( 'NONE',  ( 0.000000000000000000, 35.35772184876955038, -54.34979580218157480 ) ) ;
#10079=ORIENTED_EDGE ( 'NONE', *, *, #8108, .T. ) ;
#10080=DIRECTION ( 'NONE',  ( 0.000000000000000000, 0.000000000000000000, 1.000000000000000000 ) ) ;
#10081=VERTEX_POINT ( 'NONE', #12742 ) ;
#10084=ORIENTED_EDGE ( 'NONE', *, *, #14028, .F. ) ;
#10085=ORIENTED_EDGE ( 'NONE', *, *, #649, .T. ) ;
#10086=DIRECTION ( 'NONE',  ( 0.000000000000000000, 0.000000000000000000, 1.000000000000000000 ) ) ;
#10089=DIRECTION ( 'NONE',  ( 0.000000000000000000, 0.000000000000000000, -1.000000000000000000 ) ) ;
#10094=LINE ( 'NONE', #1937, #13018 ) ;
#10102=ORIENTED_EDGE ( 'NONE', *, *, #7665, .F. ) ;
#10109=ORIENTED_EDGE ( 'NONE', *, *, #4432, .T. ) ;
#10114=CARTESIAN_POINT ( 'NONE',  ( 0.000000000000000000, -64.44931368725528387, 10.18420179740584608 ) ) ;
#10115=AXIS2_PLACEMENT_3D ( 'NONE', #10733, #4253, #12526 ) ;
#10117=EDGE_LOOP ( 'NONE', ( #15179, #18953, #3354, #2062 ) ) ;
#10121=CYLINDRICAL_SURFACE ( 'NONE', #12869, 72.00000000007199219 ) ;
#10122=EDGE_CURVE ( 'NONE', #10739, #18397, #1421, .T. ) ;
#10123=ORIENTED_EDGE ( 'NONE', *, *, #2612, .T. ) ;
#10125=DIRECTION ( 'NONE',  ( 0.000000000000000000, 0.6310879443260539734, -0.7757112907044189098 ) ) ;
#10127=EDGE_CURVE ( 'NONE', #10560, #18447, #8503, .T. ) ;
#10129=EDGE_CURVE ( 'NONE', #12459, #20061, #6848, .T. ) ;
#10131=ORIENTED_EDGE ( 'NONE', *, *, #16466, .T. ) ;
#10134=ORIENTED_EDGE ( 'NONE', *, *, #3610, .T. ) ;
#10135=CYLINDRICAL_SURFACE ( 'NONE', #12083, 27.60000000002760245 ) ;
#10137=PRODUCT_CONTEXT ( 'NONE', #12520, 'mechanical' ) ;
#10139=VERTEX_POINT ( 'NONE', #107 ) ;
#10140=DIRECTION ( 'NONE',  ( 0.000000000000000000, 0.000000000000000000, 1.000000000000000000 ) ) ;
#10143=ADVANCED_FACE ( 'NONE', ( #16222 ), #1706, .T. ) ;
#10144=AXIS2_PLACEMENT_3D ( 'NONE', #7159, #10461, #3982 ) ;
#10146=PLANE ( 'NONE',  #20349 ) ;
#10147=VERTEX_POINT ( 'NONE', #18121 ) ;
#10151=ORIENTED_EDGE ( 'NONE', *, *, #20429, .T. ) ;
#10153=ORIENTED_EDGE ( 'NONE', *, *, #18922, .T. ) ;
#10154=DIRECTION ( 'NONE',  ( 0.000000000000000000, 0.000000000000000000, 1.000000000000000000 ) ) ;
#10157=ORIENTED_EDGE ( 'NONE', *, *, #17169, .F. ) ;
#10158=CYLINDRICAL_SURFACE ( 'NONE', #8339, 27.60000000002760245 ) ;
#10171=AXIS2_PLACEMENT_3D ( 'NONE', #16571, #19866, #11602 ) ;
#10175=LINE ( 'NONE', #8379, #1777 ) ;
#10176=VERTEX_POINT ( 'NONE', #19601 ) ;
#10177=VECTOR ( 'NONE', #8708, 1000.000000000000000 ) ;
#10180=VERTEX_POINT ( 'NONE', #5074 ) ;
#10181=VECTOR ( 'NONE', #7864, 1000.000000000000000 ) ;
#10182=VERTEX_POINT ( 'NONE', #15358 ) ;
#10183=FACE_OUTER_BOUND ( 'NONE', #14514, .T. ) ;
#10186=DIRECTION ( 'NONE',  ( 0.000000000000000000, 0.000000000000000000, 1.000000000000000000 ) ) ;
#10191=CIRCLE ( 'NONE', #15262, 27.60000000002759890 ) ;
#10196=CARTESIAN_POINT ( 'NONE',  ( 19.99999999999999645, 0.000000000000000000, 0.000000000000000000 ) ) ;
#10201=VERTEX_POINT ( 'NONE', #13776 ) ;
#10202=CARTESIAN_POINT ( 'NONE',  ( 19.99999999999999645, -71.76067541710845887, -5.865617076725382795 ) ) ;
#10206=ORIENTED_EDGE ( 'NONE', *, *, #11699, .F. ) ;
#10208=CIRCLE ( 'NONE', #13272, 72.00000000007199219 ) ;
#10209=EDGE_CURVE ( 'NONE', #15185, #5437, #14273, .T. ) ;
#10216=ADVANCED_FACE ( 'NONE', ( #18545 ), #841, .T. ) ;
#10217=VERTEX_POINT ( 'NONE', #19803 ) ;
#10220=ORIENTED_EDGE ( 'NONE', *, *, #16708, .F. ) ;
#10223=AXIS2_PLACEMENT_3D ( 'NONE', #19708, #7083, #11973 ) ;
#10224=ORIENTED_EDGE ( 'NONE', *, *, #8194, .F. ) ;
#10226=CIRCLE ( 'NONE', #18349, 4.000000000000000000 ) ;
#10228=CARTESIAN_POINT ( 'NONE',  ( 0.000000000000000000, -18.50424539729892714, 69.58155576219110117 ) ) ;
#10230=ORIENTED_EDGE ( 'NONE', *, *, #9240, .T. ) ;
#10231=VERTEX_POINT ( 'NONE', #3691 ) ;
#10233=ORIENTED_EDGE ( 'NONE', *, *, #18143, .F. ) ;
#10234=DIRECTION ( 'NONE',  ( -1.000000000000000000, -0.000000000000000000, 0.000000000000000000 ) ) ;
#10236=AXIS2_PLACEMENT_3D ( 'NONE', #18499, #9934, #16402 ) ;
#10238=CARTESIAN_POINT ( 'NONE',  ( 0.000000000000000000, 64.44931368725535492, -10.18420179740539844 ) ) ;
#10240=EDGE_CURVE ( 'NONE', #3307, #10946, #16408, .T. ) ;
#10241=ORIENTED_EDGE ( 'NONE', *, *, #5690, .F. ) ;
#10243=CARTESIAN_POINT ( 'NONE',  ( 19.99999999999999645, 43.56693332842786504, 48.57318520917521454 ) ) ;
#10244=VERTEX_POINT ( 'NONE', #18225 ) ;
#10246=DIRECTION ( 'NONE',  ( -1.000000000000000000, 0.000000000000000000, -0.000000000000000000 ) ) ;
#10251=CIRCLE ( 'NONE', #18036, 27.60000000002759535 ) ;
#10252=VECTOR ( 'NONE', #20179, 1000.000000000000000 ) ;
#10253=EDGE_LOOP ( 'NONE', ( #15922, #3032, #6681, #16329 ) ) ;
#10255=CARTESIAN_POINT ( 'NONE',  ( 19.99999999999999645, -64.79224928664389438, 25.14373648582931864 ) ) ;
#10256=ORIENTED_EDGE ( 'NONE', *, *, #16869, .F. ) ;
#10259=DIRECTION ( 'NONE',  ( 0.000000000000000000, 0.000000000000000000, 1.000000000000000000 ) ) ;
#10261=ORIENTED_EDGE ( 'NONE', *, *, #10532, .F. ) ;
#10263=VERTEX_POINT ( 'NONE', #10065 ) ;
#10264=CARTESIAN_POINT ( 'NONE',  ( 19.99999999999999645, -64.52323195238624010, -6.389157729493822657 ) ) ;
#10265=VECTOR ( 'NONE', #17506, 1000.000000000000000 ) ;
#10276=AXIS2_PLACEMENT_3D ( 'NONE', #6394, #12875, #9686 ) ;
#10277=FACE_OUTER_BOUND ( 'NONE', #8578, .T. ) ;
#10278=DIRECTION ( 'NONE',  ( -1.000000000000000000, 0.000000000000000000, -0.000000000000000000 ) ) ;
#10279=AXIS2_PLACEMENT_3D ( 'NONE', #6361, #8154, #20943 ) ;
#10280=AXIS2_PLACEMENT_3D ( 'NONE', #14050, #12452, #4601 ) ;
#10288=ORIENTED_EDGE ( 'NONE', *, *, #20348, .F. ) ;
#10293=VERTEX_POINT ( 'NONE', #6409 ) ;
#10294=CARTESIAN_POINT ( 'NONE',  ( 19.99999999999999645, -6.872116855662673274, -64.47358224882424338 ) ) ;
#10296=CIRCLE ( 'NONE', #2524, 72.00000000007199219 ) ;
#10300=AXIS2_PLACEMENT_3D ( 'NONE', #245, #1736, #14662 ) ;
#10301=AXIS2_PLACEMENT_3D ( 'NONE', #3934, #11888, #3721 ) ;
#10309=DIRECTION ( 'NONE',  ( -1.000000000000000000, -0.000000000000000000, -0.000000000000000000 ) ) ;
#10316=DIRECTION ( 'NONE',  ( 0.000000000000000000, 0.000000000000000000, 1.000000000000000000 ) ) ;
#10317=CYLINDRICAL_SURFACE ( 'NONE', #263, 27.60000000002759535 ) ;
#10319=COLOUR_RGB ( '', 0.08235294, 0.09019608, 0.10196078) ;
#10320=DIRECTION ( 'NONE',  ( -1.000000000000000000, -0.000000000000000000, 0.000000000000000000 ) ) ;
#10325=ORIENTED_EDGE ( 'NONE', *, *, #2090, .F. ) ;
#10326=DIRECTION ( 'NONE',  ( -1.000000000000000000, 0.000000000000000000, 0.000000000000000000 ) ) ;
#10327=EDGE_LOOP ( 'NONE', ( #11096, #18422, #908, #10787 ) ) ;
#10333=DIRECTION ( 'NONE',  ( 0.000000000000000000, 0.1361666490962466225, -0.9906859460363307557 ) ) ;
#10334=DIRECTION ( 'NONE',  ( -1.000000000000000000, 0.000000000000000000, 0.000000000000000000 ) ) ;
#10336=DIRECTION ( 'NONE',  ( -1.000000000000000000, 0.000000000000000000, 0.000000000000000000 ) ) ;
#10341=DIRECTION ( 'NONE',  ( 0.000000000000000000, 0.000000000000000000, 1.000000000000000000 ) ) ;
#10343=EDGE_LOOP ( 'NONE', ( #2949, #12571, #20021, #14346 ) ) ;
#10358=ORIENTED_EDGE ( 'NONE', *, *, #11250, .F. ) ;
#10359=CYLINDRICAL_SURFACE ( 'NONE', #14782, 72.00000000007199219 ) ;
#10362=ADVANCED_FACE ( 'NONE', ( #4514, #20828 ), #4106, .F. ) ;
#10363=DIRECTION ( 'NONE',  ( -1.000000000000000000, -0.000000000000000000, 0.000000000000000000 ) ) ;
#10364=VERTEX_POINT ( 'NONE', #12800 ) ;
#10371=AXIS2_PLACEMENT_3D ( 'NONE', #14837, #6172, #11346 ) ;
#10373=CYLINDRICAL_SURFACE ( 'NONE', #2265, 72.00000000007199219 ) ;
#10376=CARTESIAN_POINT ( 'NONE',  ( -10.00000000000000000, 0.000000000000000000, 0.000000000000000000 ) ) ;
#10380=LINE ( 'NONE', #2322, #17195 ) ;
#10382=AXIS2_PLACEMENT_3D ( 'NONE', #10397, #5501, #19922 ) ;
#10383=DIRECTION ( 'NONE',  ( -1.000000000000000000, 0.000000000000000000, -0.000000000000000000 ) ) ;
#10384=ADVANCED_FACE ( 'NONE', ( #14178 ), #7905, .T. ) ;
#10385=CIRCLE ( 'NONE', #18855, 27.60000000002760245 ) ;
#10387=DIRECTION ( 'NONE',  ( -1.000000000000000000, -0.000000000000000000, 0.000000000000000000 ) ) ;
#10388=AXIS2_PLACEMENT_3D ( 'NONE', #11318, #1680, #14402 ) ;
#10392=EDGE_CURVE ( 'NONE', #16888, #18949, #20818, .T. ) ;
#10396=FACE_OUTER_BOUND ( 'NONE', #10327, .T. ) ;
#10397=CARTESIAN_POINT ( 'NONE',  ( 19.99999999999999645, 51.81019761368321497, 38.98425606966075918 ) ) ;
#10398=VECTOR ( 'NONE', #11302, 1000.000000000000000 ) ;
#10399=EDGE_CURVE ( 'NONE', #7195, #10684, #2188, .T. ) ;
#10400=ORIENTED_EDGE ( 'NONE', *, *, #976, .F. ) ;
#10404=( NAMED_UNIT ( * ) SI_UNIT ( $, .STERADIAN. ) SOLID_ANGLE_UNIT ( ) );
#10406=DIRECTION ( 'NONE',  ( 0.000000000000000000, 0.000000000000000000, -1.000000000000000000 ) ) ;
#10407=VECTOR ( 'NONE', #13987, 1000.000000000000000 ) ;
#10413=CARTESIAN_POINT ( 'NONE',  ( -65.00002539999999840, 5.400000000000000355, 0.000000000000000000 ) ) ;
#10415=EDGE_CURVE ( 'NONE', #15624, #5352, #8623, .T. ) ;
#10420=CARTESIAN_POINT ( 'NONE',  ( 85.00002539999999840, 0.000000000000000000, 7.500000000000000000 ) ) ;
#10424=ORIENTED_EDGE ( 'NONE', *, *, #12746, .F. ) ;
#10426=CARTESIAN_POINT ( 'NONE',  ( 19.99999999999999645, -49.77519642623978058, -42.18840861821836796 ) ) ;
#10428=EDGE_CURVE ( 'NONE', #19634, #9123, #11674, .T. ) ;
#10430=CARTESIAN_POINT ( 'NONE',  ( 9.999999999999998224, 29.55812890832068973, -65.65300461859658299 ) ) ;
#10436=CARTESIAN_POINT ( 'NONE',  ( 19.99999999999999645, 0.000000000000000000, 0.000000000000000000 ) ) ;
#10445=DIRECTION ( 'NONE',  ( 0.000000000000000000, 0.000000000000000000, -1.000000000000000000 ) ) ;
#10452=CARTESIAN_POINT ( 'NONE',  ( 9.999999999999998224, -70.29359119158496583, 15.58239511117263554 ) ) ;
#10459=DIRECTION ( 'NONE',  ( 0.000000000000000000, 0.000000000000000000, -1.000000000000000000 ) ) ;
#10461=DIRECTION ( 'NONE',  ( -1.000000000000000000, -0.000000000000000000, 0.000000000000000000 ) ) ;
#10471=ORIENTED_EDGE ( 'NONE', *, *, #16708, .T. ) ;
#10474=ORIENTED_EDGE ( 'NONE', *, *, #565, .T. ) ;
#10475=ORIENTED_EDGE ( 'NONE', *, *, #20770, .F. ) ;
#10477=EDGE_CURVE ( 'NONE', #15053, #9908, #16089, .T. ) ;
#10478=LINE ( 'NONE', #13458, #7687 ) ;
#10484=CARTESIAN_POINT ( 'NONE',  ( 0.000000000000000000, 0.000000000000000000, 0.000000000000000000 ) ) ;
#10488=ORIENTED_EDGE ( 'NONE', *, *, #3891, .F. ) ;
#10492=ORIENTED_EDGE ( 'NONE', *, *, #2981, .T. ) ;
#10493=EDGE_CURVE ( 'NONE', #3309, #10217, #4903, .T. ) ;
#10496=CARTESIAN_POINT ( 'NONE',  ( -65.00002539999999840, 9.184850993605147944E-16, 7.500000000000000000 ) ) ;
#10498=VERTEX_POINT ( 'NONE', #6718 ) ;
#10502=CARTESIAN_POINT ( 'NONE',  ( 19.99999999999999645, -51.43306257653114955, -40.15061736769617795 ) ) ;
#10503=DIRECTION ( 'NONE',  ( 0.000000000000000000, 0.000000000000000000, -1.000000000000000000 ) ) ;
#10506=EDGE_CURVE ( 'NONE', #14556, #2235, #516, .T. ) ;
#10511=MANIFOLD_SOLID_BREP ( 'Keyway', #17445 ) ;
#10512=ORIENTED_EDGE ( 'NONE', *, *, #9080, .T. ) ;
#10515=ADVANCED_FACE ( 'NONE', ( #5870 ), #8944, .T. ) ;
#10518=CIRCLE ( 'NONE', #7466, 27.60000000002759180 ) ;
#10521=DIRECTION ( 'NONE',  ( -1.000000000000000000, -0.000000000000000000, 0.000000000000000000 ) ) ;
#10526=VERTEX_POINT ( 'NONE', #5752 ) ;
#10527=CARTESIAN_POINT ( 'NONE',  ( 19.99999999999999645, 58.44960523466241398, 28.06621538408611016 ) ) ;
#10528=EDGE_CURVE ( 'NONE', #16884, #18441, #20135, .T. ) ;
#10529=CARTESIAN_POINT ( 'NONE',  ( 0.000000000000000000, 65.23577793412344761, 1.313498510941937036 ) ) ;
#10531=DIRECTION ( 'NONE',  ( 0.000000000000000000, 0.000000000000000000, 1.000000000000000000 ) ) ;
#10532=EDGE_CURVE ( 'NONE', #15935, #7195, #2895, .T. ) ;
#10534=AXIS2_PLACEMENT_3D ( 'NONE', #2553, #8786, #8588 ) ;
#10536=ORIENTED_EDGE ( 'NONE', *, *, #7927, .F. ) ;
#10537=CARTESIAN_POINT ( 'NONE',  ( 0.000000000000000000, -58.44960523466222213, -28.06621538408651872 ) ) ;
#10538=ADVANCED_FACE ( 'NONE', ( #677 ), #899, .T. ) ;
#10542=EDGE_LOOP ( 'NONE', ( #11686, #8149, #17202, #970 ) ) ;
#10544=DIRECTION ( 'NONE',  ( -1.000000000000000000, 0.000000000000000000, 0.000000000000000000 ) ) ;
#10547=ORIENTED_EDGE ( 'NONE', *, *, #14819, .T. ) ;
#10549=CYLINDRICAL_SURFACE ( 'NONE', #14328, 27.60000000002760245 ) ;
#10553=DIRECTION ( 'NONE',  ( -1.000000000000000000, -0.000000000000000000, -0.000000000000000000 ) ) ;
#10555=CARTESIAN_POINT ( 'NONE',  ( 0.000000000000000000, 36.59093685910629290, 62.00889726308042782 ) ) ;
#10556=DIRECTION ( 'NONE',  ( 0.000000000000000000, 0.000000000000000000, 1.000000000000000000 ) ) ;
#10558=VECTOR ( 'NONE', #3228, 1000.000000000000000 ) ;
#10559=AXIS2_PLACEMENT_3D ( 'NONE', #11460, #4995, #14742 ) ;
#10560=VERTEX_POINT ( 'NONE', #12019 ) ;
#10562=VECTOR ( 'NONE', #19276, 1000.000000000000000 ) ;
#10569=CARTESIAN_POINT ( 'NONE',  ( 19.99999999999999645, 31.17893654894306721, -57.31758819669140337 ) ) ;
#10571=EDGE_CURVE ( 'NONE', #13592, #2919, #17801, .T. ) ;
#10574=CARTESIAN_POINT ( 'NONE',  ( -10.00000000000000000, 0.000000000000000000, 0.000000000000000000 ) ) ;
#10575=AXIS2_PLACEMENT_3D ( 'NONE', #16425, #3905, #5188 ) ;
#10583=DIRECTION ( 'NONE',  ( -1.000000000000000000, -0.000000000000000000, 0.000000000000000000 ) ) ;
#10584=DIRECTION ( 'NONE',  ( 0.000000000000000000, -0.6310879443260593025, 0.7757112907044144690 ) ) ;
#10585=CARTESIAN_POINT ( 'NONE',  ( 0.000000000000000000, 64.80702306891096498, 7.581672767546657532 ) ) ;
#10590=DIRECTION ( 'NONE',  ( 1.000000000000000000, 0.000000000000000000, 0.000000000000000000 ) ) ;
#10594=AXIS2_PLACEMENT_3D ( 'NONE', #14719, #18390, #8347 ) ;
#10596=AXIS2_PLACEMENT_3D ( 'NONE', #2982, #6147, #979 ) ;
#10597=AXIS2_PLACEMENT_3D ( 'NONE', #8746, #692, #5557 ) ;
#10606=FACE_OUTER_BOUND ( 'NONE', #18210, .T. ) ;
#10611=VERTEX_POINT ( 'NONE', #9470 ) ;
#10612=EDGE_CURVE ( 'NONE', #12045, #17518, #20485, .T. ) ;
#10617=SURFACE_STYLE_USAGE ( .BOTH. , #11987 ) ;
#10620=VECTOR ( 'NONE', #17749, 1000.000000000000000 ) ;
#10621=AXIS2_PLACEMENT_3D ( 'NONE', #13127, #5150, #11326 ) ;
#10627=AXIS2_PLACEMENT_3D ( 'NONE', #1524, #16135, #1630 ) ;
#10629=CARTESIAN_POINT ( 'NONE',  ( 19.99999999999999645, -28.84646472442495480, 58.52617768068423487 ) ) ;
#10635=CARTESIAN_POINT ( 'NONE',  ( 0.000000000000000000, 48.70996102988680576, 42.79495875147792106 ) ) ;
#10638=CYLINDRICAL_SURFACE ( 'NONE', #16277, 27.60000000002759890 ) ;
#10643=AXIS2_PLACEMENT_3D ( 'NONE', #15220, #20086, #10459 ) ;
#10644=EDGE_CURVE ( 'NONE', #1747, #17144, #14415, .T. ) ;
#10645=EDGE_CURVE ( 'NONE', #7485, #7828, #7673, .T. ) ;
#10650=DIRECTION ( 'NONE',  ( -1.000000000000000000, 0.000000000000000000, 0.000000000000000000 ) ) ;
#10653=ORIENTED_EDGE ( 'NONE', *, *, #4929, .T. ) ;
#10655=ORIENTED_EDGE ( 'NONE', *, *, #19776, .T. ) ;
#10656=CIRCLE ( 'NONE', #2478, 27.60000000002759890 ) ;
#10658=VERTEX_POINT ( 'NONE', #9571 ) ;
#10660=DIRECTION ( 'NONE',  ( -1.000000000000000000, 0.000000000000000000, -0.000000000000000000 ) ) ;
#10662=ORIENTED_EDGE ( 'NONE', *, *, #2705, .T. ) ;
#10663=EDGE_CURVE ( 'NONE', #10885, #7362, #14361, .T. ) ;
#10664=CARTESIAN_POINT ( 'NONE',  ( 19.99999999999999645, 0.000000000000000000, 0.000000000000000000 ) ) ;
#10667=DIRECTION ( 'NONE',  ( -1.000000000000000000, 0.000000000000000000, 0.000000000000000000 ) ) ;
#10669=EDGE_CURVE ( 'NONE', #12643, #12564, #13046, .T. ) ;
#10678=VERTEX_POINT ( 'NONE', #4383 ) ;
#10682=LINE ( 'NONE', #13963, #551 ) ;
#10683=EDGE_CURVE ( 'NONE', #17979, #3309, #17319, .T. ) ;
#10684=VERTEX_POINT ( 'NONE', #2795 ) ;
#10694=VERTEX_POINT ( 'NONE', #4488 ) ;
#10695=VERTEX_POINT ( 'NONE', #10957 ) ;
#10696=DIRECTION ( 'NONE',  ( -1.000000000000000000, 0.000000000000000000, -0.000000000000000000 ) ) ;
#10697=DIRECTION ( 'NONE',  ( -1.000000000000000000, -0.000000000000000000, -0.000000000000000000 ) ) ;
#10699=LINE ( 'NONE', #5587, #6507 ) ;
#10701=EDGE_CURVE ( 'NONE', #14496, #11746, #15834, .T. ) ;
#10709=CARTESIAN_POINT ( 'NONE',  ( 9.999999999999998224, 70.68211945903188109, 13.71269443944232336 ) ) ;
#10710=ORIENTED_EDGE ( 'NONE', *, *, #6223, .F. ) ;
#10711=DIRECTION ( 'NONE',  ( -1.000000000000000000, 0.000000000000000000, -0.000000000000000000 ) ) ;
#10713=CARTESIAN_POINT ( 'NONE',  ( 19.99999999999999645, 0.000000000000000000, 0.000000000000000000 ) ) ;
#10724=AXIS2_PLACEMENT_3D ( 'NONE', #15699, #7532, #15493 ) ;
#10726=LINE ( 'NONE', #2668, #10265 ) ;
#10728=ADVANCED_FACE ( 'NONE', ( #1733 ), #17944, .T. ) ;
#10730=DIRECTION ( 'NONE',  ( 1.000000000000000000, 0.000000000000000000, 0.000000000000000000 ) ) ;
#10733=CARTESIAN_POINT ( 'NONE',  ( 19.99999999999999645, 0.000000000000000000, 0.000000000000000000 ) ) ;
#10735=AXIS2_PLACEMENT_3D ( 'NONE', #1975, #5741, #13919 ) ;
#10736=ORIENTED_EDGE ( 'NONE', *, *, #18842, .T. ) ;
#10739=VERTEX_POINT ( 'NONE', #6696 ) ;
#10743=CARTESIAN_POINT ( 'NONE',  ( 0.000000000000000000, -63.48283426024829623, -33.96954156735433372 ) ) ;
#10745=FACE_OUTER_BOUND ( 'NONE', #4763, .T. ) ;
#10747=CIRCLE ( 'NONE', #4988, 65.24900000006526568 ) ;
#10748=ORIENTED_EDGE ( 'NONE', *, *, #17964, .T. ) ;
#10749=CARTESIAN_POINT ( 'NONE',  ( 19.99999999999999645, 15.58726123847851142, 62.93731870009410301 ) ) ;
#10750=AXIS2_PLACEMENT_3D ( 'NONE', #284, #1875, #11616 ) ;
#10751=LINE ( 'NONE', #2475, #19853 ) ;
#10753=CARTESIAN_POINT ( 'NONE',  ( 19.99999999999999645, -61.72688495901601158, -19.84591825364075746 ) ) ;
#10754=VECTOR ( 'NONE', #6828, 1000.000000000000000 ) ;
#10755=AXIS2_PLACEMENT_3D ( 'NONE', #6874, #15363, #7300 ) ;
#10756=DIRECTION ( 'NONE',  ( 0.000000000000000000, -0.1361666490962539222, 0.9906859460363298675 ) ) ;
#10758=SURFACE_STYLE_FILL_AREA ( #17219 ) ;
#10759=DIRECTION ( 'NONE',  ( -1.000000000000000000, 0.000000000000000000, 0.000000000000000000 ) ) ;
#10765=ORIENTED_EDGE ( 'NONE', *, *, #11033, .T. ) ;
#10767=DIRECTION ( 'NONE',  ( 1.000000000000000000, 0.000000000000000000, 0.000000000000000000 ) ) ;
#10769=ORIENTED_EDGE ( 'NONE', *, *, #1555, .F. ) ;
#10770=CYLINDRICAL_SURFACE ( 'NONE', #8207, 65.24900000006525147 ) ;
#10771=ORIENTED_EDGE ( 'NONE', *, *, #2103, .F. ) ;
#10779=CARTESIAN_POINT ( 'NONE',  ( 9.999999999999998224, -20.34307325858833337, 69.06634035770301239 ) ) ;
#10786=LINE ( 'NONE', #15539, #7993 ) ;
#10787=ORIENTED_EDGE ( 'NONE', *, *, #10571, .T. ) ;
#10789=CYLINDRICAL_SURFACE ( 'NONE', #6991, 27.60000000002759890 ) ;
#10791=VECTOR ( 'NONE', #4463, 1000.000000000000000 ) ;
#10796=ORIENTED_EDGE ( 'NONE', *, *, #3873, .F. ) ;
#10797=FACE_OUTER_BOUND ( 'NONE', #13212, .T. ) ;
#10799=CARTESIAN_POINT ( 'NONE',  ( 19.99999999999999645, 55.05624179292029652, -35.01774179823726740 ) ) ;
#10802=EDGE_CURVE ( 'NONE', #16683, #9551, #4594, .T. ) ;
#10810=FACE_OUTER_BOUND ( 'NONE', #7189, .T. ) ;
#10811=ORIENTED_EDGE ( 'NONE', *, *, #14519, .F. ) ;
#10814=DIRECTION ( 'NONE',  ( -1.000000000000000000, -0.000000000000000000, -0.000000000000000000 ) ) ;
#10816=CARTESIAN_POINT ( 'NONE',  ( -10.00000000000000000, 0.000000000000000000, 0.000000000000000000 ) ) ;
#10820=ORIENTED_EDGE ( 'NONE', *, *, #962, .T. ) ;
#10821=ORIENTED_EDGE ( 'NONE', *, *, #20770, .T. ) ;
#10822=DIRECTION ( 'NONE',  ( -1.000000000000000000, 0.000000000000000000, 0.000000000000000000 ) ) ;
#10823=FACE_OUTER_BOUND ( 'NONE', #5497, .T. ) ;
#10827=CARTESIAN_POINT ( 'NONE',  ( 0.000000000000000000, 9.184850993605147944E-16, 7.500000000000000000 ) ) ;
#10829=AXIS2_PLACEMENT_3D ( 'NONE', #17771, #13308, #1860 ) ;
#10835=ORIENTED_EDGE ( 'NONE', *, *, #16284, .T. ) ;
#10844=DIRECTION ( 'NONE',  ( 0.000000000000000000, 0.000000000000000000, 1.000000000000000000 ) ) ;
#10847=AXIS2_PLACEMENT_3D ( 'NONE', #14633, #6673, #5080 ) ;
#10851=CARTESIAN_POINT ( 'NONE',  ( 19.99999999999999645, 0.000000000000000000, 0.000000000000000000 ) ) ;
#10856=ORIENTED_EDGE ( 'NONE', *, *, #11530, .T. ) ;
#10858=DIRECTION ( 'NONE',  ( 0.000000000000000000, 0.000000000000000000, 1.000000000000000000 ) ) ;
#10861=DIRECTION ( 'NONE',  ( -1.000000000000000000, 0.000000000000000000, 0.000000000000000000 ) ) ;
#10862=ORIENTED_EDGE ( 'NONE', *, *, #16574, .T. ) ;
#10865=AXIS2_PLACEMENT_3D ( 'NONE', #6612, #19556, #5032 ) ;
#10866=ORIENTED_EDGE ( 'NONE', *, *, #653, .F. ) ;
#10867=AXIS2_PLACEMENT_3D ( 'NONE', #4045, #13918, #10316 ) ;
#10869=EDGE_CURVE ( 'NONE', #714, #10217, #1217, .T. ) ;
#10870=LINE ( 'NONE', #14267, #16024 ) ;
#10873=DIRECTION ( 'NONE',  ( 0.000000000000000000, -7.039457583666960603E-15, 1.000000000000000000 ) ) ;
#10875=CARTESIAN_POINT ( 'NONE',  ( 0.000000000000000000, -62.46228066917801414, 18.86519267363435048 ) ) ;
#10876=VECTOR ( 'NONE', #1434, 1000.000000000000000 ) ;
#10880=DIRECTION ( 'NONE',  ( -1.000000000000000000, 0.000000000000000000, 0.000000000000000000 ) ) ;
#10883=CARTESIAN_POINT ( 'NONE',  ( -10.00000000000000000, 0.000000000000000000, 0.000000000000000000 ) ) ;
#10885=VERTEX_POINT ( 'NONE', #6068 ) ;
#10887=DIRECTION ( 'NONE',  ( -1.000000000000000000, -0.000000000000000000, 0.000000000000000000 ) ) ;
#10891=CARTESIAN_POINT ( 'NONE',  ( 19.99999999999999645, 60.40676135667438729, 23.56039007469059143 ) ) ;
#10896=CARTESIAN_POINT ( 'NONE',  ( 19.99999999999999645, -31.98952867950364265, 56.39803944231574206 ) ) ;
#10901=EDGE_CURVE ( 'NONE', #14245, #10263, #1559, .T. ) ;
#10902=ORIENTED_EDGE ( 'NONE', *, *, #19809, .T. ) ;
#10906=VERTEX_POINT ( 'NONE', #12642 ) ;
#10907=DIRECTION ( 'NONE',  ( 0.000000000000000000, 0.000000000000000000, 1.000000000000000000 ) ) ;
#10910=CIRCLE ( 'NONE', #4119, 65.24900000006526568 ) ;
#10913=DIRECTION ( 'NONE',  ( -1.000000000000000000, -0.000000000000000000, 0.000000000000000000 ) ) ;
#10914=ORIENTED_EDGE ( 'NONE', *, *, #3080, .T. ) ;
#10920=EDGE_CURVE ( 'NONE', #12091, #8697, #18897, .T. ) ;
#10922=DIRECTION ( 'NONE',  ( 0.000000000000000000, 0.9422609221188213979, -0.3348796121709836093 ) ) ;
#10924=AXIS2_PLACEMENT_3D ( 'NONE', #16799, #688, #10445 ) ;
#10926=AXIS2_PLACEMENT_3D ( 'NONE', #2716, #17351, #20416 ) ;
#10927=AXIS2_PLACEMENT_3D ( 'NONE', #16694, #8635, #11921 ) ;
#10929=CYLINDRICAL_SURFACE ( 'NONE', #18679, 27.60000000002760245 ) ;
#10935=VERTEX_POINT ( 'NONE', #20670 ) ;
#10938=CIRCLE ( 'NONE', #454, 27.60000000002759890 ) ;
#10939=ORIENTED_EDGE ( 'NONE', *, *, #799, .T. ) ;
#10944=CARTESIAN_POINT ( 'NONE',  ( 0.000000000000000000, 0.000000000000000000, 0.000000000000000000 ) ) ;
#10945=CARTESIAN_POINT ( 'NONE',  ( 19.99999999999999645, 70.29359119158485214, 15.58239511117312226 ) ) ;
#10946=VERTEX_POINT ( 'NONE', #6053 ) ;
#10948=AXIS2_PLACEMENT_3D ( 'NONE', #18881, #4352, #4561 ) ;
#10949=CARTESIAN_POINT ( 'NONE',  ( 19.99999999999999645, 31.17893654894306721, -57.31758819669140337 ) ) ;
#10954=AXIS2_PLACEMENT_3D ( 'NONE', #1220, #15832, #7669 ) ;
#10955=CIRCLE ( 'NONE', #16043, 72.00000000007199219 ) ;
#10956=EDGE_LOOP ( 'NONE', ( #10151, #16459, #11459, #9897 ) ) ;
#10957=CARTESIAN_POINT ( 'NONE',  ( 0.000000000000000000, -36.54710069451017063, -54.05313526368150434 ) ) ;
#10959=DIRECTION ( 'NONE',  ( 0.000000000000000000, 0.000000000000000000, 1.000000000000000000 ) ) ;
#10962=CARTESIAN_POINT ( 'NONE',  ( 0.000000000000000000, 0.000000000000000000, 0.000000000000000000 ) ) ;
#10965=DIRECTION ( 'NONE',  ( 0.000000000000000000, 0.000000000000000000, 1.000000000000000000 ) ) ;
#10967=AXIS2_PLACEMENT_3D ( 'NONE', #16656, #8603, #13492 ) ;
#10969=VECTOR ( 'NONE', #12915, 1000.000000000000000 ) ;
#10975=DIRECTION ( 'NONE',  ( 0.000000000000000000, 0.000000000000000000, -1.000000000000000000 ) ) ;
#10982=LINE ( 'NONE', #15860, #17061 ) ;
#10989=LINE ( 'NONE', #18947, #17517 ) ;
#10998=CARTESIAN_POINT ( 'NONE',  ( 19.99999999999999645, 0.000000000000000000, 0.000000000000000000 ) ) ;
#10999=FACE_OUTER_BOUND ( 'NONE', #13050, .T. ) ;
#11000=DIRECTION ( 'NONE',  ( 1.000000000000000000, 0.000000000000000000, 0.000000000000000000 ) ) ;
#11005=ORIENTED_EDGE ( 'NONE', *, *, #17189, .T. ) ;
#11008=DIRECTION ( 'NONE',  ( -1.000000000000000000, 0.000000000000000000, 0.000000000000000000 ) ) ;
#11012=PLANE ( 'NONE',  #6184 ) ;
#11015=CARTESIAN_POINT ( 'NONE',  ( 19.99999999999999645, -59.36728637278046250, 40.73727173906767973 ) ) ;
#11019=ORIENTED_EDGE ( 'NONE', *, *, #5565, .T. ) ;
#11024=ORIENTED_EDGE ( 'NONE', *, *, #5354, .F. ) ;
#11025=CARTESIAN_POINT ( 'NONE',  ( 19.99999999999999645, -31.17893654894190902, -57.31758819669202865 ) ) ;
#11031=CARTESIAN_POINT ( 'NONE',  ( 0.000000000000000000, -63.85430960833482317, -11.25592921604904539 ) ) ;
#11033=EDGE_CURVE ( 'NONE', #4233, #15895, #17086, .T. ) ;
#11036=CYLINDRICAL_SURFACE ( 'NONE', #15444, 27.60000000002759890 ) ;
#11041=FACE_OUTER_BOUND ( 'NONE', #689, .T. ) ;
#11043=EDGE_CURVE ( 'NONE', #2557, #2098, #12424, .T. ) ;
#11044=ORIENTED_EDGE ( 'NONE', *, *, #16591, .T. ) ;
#11048=DIRECTION ( 'NONE',  ( -1.000000000000000000, -0.000000000000000000, -0.000000000000000000 ) ) ;
#11049=CIRCLE ( 'NONE', #19497, 72.00000000007199219 ) ;
#11051=AXIS2_PLACEMENT_3D ( 'NONE', #13361, #10278, #10073 ) ;
#11056=VERTEX_POINT ( 'NONE', #9133 ) ;
#11057=DIRECTION ( 'NONE',  ( 0.000000000000000000, 0.9422609221188191775, 0.3348796121709899376 ) ) ;
#11058=AXIS2_PLACEMENT_3D ( 'NONE', #6380, #19116, #4694 ) ;
#11064=EDGE_CURVE ( 'NONE', #8436, #3519, #2238, .T. ) ;
#11066=ADVANCED_FACE ( 'NONE', ( #8266 ), #9852, .T. ) ;
#11068=CIRCLE ( 'NONE', #7672, 72.00000000007199219 ) ;
#11069=EDGE_CURVE ( 'NONE', #1553, #15627, #9335, .T. ) ;
#11070=CARTESIAN_POINT ( 'NONE',  ( 19.99999999999999645, 36.54710069451054011, 54.05313526368126276 ) ) ;
#11078=VECTOR ( 'NONE', #972, 1000.000000000000000 ) ;
#11079=DIRECTION ( 'NONE',  ( -1.000000000000000000, -0.000000000000000000, -0.000000000000000000 ) ) ;
#11080=CARTESIAN_POINT ( 'NONE',  ( 19.99999999999999645, 0.000000000000000000, 0.000000000000000000 ) ) ;
#11081=ORIENTED_EDGE ( 'NONE', *, *, #5311, .T. ) ;
#11090=CYLINDRICAL_SURFACE ( 'NONE', #9593, 27.60000000002760245 ) ;
#11096=ORIENTED_EDGE ( 'NONE', *, *, #6726, .T. ) ;
#11097=DIRECTION ( 'NONE',  ( -1.000000000000000000, 0.000000000000000000, -0.000000000000000000 ) ) ;
#11100=CARTESIAN_POINT ( 'NONE',  ( 0.000000000000000000, -49.77519642624037743, 42.18840861821767874 ) ) ;
#11102=LINE ( 'NONE', #8024, #12793 ) ;
#11104=ORIENTED_EDGE ( 'NONE', *, *, #13351, .T. ) ;
#11106=EDGE_CURVE ( 'NONE', #12251, #273, #3569, .T. ) ;
#11109=ADVANCED_FACE ( 'NONE', ( #1813 ), #14336, .T. ) ;
#11110=AXIS2_PLACEMENT_3D ( 'NONE', #18911, #5746, #19006 ) ;
#11113=DIRECTION ( 'NONE',  ( 0.000000000000000000, -0.9976687691905385957, -0.06824241336468162000 ) ) ;
#11117=ORIENTED_EDGE ( 'NONE', *, *, #13247, .F. ) ;
#11118=LINE ( 'NONE', #16199, #14148 ) ;
#11124=CARTESIAN_POINT ( 'NONE',  ( 19.99999999999999645, 0.000000000000000000, 0.000000000000000000 ) ) ;
#11125=ORIENTED_EDGE ( 'NONE', *, *, #17128, .F. ) ;
#11127=ORIENTED_EDGE ( 'NONE', *, *, #7546, .F. ) ;
#11129=DIRECTION ( 'NONE',  ( -1.000000000000000000, 0.000000000000000000, -0.000000000000000000 ) ) ;
#11134=DIRECTION ( 'NONE',  ( -1.000000000000000000, 0.000000000000000000, -0.000000000000000000 ) ) ;
#11136=EDGE_CURVE ( 'NONE', #3825, #15895, #7296, .T. ) ;
#11137=DIRECTION ( 'NONE',  ( 0.000000000000000000, 0.000000000000000000, 1.000000000000000000 ) ) ;
#11141=CARTESIAN_POINT ( 'NONE',  ( 19.99999999999999645, 18.50424539729942808, -69.58155576219097327 ) ) ;
#11145=DIRECTION ( 'NONE',  ( 0.000000000000000000, 0.000000000000000000, -1.000000000000000000 ) ) ;
#11149=ORIENTED_EDGE ( 'NONE', *, *, #2866, .T. ) ;
#11153=FACE_OUTER_BOUND ( 'NONE', #14960, .T. ) ;
#11156=ORIENTED_EDGE ( 'NONE', *, *, #16824, .T. ) ;
#11157=CYLINDRICAL_SURFACE ( 'NONE', #2232, 65.24900000006525147 ) ;
#11159=DIRECTION ( 'NONE',  ( 0.000000000000000000, 0.000000000000000000, -1.000000000000000000 ) ) ;
#11163=VERTEX_POINT ( 'NONE', #17612 ) ;
#11170=DIRECTION ( 'NONE',  ( -1.000000000000000000, 0.000000000000000000, 0.000000000000000000 ) ) ;
#11171=ORIENTED_EDGE ( 'NONE', *, *, #11136, .F. ) ;
#11173=DIRECTION ( 'NONE',  ( -1.000000000000000000, -0.000000000000000000, 0.000000000000000000 ) ) ;
#11174=DIRECTION ( 'NONE',  ( -1.000000000000000000, 0.000000000000000000, 0.000000000000000000 ) ) ;
#11182=CYLINDRICAL_SURFACE ( 'NONE', #13802, 72.00000000007199219 ) ;
#11183=EDGE_CURVE ( 'NONE', #17307, #1684, #10010, .T. ) ;
#11184=LINE ( 'NONE', #20823, #17376 ) ;
#11192=ORIENTED_EDGE ( 'NONE', *, *, #8305, .F. ) ;
#11196=CARTESIAN_POINT ( 'NONE',  ( 19.99999999999999645, -27.62776854598897813, 58.65812137498992485 ) ) ;
#11197=ORIENTED_EDGE ( 'NONE', *, *, #19095, .F. ) ;
#11205=LINE ( 'NONE', #11414, #18826 ) ;
#11207=ORIENTED_EDGE ( 'NONE', *, *, #19552, .F. ) ;
#11210=DIRECTION ( 'NONE',  ( -1.000000000000000000, -0.000000000000000000, 0.000000000000000000 ) ) ;
#11215=DIRECTION ( 'NONE',  ( 0.000000000000000000, 0.000000000000000000, 1.000000000000000000 ) ) ;
#11217=EDGE_CURVE ( 'NONE', #2782, #6278, #10786, .T. ) ;
#11219=CIRCLE ( 'NONE', #4109, 72.00000000007199219 ) ;
#11221=CARTESIAN_POINT ( 'NONE',  ( 19.99999999999999645, 56.42118728228200553, -32.77318456705383198 ) ) ;
#11225=AXIS2_PLACEMENT_3D ( 'NONE', #12309, #1304, #11137 ) ;
#11229=FACE_OUTER_BOUND ( 'NONE', #19015, .T. ) ;
#11230=DIRECTION ( 'NONE',  ( 1.000000000000000000, 0.000000000000000000, 0.000000000000000000 ) ) ;
#11240=EDGE_CURVE ( 'NONE', #5613, #9780, #10682, .T. ) ;
#11244=ORIENTED_EDGE ( 'NONE', *, *, #20628, .F. ) ;
#11245=DIRECTION ( 'NONE',  ( -1.000000000000000000, -0.000000000000000000, -0.000000000000000000 ) ) ;
#11246=ORIENTED_EDGE ( 'NONE', *, *, #9237, .F. ) ;
#11248=CARTESIAN_POINT ( 'NONE',  ( 19.99999999999999645, 20.60847369612982405, 61.90898814327722732 ) ) ;
#11250=EDGE_CURVE ( 'NONE', #18356, #19780, #2015, .T. ) ;
#11252=ORIENTED_EDGE ( 'NONE', *, *, #12887, .F. ) ;
#11253=LINE ( 'NONE', #1720, #2741 ) ;
#11255=ORIENTED_EDGE ( 'NONE', *, *, #16340, .T. ) ;
#11261=AXIS2_PLACEMENT_3D ( 'NONE', #12907, #19462, #20729 ) ;
#11262=DIRECTION ( 'NONE',  ( 1.000000000000000000, -0.000000000000000000, 0.000000000000000000 ) ) ;
#11266=ORIENTED_EDGE ( 'NONE', *, *, #16284, .F. ) ;
#11271=DIRECTION ( 'NONE',  ( -1.000000000000000000, 0.000000000000000000, 0.000000000000000000 ) ) ;
#11274=DIRECTION ( 'NONE',  ( 0.000000000000000000, 0.8169698930104392076, 0.5766803221148710801 ) ) ;
#11280=DIRECTION ( 'NONE',  ( 0.000000000000000000, 0.000000000000000000, 1.000000000000000000 ) ) ;
#11282=DIRECTION ( 'NONE',  ( -1.000000000000000000, 0.000000000000000000, 0.000000000000000000 ) ) ;
#11283=EDGE_CURVE ( 'NONE', #17758, #16351, #18127, .T. ) ;
#11284=CIRCLE ( 'NONE', #8231, 65.24900000006525147 ) ;
#11285=EDGE_LOOP ( 'NONE', ( #250, #19985, #19229, #563 ) ) ;
#11286=EDGE_CURVE ( 'NONE', #12603, #11771, #20514, .T. ) ;
#11287=DIRECTION ( 'NONE',  ( 0.000000000000000000, 0.9976687691905394839, -0.06824241336466757568 ) ) ;
#11292=EDGE_LOOP ( 'NONE', ( #15858, #1201, #15208, #2315 ) ) ;
#11296=CIRCLE ( 'NONE', #4532, 27.60000000002759890 ) ;
#11300=AXIS2_PLACEMENT_3D ( 'NONE', #4284, #12779, #9159 ) ;
#11302=DIRECTION ( 'NONE',  ( -1.000000000000000000, 0.000000000000000000, 0.000000000000000000 ) ) ;
#11304=CIRCLE ( 'NONE', #805, 72.00000000007199219 ) ;
#11306=ADVANCED_FACE ( 'NONE', ( #5903 ), #8373, .T. ) ;
#11307=ORIENTED_EDGE ( 'NONE', *, *, #653, .T. ) ;
#11311=EDGE_LOOP ( 'NONE', ( #14167, #9119, #15190, #19542 ) ) ;
#11314=EDGE_CURVE ( 'NONE', #16060, #14491, #19839, .T. ) ;
#11318=CARTESIAN_POINT ( 'NONE',  ( 19.99999999999999645, -61.72688495901601158, -19.84591825364075746 ) ) ;
#11320=DIRECTION ( 'NONE',  ( -1.000000000000000000, 0.000000000000000000, -0.000000000000000000 ) ) ;
#11325=AXIS2_PLACEMENT_3D ( 'NONE', #9139, #2777, #2884 ) ;
#11326=DIRECTION ( 'NONE',  ( -0.000000000000000000, 0.000000000000000000, 1.000000000000000000 ) ) ;
#11332=DIRECTION ( 'NONE',  ( 1.000000000000000000, 0.000000000000000000, -0.000000000000000000 ) ) ;
#11335=DIRECTION ( 'NONE',  ( -1.000000000000000000, 0.000000000000000000, 0.000000000000000000 ) ) ;
#11336=VERTEX_POINT ( 'NONE', #18732 ) ;
#11338=VERTEX_POINT ( 'NONE', #8464 ) ;
#11344=CARTESIAN_POINT ( 'NONE',  ( 9.999999999999998224, -10.74906464462166866, 71.19310085447965264 ) ) ;
#11346=DIRECTION ( 'NONE',  ( 0.000000000000000000, 0.000000000000000000, 1.000000000000000000 ) ) ;
#11360=ORIENTED_EDGE ( 'NONE', *, *, #12738, .F. ) ;
#11365=VECTOR ( 'NONE', #14901, 1000.000000000000000 ) ;
#11368=DIRECTION ( 'NONE',  ( -1.000000000000000000, 0.000000000000000000, -0.000000000000000000 ) ) ;
#11371=EDGE_CURVE ( 'NONE', #7828, #3309, #9701, .T. ) ;
#11372=CYLINDRICAL_SURFACE ( 'NONE', #1530, 27.60000000002759890 ) ;
#11377=DIRECTION ( 'NONE',  ( 0.000000000000000000, 0.000000000000000000, 1.000000000000000000 ) ) ;
#11378=CARTESIAN_POINT ( 'NONE',  ( -65.00002539999999840, 0.000000000000000000, -7.500000000000000000 ) ) ;
#11382=EDGE_LOOP ( 'NONE', ( #16864, #15846, #4865, #14890 ) ) ;
#11386=ORIENTED_EDGE ( 'NONE', *, *, #9885, .T. ) ;
#11387=DIRECTION ( 'NONE',  ( 0.000000000000000000, 0.000000000000000000, 1.000000000000000000 ) ) ;
#11389=CARTESIAN_POINT ( 'NONE',  ( -10.00000000000000000, 0.000000000000000000, 72.00000000007199219 ) ) ;
#11390=ORIENTED_EDGE ( 'NONE', *, *, #11069, .F. ) ;
#11391=AXIS2_PLACEMENT_3D ( 'NONE', #20133, #5614, #17188 ) ;
#11396=ADVANCED_FACE ( 'NONE', ( #18231 ), #11656, .T. ) ;
#11397=ORIENTED_EDGE ( 'NONE', *, *, #3140, .T. ) ;
#11399=DIRECTION ( 'NONE',  ( -1.000000000000000000, -0.000000000000000000, -0.000000000000000000 ) ) ;
#11402=AXIS2_PLACEMENT_3D ( 'NONE', #16523, #3997, #3892 ) ;
#11403=AXIS2_PLACEMENT_3D ( 'NONE', #5480, #11954, #16836 ) ;
#11405=DIRECTION ( 'NONE',  ( 0.000000000000000000, 0.000000000000000000, 1.000000000000000000 ) ) ;
#11409=VERTEX_POINT ( 'NONE', #14279 ) ;
#11414=CARTESIAN_POINT ( 'NONE',  ( 19.99999999999999645, -23.08379033237309841, -61.02926039941459635 ) ) ;
#11420=VECTOR ( 'NONE', #1270, 1000.000000000000000 ) ;
#11424=EDGE_CURVE ( 'NONE', #17144, #5709, #15756, .T. ) ;
#11427=AXIS2_PLACEMENT_3D ( 'NONE', #4390, #17753, #6295 ) ;
#11428=EDGE_CURVE ( 'NONE', #15524, #18653, #9022, .T. ) ;
#11433=ADVANCED_FACE ( 'NONE', ( #19251 ), #1257, .T. ) ;
#11434=AXIS2_PLACEMENT_3D ( 'NONE', #6419, #12810, #1950 ) ;
#11436=CARTESIAN_POINT ( 'NONE',  ( 9.999999999999998224, -53.26727847779503833, -48.44168704307686113 ) ) ;
#11438=DIRECTION ( 'NONE',  ( 1.000000000000000000, -0.000000000000000000, 0.000000000000000000 ) ) ;
#11442=CIRCLE ( 'NONE', #17879, 65.24900000006525147 ) ;
#11443=VERTEX_POINT ( 'NONE', #3039 ) ;
#11444=FACE_OUTER_BOUND ( 'NONE', #16829, .T. ) ;
#11449=CARTESIAN_POINT ( 'NONE',  ( 0.000000000000000000, 0.000000000000000000, 0.000000000000000000 ) ) ;
#11459=ORIENTED_EDGE ( 'NONE', *, *, #16212, .T. ) ;
#11460=CARTESIAN_POINT ( 'NONE',  ( 19.99999999999999645, 0.000000000000000000, 0.000000000000000000 ) ) ;
#11462=CARTESIAN_POINT ( 'NONE',  ( 19.99999999999999645, 63.85430960833490843, -11.25592921604860663 ) ) ;
#11465=VERTEX_POINT ( 'NONE', #11100 ) ;
#11466=CARTESIAN_POINT ( 'NONE',  ( 0.000000000000000000, -29.55812890832026341, 65.65300461859676773 ) ) ;
#11468=VERTEX_POINT ( 'NONE', #9186 ) ;
#11469=ORIENTED_EDGE ( 'NONE', *, *, #13687, .F. ) ;
#11472=DIRECTION ( 'NONE',  ( -1.000000000000000000, 0.000000000000000000, 0.000000000000000000 ) ) ;
#11475=DIRECTION ( 'NONE',  ( -1.000000000000000000, 0.000000000000000000, -0.000000000000000000 ) ) ;
#11477=CARTESIAN_POINT ( 'NONE',  ( 19.99999999999999645, 64.52323195238639642, -6.389157729492497495 ) ) ;
#11479=EDGE_CURVE ( 'NONE', #9276, #19491, #14116, .T. ) ;
#11480=CARTESIAN_POINT ( 'NONE',  ( 0.000000000000000000, 0.000000000000000000, 0.000000000000000000 ) ) ;
#11483=DIRECTION ( 'NONE',  ( -1.000000000000000000, 0.000000000000000000, 0.000000000000000000 ) ) ;
#11484=ORIENTED_EDGE ( 'NONE', *, *, #2742, .T. ) ;
#11487=DIRECTION ( 'NONE',  ( -1.000000000000000000, -0.000000000000000000, -0.000000000000000000 ) ) ;
#11489=CARTESIAN_POINT ( 'NONE',  ( 19.99999999999999645, -51.43306257653114955, -40.15061736769617795 ) ) ;
#11490=CARTESIAN_POINT ( 'NONE',  ( -10.00000000000000000, 0.000000000000000000, 0.000000000000000000 ) ) ;
#11493=DIRECTION ( 'NONE',  ( 0.000000000000000000, 0.9790840876823220240, 0.2034560130526375243 ) ) ;
#11499=DIRECTION ( 'NONE',  ( 0.000000000000000000, 0.000000000000000000, 1.000000000000000000 ) ) ;
#11501=ORIENTED_EDGE ( 'NONE', *, *, #10612, .F. ) ;
#11503=ORIENTED_EDGE ( 'NONE', *, *, #9111, .F. ) ;
#11506=CYLINDRICAL_SURFACE ( 'NONE', #12737, 65.24900000006525147 ) ;
#11515=DIRECTION ( 'NONE',  ( -1.000000000000000000, 0.000000000000000000, 0.000000000000000000 ) ) ;
#11521=CARTESIAN_POINT ( 'NONE',  ( 19.99999999999999645, 51.43306257653143376, 40.15061736769582268 ) ) ;
#11524=ORIENTED_EDGE ( 'NONE', *, *, #1261, .F. ) ;
#11526=CARTESIAN_POINT ( 'NONE',  ( 19.99999999999999645, -29.55812890832025985, 65.65300461859676773 ) ) ;
#11527=ORIENTED_EDGE ( 'NONE', *, *, #380, .F. ) ;
#11530=EDGE_CURVE ( 'NONE', #12115, #18900, #1145, .T. ) ;
#11536=DIRECTION ( 'NONE',  ( -1.000000000000000000, 0.000000000000000000, 0.000000000000000000 ) ) ;
#11539=CARTESIAN_POINT ( 'NONE',  ( 19.99999999999999645, 0.000000000000000000, 0.000000000000000000 ) ) ;
#11546=AXIS2_PLACEMENT_3D ( 'NONE', #7076, #13555, #20225 ) ;
#11553=AXIS2_PLACEMENT_3D ( 'NONE', #15035, #13546, #5688 ) ;
#11556=CYLINDRICAL_SURFACE ( 'NONE', #2828, 65.24900000006525147 ) ;
#11557=VERTEX_POINT ( 'NONE', #20625 ) ;
#11561=ORIENTED_EDGE ( 'NONE', *, *, #16113, .T. ) ;
#11563=ORIENTED_EDGE ( 'NONE', *, *, #15706, .T. ) ;
#11566=DIRECTION ( 'NONE',  ( 0.000000000000000000, 0.000000000000000000, 1.000000000000000000 ) ) ;
#11570=AXIS2_PLACEMENT_3D ( 'NONE', #7412, #15574, #969 ) ;
#11571=ORIENTED_EDGE ( 'NONE', *, *, #19482, .F. ) ;
#11577=ADVANCED_FACE ( 'NONE', ( #15002 ), #16380, .T. ) ;
#11583=CIRCLE ( 'NONE', #7869, 27.60000000002759890 ) ;
#11594=EDGE_CURVE ( 'NONE', #1369, #141, #5286, .T. ) ;
#11595=CARTESIAN_POINT ( 'NONE',  ( 0.000000000000000000, -18.50424539729797502, -69.58155576219135696 ) ) ;
#11597=CIRCLE ( 'NONE', #1469, 72.00000000007199219 ) ;
#11598=AXIS2_PLACEMENT_3D ( 'NONE', #16297, #12029, #4065 ) ;
#11599=ORIENTED_EDGE ( 'NONE', *, *, #10240, .T. ) ;
#11602=DIRECTION ( 'NONE',  ( 0.000000000000000000, 0.2697967711570248839, -0.9629172873477991335 ) ) ;
#11603=ORIENTED_EDGE ( 'NONE', *, *, #109, .T. ) ;
#11607=DIRECTION ( 'NONE',  ( 1.000000000000000000, 0.000000000000000000, 0.000000000000000000 ) ) ;
#11610=ORIENTED_EDGE ( 'NONE', *, *, #8959, .T. ) ;
#11611=DIRECTION ( 'NONE',  ( -1.000000000000000000, 0.000000000000000000, 0.000000000000000000 ) ) ;
#11613=AXIS2_PLACEMENT_3D ( 'NONE', #19635, #1744, #6599 ) ;
#11614=DIRECTION ( 'NONE',  ( 0.000000000000000000, 0.000000000000000000, -1.000000000000000000 ) ) ;
#11616=DIRECTION ( 'NONE',  ( 0.000000000000000000, 0.000000000000000000, 1.000000000000000000 ) ) ;
#11618=DIRECTION ( 'NONE',  ( 0.000000000000000000, -0.9422609221188236184, 0.3348796121709771145 ) ) ;
#11622=VERTEX_POINT ( 'NONE', #16183 ) ;
#11624=VECTOR ( 'NONE', #3614, 1000.000000000000000 ) ;
#11626=CIRCLE ( 'NONE', #3842, 65.24900000006526568 ) ;
#11629=ORIENTED_EDGE ( 'NONE', *, *, #12963, .F. ) ;
#11633=CIRCLE ( 'NONE', #17043, 27.60000000002759890 ) ;
#11634=ORIENTED_EDGE ( 'NONE', *, *, #16875, .F. ) ;
#11635=CIRCLE ( 'NONE', #814, 65.24900000006525147 ) ;
#11636=CARTESIAN_POINT ( 'NONE',  ( 19.99999999999999645, -51.43306257653170377, 40.15061736769546741 ) ) ;
#11641=ORIENTED_EDGE ( 'NONE', *, *, #18044, .F. ) ;
#11643=AXIS2_PLACEMENT_3D ( 'NONE', #7002, #755, #8596 ) ;
#11649=DIRECTION ( 'NONE',  ( 0.000000000000000000, 0.000000000000000000, 1.000000000000000000 ) ) ;
#11656=CYLINDRICAL_SURFACE ( 'NONE', #9355, 65.24900000006525147 ) ;
#11657=AXIS2_PLACEMENT_3D ( 'NONE', #4011, #6882, #11864 ) ;
#11658=EDGE_LOOP ( 'NONE', ( #20898, #11197, #20460, #683 ) ) ;
#11662=EDGE_CURVE ( 'NONE', #10684, #5273, #13752, .T. ) ;
#11663=ORIENTED_EDGE ( 'NONE', *, *, #20584, .F. ) ;
#11665=EDGE_LOOP ( 'NONE', ( #11953, #1137, #2861, #9715 ) ) ;
#11667=DIRECTION ( 'NONE',  ( 1.000000000000000000, -0.000000000000000000, -0.000000000000000000 ) ) ;
#11671=DIRECTION ( 'NONE',  ( 0.000000000000000000, 0.000000000000000000, 1.000000000000000000 ) ) ;
#11672=DIRECTION ( 'NONE',  ( 0.000000000000000000, 0.000000000000000000, 1.000000000000000000 ) ) ;
#11674=CIRCLE ( 'NONE', #17789, 65.24900000006525147 ) ;
#11684=ORIENTED_EDGE ( 'NONE', *, *, #20429, .F. ) ;
#11685=CARTESIAN_POINT ( 'NONE',  ( 19.99999999999999645, 0.000000000000000000, 0.000000000000000000 ) ) ;
#11686=ORIENTED_EDGE ( 'NONE', *, *, #1714, .F. ) ;
#11693=AXIS2_PLACEMENT_3D ( 'NONE', #13720, #13610, #20059 ) ;
#11695=CARTESIAN_POINT ( 'NONE',  ( 0.000000000000000000, 0.000000000000000000, 0.000000000000000000 ) ) ;
#11696=DIRECTION ( 'NONE',  ( 0.000000000000000000, 0.000000000000000000, -1.000000000000000000 ) ) ;
#11699=EDGE_CURVE ( 'NONE', #15235, #18900, #6973, .T. ) ;
#11700=DIRECTION ( 'NONE',  ( -1.000000000000000000, 0.000000000000000000, 0.000000000000000000 ) ) ;
#11702=EDGE_CURVE ( 'NONE', #7786, #19208, #562, .T. ) ;
#11704=CIRCLE ( 'NONE', #187, 27.60000000002759535 ) ;
#11716=CARTESIAN_POINT ( 'NONE',  ( 19.99999999999999645, 61.72688495901586947, 19.84591825364119089 ) ) ;
#11719=AXIS2_PLACEMENT_3D ( 'NONE', #17534, #7868, #20797 ) ;
#11722=CARTESIAN_POINT ( 'NONE',  ( 0.000000000000000000, -48.70996102988709708, 42.79495875147758710 ) ) ;
#11726=CARTESIAN_POINT ( 'NONE',  ( 9.999999999999998224, -71.89099403602352822, -3.960426305689549675 ) ) ;
#11728=CARTESIAN_POINT ( 'NONE',  ( 85.00002539999999840, 0.000000000000000000, 0.000000000000000000 ) ) ;
#11733=CIRCLE ( 'NONE', #17160, 72.00000000007199219 ) ;
#11734=CARTESIAN_POINT ( 'NONE',  ( 19.99999999999999645, -23.08379033237394395, 61.02926039941428371 ) ) ;
#11735=DIRECTION ( 'NONE',  ( -1.000000000000000000, 0.000000000000000000, 0.000000000000000000 ) ) ;
#11739=CARTESIAN_POINT ( 'NONE',  ( 19.99999999999999645, -51.81019761368295207, -38.98425606966110735 ) ) ;
#11745=CARTESIAN_POINT ( 'NONE',  ( 0.000000000000000000, 70.29359119158485214, 15.58239511117312226 ) ) ;
#11746=VERTEX_POINT ( 'NONE', #12027 ) ;
#11749=CIRCLE ( 'NONE', #1617, 65.24900000006525147 ) ;
#11750=VERTEX_POINT ( 'NONE', #3746 ) ;
#11754=VECTOR ( 'NONE', #8117, 1000.000000000000000 ) ;
#11755=DIRECTION ( 'NONE',  ( -1.000000000000000000, -0.000000000000000000, -0.000000000000000000 ) ) ;
#11763=DIRECTION ( 'NONE',  ( 0.000000000000000000, 0.000000000000000000, 1.000000000000000000 ) ) ;
#11766=ORIENTED_EDGE ( 'NONE', *, *, #2345, .T. ) ;
#11768=CARTESIAN_POINT ( 'NONE',  ( 0.000000000000000000, 20.60847369612982405, 61.90898814327722732 ) ) ;
#11771=VERTEX_POINT ( 'NONE', #18387 ) ;
#11772=CARTESIAN_POINT ( 'NONE',  ( 19.99999999999999645, -20.60847369613026103, 61.90898814327709943 ) ) ;
#11775=DIRECTION ( 'NONE',  ( 0.000000000000000000, 0.000000000000000000, -1.000000000000000000 ) ) ;
#11776=VERTEX_POINT ( 'NONE', #10228 ) ;
#11777=ORIENTED_EDGE ( 'NONE', *, *, #17155, .F. ) ;
#11778=DIRECTION ( 'NONE',  ( -1.000000000000000000, 0.000000000000000000, 0.000000000000000000 ) ) ;
#11780=DIRECTION ( 'NONE',  ( -1.000000000000000000, 0.000000000000000000, 0.000000000000000000 ) ) ;
#11785=CARTESIAN_POINT ( 'NONE',  ( 9.999999999999998224, -71.76067541710847308, -5.865617076725375689 ) ) ;
#11786=CARTESIAN_POINT ( 'NONE',  ( 19.99999999999999645, 5.762283366691162811, 64.99406197038673838 ) ) ;
#11799=EDGE_CURVE ( 'NONE', #9794, #8219, #3856, .T. ) ;
#11804=EDGE_CURVE ( 'NONE', #3682, #17307, #11068, .T. ) ;
#11805=CARTESIAN_POINT ( 'NONE',  ( 9.999999999999998224, 36.59093685910711002, -62.00889726307995176 ) ) ;
#11808=VERTEX_POINT ( 'NONE', #11816 ) ;
#11813=ORIENTED_EDGE ( 'NONE', *, *, #12572, .T. ) ;
#11815=DIRECTION ( 'NONE',  ( 0.000000000000000000, 0.000000000000000000, -1.000000000000000000 ) ) ;
#11816=CARTESIAN_POINT ( 'NONE',  ( 19.99999999999999645, 45.48683723007275148, -46.78012013466171481 ) ) ;
#11827=ADVANCED_FACE ( 'NONE', ( #18497 ), #8740, .T. ) ;
#11828=CYLINDRICAL_SURFACE ( 'NONE', #17711, 72.00000000007199219 ) ;
#11830=ORIENTED_EDGE ( 'NONE', *, *, #6233, .T. ) ;
#11831=CARTESIAN_POINT ( 'NONE',  ( 0.000000000000000000, -27.62776854598816101, -58.65812137499030854 ) ) ;
#11836=CARTESIAN_POINT ( 'NONE',  ( 0.000000000000000000, -71.76067541710854414, 5.865617076724380041 ) ) ;
#11842=CARTESIAN_POINT ( 'NONE',  ( 0.000000000000000000, 11.98658579560678206, -64.13855129306456604 ) ) ;
#11846=ORIENTED_EDGE ( 'NONE', *, *, #14919, .F. ) ;
#11850=DIRECTION ( 'NONE',  ( -1.000000000000000000, 0.000000000000000000, 0.000000000000000000 ) ) ;
#11852=DIRECTION ( 'NONE',  ( 0.000000000000000000, 0.000000000000000000, 1.000000000000000000 ) ) ;
#11856=CIRCLE ( 'NONE', #15921, 65.24900000006525147 ) ;
#11859=DIRECTION ( 'NONE',  ( -1.000000000000000000, -0.000000000000000000, 0.000000000000000000 ) ) ;
#11860=ORIENTED_EDGE ( 'NONE', *, *, #8584, .F. ) ;
#11864=DIRECTION ( 'NONE',  ( 0.000000000000000000, 0.000000000000000000, 1.000000000000000000 ) ) ;
#11877=DIRECTION ( 'NONE',  ( -1.000000000000000000, 0.000000000000000000, 0.000000000000000000 ) ) ;
#11881=FACE_OUTER_BOUND ( 'NONE', #1015, .T. ) ;
#11883=CARTESIAN_POINT ( 'NONE',  ( 0.000000000000000000, -68.15657073222450890, 23.20952102120257976 ) ) ;
#11888=DIRECTION ( 'NONE',  ( -1.000000000000000000, 0.000000000000000000, 0.000000000000000000 ) ) ;
#11889=CIRCLE ( 'NONE', #6145, 65.24900000006525147 ) ;
#11890=ORIENTED_EDGE ( 'NONE', *, *, #14818, .F. ) ;
#11904=DIRECTION ( 'NONE',  ( -1.000000000000000000, 0.000000000000000000, 0.000000000000000000 ) ) ;
#11905=CARTESIAN_POINT ( 'NONE',  ( 20.00000000000000355, 0.000000000000000000, 0.000000000000000000 ) ) ;
#11906=ORIENTED_EDGE ( 'NONE', *, *, #4929, .F. ) ;
#11909=VECTOR ( 'NONE', #14417, 1000.000000000000000 ) ;
#11914=CARTESIAN_POINT ( 'NONE',  ( 19.99999999999999645, 0.000000000000000000, 0.000000000000000000 ) ) ;
#11918=CARTESIAN_POINT ( 'NONE',  ( 19.99999999999999645, -60.40676135667420965, -23.56039007469101421 ) ) ;
#11920=VERTEX_POINT ( 'NONE', #9166 ) ;
#11921=DIRECTION ( 'NONE',  ( 0.000000000000000000, 0.9976687691905394839, -0.06824241336466758956 ) ) ;
#11923=DIRECTION ( 'NONE',  ( 0.000000000000000000, -0.8169698930104354329, -0.5766803221148765202 ) ) ;
#11924=AXIS2_PLACEMENT_3D ( 'NONE', #382, #16588, #11618 ) ;
#11925=CIRCLE ( 'NONE', #14648, 65.24900000006526568 ) ;
#11926=CARTESIAN_POINT ( 'NONE',  ( 19.99999999999999645, -39.37110852956777762, -51.51683813304910586 ) ) ;
#11929=ADVANCED_FACE ( 'NONE', ( #16053 ), #20814, .T. ) ;
#11933=AXIS2_PLACEMENT_3D ( 'NONE', #1138, #7474, #13957 ) ;
#11936=EDGE_CURVE ( 'NONE', #5449, #2438, #7582, .T. ) ;
#11945=DIRECTION ( 'NONE',  ( 1.000000000000000000, 0.000000000000000000, 0.000000000000000000 ) ) ;
#11946=ORIENTED_EDGE ( 'NONE', *, *, #10869, .T. ) ;
#11947=CYLINDRICAL_SURFACE ( 'NONE', #19378, 27.60000000002759890 ) ;
#11948=ORIENTED_EDGE ( 'NONE', *, *, #150, .T. ) ;
#11949=DIRECTION ( 'NONE',  ( -1.000000000000000000, -0.000000000000000000, -0.000000000000000000 ) ) ;
#11951=ORIENTED_EDGE ( 'NONE', *, *, #14911, .F. ) ;
#11953=ORIENTED_EDGE ( 'NONE', *, *, #11283, .T. ) ;
#11954=DIRECTION ( 'NONE',  ( -1.000000000000000000, 0.000000000000000000, 0.000000000000000000 ) ) ;
#11957=DIRECTION ( 'NONE',  ( -1.000000000000000000, 0.000000000000000000, -0.000000000000000000 ) ) ;
#11964=DIRECTION ( 'NONE',  ( -1.000000000000000000, -0.000000000000000000, -0.000000000000000000 ) ) ;
#11970=DIRECTION ( 'NONE',  ( 0.000000000000000000, 0.000000000000000000, 1.000000000000000000 ) ) ;
#11971=VECTOR ( 'NONE', #11515, 1000.000000000000000 ) ;
#11973=DIRECTION ( 'NONE',  ( 0.000000000000000000, 0.000000000000000000, 1.000000000000000000 ) ) ;
#11977=ORIENTED_EDGE ( 'NONE', *, *, #1611, .F. ) ;
#11978=DIRECTION ( 'NONE',  ( 0.000000000000000000, -0.9790840876823249106, 0.2034560130526240906 ) ) ;
#11980=AXIS2_PLACEMENT_3D ( 'NONE', #8196, #11483, #8101 ) ;
#11981=CARTESIAN_POINT ( 'NONE',  ( 19.99999999999999645, -58.44960523466222213, -28.06621538408651872 ) ) ;
#11987=SURFACE_SIDE_STYLE ('',( #7097 ) ) ;
#11988=FACE_OUTER_BOUND ( 'NONE', #10956, .T. ) ;
#11991=AXIS2_PLACEMENT_3D ( 'NONE', #14638, #116, #19508 ) ;
#11999=ORIENTED_EDGE ( 'NONE', *, *, #2562, .T. ) ;
#12002=VERTEX_POINT ( 'NONE', #17555 ) ;
#12006=CARTESIAN_POINT ( 'NONE',  ( 0.000000000000000000, -20.60847369612940128, -61.90898814327737654 ) ) ;
#12014=DIRECTION ( 'NONE',  ( -1.000000000000000000, -0.000000000000000000, -0.000000000000000000 ) ) ;
#12015=CARTESIAN_POINT ( 'NONE',  ( 0.000000000000000000, 0.000000000000000000, 0.000000000000000000 ) ) ;
#12019=CARTESIAN_POINT ( 'NONE',  ( 19.99999999999999645, 3.141410481201071914, 65.17333458706188765 ) ) ;
#12024=ORIENTED_EDGE ( 'NONE', *, *, #1193, .T. ) ;
#12026=CARTESIAN_POINT ( 'NONE',  ( 19.99999999999999645, 63.17103598352149874, -16.33561182745074447 ) ) ;
#12027=CARTESIAN_POINT ( 'NONE',  ( 19.99999999999999645, 67.51707036274447660, -25.00890260772307272 ) ) ;
#12029=DIRECTION ( 'NONE',  ( -1.000000000000000000, 0.000000000000000000, 0.000000000000000000 ) ) ;
#12030=ORIENTED_EDGE ( 'NONE', *, *, #18842, .F. ) ;
#12038=AXIS2_PLACEMENT_3D ( 'NONE', #4992, #19399, #6569 ) ;
#12043=ORIENTED_EDGE ( 'NONE', *, *, #18120, .T. ) ;
#12045=VERTEX_POINT ( 'NONE', #17645 ) ;
#12046=EDGE_CURVE ( 'NONE', #4233, #1822, #5891, .T. ) ;
#12052=AXIS2_PLACEMENT_3D ( 'NONE', #3345, #8421, #11499 ) ;
#12054=ORIENTED_EDGE ( 'NONE', *, *, #10663, .F. ) ;
#12055=DIRECTION ( 'NONE',  ( 0.000000000000000000, 0.000000000000000000, 1.000000000000000000 ) ) ;
#12062=AXIS2_PLACEMENT_3D ( 'NONE', #2231, #18449, #11775 ) ;
#12065=FACE_OUTER_BOUND ( 'NONE', #9970, .T. ) ;
#12066=EDGE_CURVE ( 'NONE', #7485, #17979, #4544, .T. ) ;
#12067=AXIS2_PLACEMENT_3D ( 'NONE', #14836, #1701, #10059 ) ;
#12080=CARTESIAN_POINT ( 'NONE',  ( 19.99999999999999645, 70.68211945903208004, -13.71269443944133570 ) ) ;
#12081=ORIENTED_EDGE ( 'NONE', *, *, #10013, .T. ) ;
#12082=DIRECTION ( 'NONE',  ( 0.000000000000000000, 0.000000000000000000, 1.000000000000000000 ) ) ;
#12083=AXIS2_PLACEMENT_3D ( 'NONE', #8429, #16586, #14904 ) ;
#12085=DIRECTION ( 'NONE',  ( 0.000000000000000000, 0.000000000000000000, 1.000000000000000000 ) ) ;
#12086=EDGE_CURVE ( 'NONE', #9945, #2326, #4204, .T. ) ;
#12090=VECTOR ( 'NONE', #15649, 1000.000000000000000 ) ;
#12091=VERTEX_POINT ( 'NONE', #1742 ) ;
#12093=DIRECTION ( 'NONE',  ( -1.000000000000000000, 0.000000000000000000, 0.000000000000000000 ) ) ;
#12095=ORIENTED_EDGE ( 'NONE', *, *, #11428, .T. ) ;
#12099=CIRCLE ( 'NONE', #13799, 27.60000000002759890 ) ;
#12100=FACE_OUTER_BOUND ( 'NONE', #15202, .T. ) ;
#12102=VECTOR ( 'NONE', #4437, 1000.000000000000000 ) ;
#12104=CARTESIAN_POINT ( 'NONE',  ( 9.999999999999998224, -38.22257254261700155, -61.01667762370178139 ) ) ;
#12105=CARTESIAN_POINT ( 'NONE',  ( 0.000000000000000000, -20.60847369613026103, 61.90898814327709943 ) ) ;
#12106=LINE ( 'NONE', #18572, #3733 ) ;
#12110=VERTEX_POINT ( 'NONE', #14872 ) ;
#12115=VERTEX_POINT ( 'NONE', #347 ) ;
#12129=FACE_OUTER_BOUND ( 'NONE', #15851, .T. ) ;
#12130=ORIENTED_EDGE ( 'NONE', *, *, #12195, .T. ) ;
#12132=VERTEX_POINT ( 'NONE', #2041 ) ;
#12137=LINE ( 'NONE', #9830, #3148 ) ;
#12148=CARTESIAN_POINT ( 'NONE',  ( 0.000000000000000000, 31.98952867950403345, -56.39803944231551469 ) ) ;
#12149=ORIENTED_EDGE ( 'NONE', *, *, #12844, .F. ) ;
#12152=FACE_BOUND ( 'NONE', #2183, .T. ) ;
#12156=CYLINDRICAL_SURFACE ( 'NONE', #14488, 65.24900000006525147 ) ;
#12160=DIRECTION ( 'NONE',  ( 0.000000000000000000, 0.000000000000000000, 1.000000000000000000 ) ) ;
#12162=ORIENTED_EDGE ( 'NONE', *, *, #8438, .T. ) ;
#12165=FACE_OUTER_BOUND ( 'NONE', #1240, .T. ) ;
#12166=DIRECTION ( 'NONE',  ( 0.000000000000000000, 0.000000000000000000, 1.000000000000000000 ) ) ;
#12177=ADVANCED_FACE ( 'NONE', ( #5110 ), #20920, .T. ) ;
#12178=ORIENTED_EDGE ( 'NONE', *, *, #19706, .T. ) ;
#12183=EDGE_LOOP ( 'NONE', ( #18680, #13054, #16400, #2758 ) ) ;
#12186=DIRECTION ( 'NONE',  ( -1.000000000000000000, 0.000000000000000000, 0.000000000000000000 ) ) ;
#12188=ORIENTED_EDGE ( 'NONE', *, *, #10869, .F. ) ;
#12192=( NAMED_UNIT ( * ) PLANE_ANGLE_UNIT ( ) SI_UNIT ( $, .RADIAN. ) );
#12194=DIRECTION ( 'NONE',  ( -1.000000000000000000, -0.000000000000000000, 0.000000000000000000 ) ) ;
#12195=EDGE_CURVE ( 'NONE', #10678, #6079, #6596, .T. ) ;
#12197=CIRCLE ( 'NONE', #8132, 72.00000000007199219 ) ;
#12199=DIRECTION ( 'NONE',  ( 0.000000000000000000, -0.6310879443260593025, 0.7757112907044145800 ) ) ;
#12200=CARTESIAN_POINT ( 'NONE',  ( 19.99999999999999645, 63.48283426024850229, 33.96954156735390740 ) ) ;
#12205=FACE_OUTER_BOUND ( 'NONE', #8138, .T. ) ;
#12212=FACE_OUTER_BOUND ( 'NONE', #12936, .T. ) ;
#12213=ORIENTED_EDGE ( 'NONE', *, *, #11702, .T. ) ;
#12219=ORIENTED_EDGE ( 'NONE', *, *, #12269, .T. ) ;
#12230=EDGE_LOOP ( 'NONE', ( #4580, #5601, #9821, #1738 ) ) ;
#12232=ORIENTED_EDGE ( 'NONE', *, *, #16816, .F. ) ;
#12238=CIRCLE ( 'NONE', #10926, 65.24900000006525147 ) ;
#12243=ORIENTED_EDGE ( 'NONE', *, *, #14281, .F. ) ;
#12244=EDGE_CURVE ( 'NONE', #12867, #14502, #1943, .T. ) ;
#12249=VECTOR ( 'NONE', #7363, 1000.000000000000000 ) ;
#12250=VECTOR ( 'NONE', #19506, 1000.000000000000000 ) ;
#12251=VERTEX_POINT ( 'NONE', #5021 ) ;
#12252=DIRECTION ( 'NONE',  ( -1.000000000000000000, -0.000000000000000000, 0.000000000000000000 ) ) ;
#12258=DIRECTION ( 'NONE',  ( 0.000000000000000000, 0.000000000000000000, 1.000000000000000000 ) ) ;
#12264=DIRECTION ( 'NONE',  ( -1.000000000000000000, -0.000000000000000000, -0.000000000000000000 ) ) ;
#12265=EDGE_CURVE ( 'NONE', #16773, #6425, #9283, .T. ) ;
#12267=ORIENTED_EDGE ( 'NONE', *, *, #4019, .T. ) ;
#12269=EDGE_CURVE ( 'NONE', #857, #3130, #134, .T. ) ;
#12270=VECTOR ( 'NONE', #19580, 1000.000000000000000 ) ;
#12272=VECTOR ( 'NONE', #8553, 1000.000000000000000 ) ;
#12276=DIRECTION ( 'NONE',  ( 0.000000000000000000, -0.1361666490962331333, -0.9906859460363326431 ) ) ;
#12277=DIRECTION ( 'NONE',  ( 0.000000000000000000, 0.2697967711570183891, 0.9629172873478009098 ) ) ;
#12279=VECTOR ( 'NONE', #13329, 1000.000000000000000 ) ;
#12283=CIRCLE ( 'NONE', #20039, 27.60000000002760245 ) ;
#12290=VERTEX_POINT ( 'NONE', #14572 ) ;
#12291=CYLINDRICAL_SURFACE ( 'NONE', #4824, 65.24900000006525147 ) ;
#12295=ORIENTED_EDGE ( 'NONE', *, *, #3259, .F. ) ;
#12301=ORIENTED_EDGE ( 'NONE', *, *, #19682, .T. ) ;
#12302=ORIENTED_EDGE ( 'NONE', *, *, #4704, .F. ) ;
#12305=CIRCLE ( 'NONE', #5506, 65.24900000006525147 ) ;
#12308=EDGE_CURVE ( 'NONE', #4610, #12350, #8267, .T. ) ;
#12309=CARTESIAN_POINT ( 'NONE',  ( 19.99999999999999645, 46.01927912072591198, -45.67597560296339765 ) ) ;
#12310=VECTOR ( 'NONE', #16764, 1000.000000000000000 ) ;
#12320=ORIENTED_EDGE ( 'NONE', *, *, #12819, .T. ) ;
#12327=ORIENTED_EDGE ( 'NONE', *, *, #9057, .T. ) ;
#12330=DIRECTION ( 'NONE',  ( 0.000000000000000000, 0.000000000000000000, 1.000000000000000000 ) ) ;
#12331=AXIS2_PLACEMENT_3D ( 'NONE', #9151, #17430, #20907 ) ;
#12334=CIRCLE ( 'NONE', #4506, 72.00000000007199219 ) ;
#12338=EDGE_CURVE ( 'NONE', #11557, #8862, #766, .T. ) ;
#12340=EDGE_CURVE ( 'NONE', #10176, #6274, #18429, .T. ) ;
#12343=FILL_AREA_STYLE_COLOUR ( '', #10319 ) ;
#12344=EDGE_CURVE ( 'NONE', #8735, #8470, #5417, .T. ) ;
#12345=CYLINDRICAL_SURFACE ( 'NONE', #3713, 72.00000000007199219 ) ;
#12346=EDGE_LOOP ( 'NONE', ( #13266, #7118, #17134, #17565 ) ) ;
#12347=AXIS2_PLACEMENT_3D ( 'NONE', #25, #19728, #11672 ) ;
#12348=CARTESIAN_POINT ( 'NONE',  ( 19.99999999999999645, 38.69327817041775575, 52.53819777490647880 ) ) ;
#12350=VERTEX_POINT ( 'NONE', #2356 ) ;
#12352=CARTESIAN_POINT ( 'NONE',  ( 0.000000000000000000, 61.72688495901613948, -19.84591825364033468 ) ) ;
#12356=ORIENTED_EDGE ( 'NONE', *, *, #2631, .T. ) ;
#12369=LINE ( 'NONE', #10779, #16002 ) ;
#12379=DIRECTION ( 'NONE',  ( -1.000000000000000000, -0.000000000000000000, -0.000000000000000000 ) ) ;
#12384=ORIENTED_EDGE ( 'NONE', *, *, #16346, .F. ) ;
#12386=DIRECTION ( 'NONE',  ( -1.000000000000000000, 0.000000000000000000, 0.000000000000000000 ) ) ;
#12387=DIRECTION ( 'NONE',  ( 0.000000000000000000, 0.000000000000000000, 1.000000000000000000 ) ) ;
#12388=CARTESIAN_POINT ( 'NONE',  ( 19.99999999999999645, -48.70996102988652154, -42.79495875147824790 ) ) ;
#12393=ORIENTED_EDGE ( 'NONE', *, *, #18959, .F. ) ;
#12395=VECTOR ( 'NONE', #20417, 1000.000000000000000 ) ;
#12399=DIRECTION ( 'NONE',  ( -1.000000000000000000, -0.000000000000000000, 0.000000000000000000 ) ) ;
#12408=DIRECTION ( 'NONE',  ( 0.000000000000000000, -0.9976687691905398170, 0.06824241336466078944 ) ) ;
#12410=VERTEX_POINT ( 'NONE', #14230 ) ;
#12411=ORIENTED_EDGE ( 'NONE', *, *, #14490, .F. ) ;
#12412=CYLINDRICAL_SURFACE ( 'NONE', #16468, 27.60000000002759535 ) ;
#12413=CIRCLE ( 'NONE', #9371, 65.24900000006525147 ) ;
#12414=VECTOR ( 'NONE', #6211, 1000.000000000000000 ) ;
#12416=CIRCLE ( 'NONE', #6312, 7.500000000000000000 ) ;
#12418=AXIS2_PLACEMENT_3D ( 'NONE', #7178, #17161, #13659 ) ;
#12421=AXIS2_PLACEMENT_3D ( 'NONE', #2413, #835, #8666 ) ;
#12424=LINE ( 'NONE', #5840, #20842 ) ;
#12428=VERTEX_POINT ( 'NONE', #15596 ) ;
#12431=VERTEX_POINT ( 'NONE', #6269 ) ;
#12437=LINE ( 'NONE', #4269, #9706 ) ;
#12438=AXIS2_PLACEMENT_3D ( 'NONE', #6350, #4969, #14721 ) ;
#12440=DIRECTION ( 'NONE',  ( 0.000000000000000000, 0.9422609221188213979, -0.3348796121709836648 ) ) ;
#12443=CARTESIAN_POINT ( 'NONE',  ( 19.99999999999999645, 51.81019761368373366, -38.98425606966007706 ) ) ;
#12444=CIRCLE ( 'NONE', #17538, 65.24900000006525147 ) ;
#12449=DIRECTION ( 'NONE',  ( 0.000000000000000000, 0.000000000000000000, 1.000000000000000000 ) ) ;
#12450=ORIENTED_EDGE ( 'NONE', *, *, #11314, .F. ) ;
#12452=DIRECTION ( 'NONE',  ( -1.000000000000000000, -0.000000000000000000, 0.000000000000000000 ) ) ;
#12459=VERTEX_POINT ( 'NONE', #6159 ) ;
#12460=EDGE_CURVE ( 'NONE', #939, #9908, #5952, .T. ) ;
#12461=AXIS2_PLACEMENT_3D ( 'NONE', #19474, #3361, #185 ) ;
#12465=EDGE_CURVE ( 'NONE', #20215, #4706, #13363, .T. ) ;
#12467=EDGE_CURVE ( 'NONE', #12002, #10263, #9245, .T. ) ;
#12472=ORIENTED_EDGE ( 'NONE', *, *, #20293, .F. ) ;
#12473=DIRECTION ( 'NONE',  ( 0.000000000000000000, 0.000000000000000000, 1.000000000000000000 ) ) ;
#12474=ORIENTED_EDGE ( 'NONE', *, *, #3400, .T. ) ;
#12479=DIRECTION ( 'NONE',  ( 1.000000000000000000, -0.000000000000000000, -0.000000000000000000 ) ) ;
#12481=ORIENTED_EDGE ( 'NONE', *, *, #1529, .T. ) ;
#12482=EDGE_CURVE ( 'NONE', #17420, #5525, #17617, .T. ) ;
#12483=CARTESIAN_POINT ( 'NONE',  ( 19.99999999999999645, -27.62776854598816101, -58.65812137499030854 ) ) ;
#12489=EDGE_CURVE ( 'NONE', #18834, #4546, #6058, .T. ) ;
#12491=EDGE_CURVE ( 'NONE', #833, #15651, #503, .T. ) ;
#12494=DIRECTION ( 'NONE',  ( 0.000000000000000000, -0.8878852184023702243, -0.4600650377311618633 ) ) ;
#12495=DIRECTION ( 'NONE',  ( -1.000000000000000000, -0.000000000000000000, -0.000000000000000000 ) ) ;
#12496=CARTESIAN_POINT ( 'NONE',  ( 0.000000000000000000, 1.971042061628357933, 64.80882494896107460 ) ) ;
#12501=CIRCLE ( 'NONE', #3672, 27.60000000002759535 ) ;
#12502=CARTESIAN_POINT ( 'NONE',  ( 19.99999999999999645, -64.80702306891090814, -7.581672767547114944 ) ) ;
#12506=EDGE_LOOP ( 'NONE', ( #19773, #3846, #5128, #3808 ) ) ;
#12509=CARTESIAN_POINT ( 'NONE',  ( 9.999999999999998224, 38.22257254261821657, -61.01667762370101400 ) ) ;
#12511=ORIENTED_EDGE ( 'NONE', *, *, #17325, .T. ) ;
#12512=DIRECTION ( 'NONE',  ( 0.000000000000000000, -0.8878852184023701133, -0.4600650377311617523 ) ) ;
#12516=VERTEX_POINT ( 'NONE', #16327 ) ;
#12520=APPLICATION_CONTEXT ( 'automotive_design' ) ;
#12522=DIRECTION ( 'NONE',  ( -1.000000000000000000, 0.000000000000000000, 0.000000000000000000 ) ) ;
#12526=DIRECTION ( 'NONE',  ( 0.000000000000000000, 0.000000000000000000, 1.000000000000000000 ) ) ;
#12530=VERTEX_POINT ( 'NONE', #3199 ) ;
#12532=CARTESIAN_POINT ( 'NONE',  ( 9.999999999999998224, 70.68211945903209426, -13.71269443944134281 ) ) ;
#12534=CARTESIAN_POINT ( 'NONE',  ( -10.00000000000000000, 0.000000000000000000, 0.000000000000000000 ) ) ;
#12535=VERTEX_POINT ( 'NONE', #18025 ) ;
#12537=DIRECTION ( 'NONE',  ( -1.000000000000000000, 0.000000000000000000, -0.000000000000000000 ) ) ;
#12538=DIRECTION ( 'NONE',  ( 0.000000000000000000, 0.000000000000000000, -1.000000000000000000 ) ) ;
#12540=ORIENTED_EDGE ( 'NONE', *, *, #17155, .T. ) ;
#12541=CARTESIAN_POINT ( 'NONE',  ( 19.99999999999999645, -56.63599015375651646, -31.56633360682521072 ) ) ;
#12543=FACE_OUTER_BOUND ( 'NONE', #10117, .T. ) ;
#12546=CIRCLE ( 'NONE', #20658, 65.24900000006526568 ) ;
#12552=ORIENTED_EDGE ( 'NONE', *, *, #16188, .T. ) ;
#12555=ORIENTED_EDGE ( 'NONE', *, *, #1853, .F. ) ;
#12557=CARTESIAN_POINT ( 'NONE',  ( 0.000000000000000000, 19.38316218894295417, -61.87375713200968619 ) ) ;
#12561=VERTEX_POINT ( 'NONE', #11248 ) ;
#12562=CARTESIAN_POINT ( 'NONE',  ( 19.99999999999999645, -55.05624179292004072, 35.01774179823764399 ) ) ;
#12564=VERTEX_POINT ( 'NONE', #323 ) ;
#12571=ORIENTED_EDGE ( 'NONE', *, *, #13639, .T. ) ;
#12572=EDGE_CURVE ( 'NONE', #18871, #15500, #15724, .T. ) ;
#12573=CARTESIAN_POINT ( 'NONE',  ( 0.000000000000000000, -64.80702306891090814, -7.581672767547114944 ) ) ;
#12574=ORIENTED_EDGE ( 'NONE', *, *, #16116, .T. ) ;
#12580=CARTESIAN_POINT ( 'NONE',  ( 9.999999999999998224, 20.34307325858785731, 69.06634035770315450 ) ) ;
#12584=CARTESIAN_POINT ( 'NONE',  ( 9.999999999999998224, -53.26727847779572045, 48.44168704307611506 ) ) ;
#12585=VERTEX_POINT ( 'NONE', #1627 ) ;
#12603=VERTEX_POINT ( 'NONE', #7972 ) ;
#12605=DIRECTION ( 'NONE',  ( 0.000000000000000000, 0.000000000000000000, -1.000000000000000000 ) ) ;
#12610=VECTOR ( 'NONE', #12711, 1000.000000000000000 ) ;
#12612=ORIENTED_EDGE ( 'NONE', *, *, #1872, .T. ) ;
#12614=DIRECTION ( 'NONE',  ( 0.000000000000000000, 0.000000000000000000, 1.000000000000000000 ) ) ;
#12623=CARTESIAN_POINT ( 'NONE',  ( 9.999999999999998224, 71.76067541710858677, -5.865617076723870227 ) ) ;
#12625=EDGE_CURVE ( 'NONE', #18498, #7039, #16393, .T. ) ;
#12628=ADVANCED_FACE ( 'NONE', ( #16231 ), #8167, .T. ) ;
#12631=CARTESIAN_POINT ( 'NONE',  ( 19.99999999999999645, -24.01204443665145405, -60.22865198596149838 ) ) ;
#12637=AXIS2_PLACEMENT_3D ( 'NONE', #16189, #6421, #8122 ) ;
#12640=AXIS2_PLACEMENT_3D ( 'NONE', #19343, #3340, #6313 ) ;
#12641=CARTESIAN_POINT ( 'NONE',  ( 0.000000000000000000, 53.26727847779537939, 48.44168704307649875 ) ) ;
#12642=CARTESIAN_POINT ( 'NONE',  ( 19.99999999999999645, 38.22257254261739945, 61.01667762370151138 ) ) ;
#12643=VERTEX_POINT ( 'NONE', #20012 ) ;
#12644=DIRECTION ( 'NONE',  ( 0.000000000000000000, 0.000000000000000000, 1.000000000000000000 ) ) ;
#12645=ORIENTED_EDGE ( 'NONE', *, *, #4009, .F. ) ;
#12647=CARTESIAN_POINT ( 'NONE',  ( 19.99999999999999645, -11.98658579560631843, 64.13855129306463709 ) ) ;
#12649=EDGE_LOOP ( 'NONE', ( #2207, #4323, #9554, #15342 ) ) ;
#12652=VERTEX_POINT ( 'NONE', #5298 ) ;
#12656=ORIENTED_EDGE ( 'NONE', *, *, #4019, .F. ) ;
#12658=AXIS2_PLACEMENT_3D ( 'NONE', #5979, #6077, #19231 ) ;
#12659=DIRECTION ( 'NONE',  ( 0.000000000000000000, 0.000000000000000000, 1.000000000000000000 ) ) ;
#12662=AXIS2_PLACEMENT_3D ( 'NONE', #2980, #20664, #6146 ) ;
#12664=ORIENTED_EDGE ( 'NONE', *, *, #9379, .F. ) ;
#12672=EDGE_CURVE ( 'NONE', #13929, #5677, #19122, .T. ) ;
#12677=ORIENTED_EDGE ( 'NONE', *, *, #18143, .T. ) ;
#12679=CARTESIAN_POINT ( 'NONE',  ( 19.99999999999999645, 0.000000000000000000, 0.000000000000000000 ) ) ;
#12680=ORIENTED_EDGE ( 'NONE', *, *, #8441, .F. ) ;
#12685=CARTESIAN_POINT ( 'NONE',  ( 0.000000000000000000, 6.872116855663142232, 64.47358224882421496 ) ) ;
#12687=ADVANCED_FACE ( 'NONE', ( #14951 ), #3907, .T. ) ;
#12689=ORIENTED_EDGE ( 'NONE', *, *, #3140, .F. ) ;
#12695=EDGE_CURVE ( 'NONE', #12251, #9297, #8957, .T. ) ;
#12698=ORIENTED_EDGE ( 'NONE', *, *, #6098, .T. ) ;
#12702=ORIENTED_EDGE ( 'NONE', *, *, #8624, .F. ) ;
#12708=CARTESIAN_POINT ( 'NONE',  ( -10.00000000000000000, 0.000000000000000000, 0.000000000000000000 ) ) ;
#12711=DIRECTION ( 'NONE',  ( 1.000000000000000000, 0.000000000000000000, -0.000000000000000000 ) ) ;
#12715=EDGE_CURVE ( 'NONE', #2314, #6220, #13787, .T. ) ;
#12718=LINE ( 'NONE', #12719, #12102 ) ;
#12719=CARTESIAN_POINT ( 'NONE',  ( 19.99999999999999645, -3.141410481200616278, -65.17333458706190186 ) ) ;
#12727=VERTEX_POINT ( 'NONE', #16856 ) ;
#12730=EDGE_LOOP ( 'NONE', ( #973, #4211, #11641, #15757 ) ) ;
#12732=DIRECTION ( 'NONE',  ( 0.000000000000000000, -0.8878852184023701133, -0.4600650377311617523 ) ) ;
#12733=ADVANCED_FACE ( 'NONE', ( #19815 ), #3601, .T. ) ;
#12737=AXIS2_PLACEMENT_3D ( 'NONE', #4739, #19463, #7921 ) ;
#12738=EDGE_CURVE ( 'NONE', #9460, #3717, #740, .T. ) ;
#12741=AXIS2_PLACEMENT_3D ( 'NONE', #15908, #17516, #13907 ) ;
#12742=CARTESIAN_POINT ( 'NONE',  ( 0.000000000000000000, 53.26727847779604019, -48.44168704307576689 ) ) ;
#12746=EDGE_CURVE ( 'NONE', #19589, #8077, #20552, .T. ) ;
#12751=ORIENTED_EDGE ( 'NONE', *, *, #18678, .T. ) ;
#12762=LINE ( 'NONE', #9356, #6108 ) ;
#12765=EDGE_CURVE ( 'NONE', #12727, #17488, #6037, .T. ) ;
#12767=DIRECTION ( 'NONE',  ( -1.000000000000000000, 0.000000000000000000, 0.000000000000000000 ) ) ;
#12770=CARTESIAN_POINT ( 'NONE',  ( 0.000000000000000000, 6.872116855664026858, -64.47358224882410127 ) ) ;
#12772=AXIS2_PLACEMENT_3D ( 'NONE', #2642, #15974, #19058 ) ;
#12773=DIRECTION ( 'NONE',  ( -1.000000000000000000, 0.000000000000000000, -0.000000000000000000 ) ) ;
#12775=CARTESIAN_POINT ( 'NONE',  ( 9.999999999999998224, -38.22257254261782577, 61.01667762370126269 ) ) ;
#12779=DIRECTION ( 'NONE',  ( -1.000000000000000000, -0.000000000000000000, -0.000000000000000000 ) ) ;
#12793=VECTOR ( 'NONE', #9716, 1000.000000000000000 ) ;
#12795=CARTESIAN_POINT ( 'NONE',  ( 0.000000000000000000, -45.48683723007179935, -46.78012013466265984 ) ) ;
#12799=VERTEX_POINT ( 'NONE', #20331 ) ;
#12800=CARTESIAN_POINT ( 'NONE',  ( 0.000000000000000000, -59.31169354540720207, -27.19476070466916795 ) ) ;
#12804=LINE ( 'NONE', #14071, #15222 ) ;
#12806=CYLINDRICAL_SURFACE ( 'NONE', #19333, 72.00000000007199219 ) ;
#12807=DIRECTION ( 'NONE',  ( 1.000000000000000000, -0.000000000000000000, -0.000000000000000000 ) ) ;
#12809=CARTESIAN_POINT ( 'NONE',  ( 19.99999999999999645, 18.50424539729845463, 69.58155576219121485 ) ) ;
#12810=DIRECTION ( 'NONE',  ( -1.000000000000000000, -0.000000000000000000, -0.000000000000000000 ) ) ;
#12815=CARTESIAN_POINT ( 'NONE',  ( 19.99999999999999645, 36.54710069451126486, -54.05313526368077248 ) ) ;
#12818=CYLINDRICAL_SURFACE ( 'NONE', #13948, 65.24900000006525147 ) ;
#12819=EDGE_CURVE ( 'NONE', #19326, #14998, #10747, .T. ) ;
#12820=CARTESIAN_POINT ( 'NONE',  ( 19.99999999999999645, -6.872116855662673274, -64.47358224882424338 ) ) ;
#12824=FACE_OUTER_BOUND ( 'NONE', #12730, .T. ) ;
#12829=FACE_OUTER_BOUND ( 'NONE', #16260, .T. ) ;
#12832=ORIENTED_EDGE ( 'NONE', *, *, #11183, .T. ) ;
#12833=LINE ( 'NONE', #6442, #14967 ) ;
#12834=ORIENTED_EDGE ( 'NONE', *, *, #20084, .F. ) ;
#12835=DIRECTION ( 'NONE',  ( 0.000000000000000000, 0.000000000000000000, 1.000000000000000000 ) ) ;
#12838=ORIENTED_EDGE ( 'NONE', *, *, #1328, .F. ) ;
#12844=EDGE_CURVE ( 'NONE', #281, #8899, #20652, .T. ) ;
#12846=EDGE_CURVE ( 'NONE', #13708, #3116, #17384, .T. ) ;
#12847=CARTESIAN_POINT ( 'NONE',  ( 19.99999999999999645, -8.857208570069305509, -71.45313048675095047 ) ) ;
#12854=CARTESIAN_POINT ( 'NONE',  ( 0.000000000000000000, 63.85430960833490843, -11.25592921604860663 ) ) ;
#12857=CARTESIAN_POINT ( 'NONE',  ( -10.00000000000000000, 0.000000000000000000, 0.000000000000000000 ) ) ;
#12858=ORIENTED_EDGE ( 'NONE', *, *, #1459, .F. ) ;
#12863=DIRECTION ( 'NONE',  ( 0.000000000000000000, 0.6310879443260540844, -0.7757112907044187988 ) ) ;
#12867=VERTEX_POINT ( 'NONE', #11015 ) ;
#12869=AXIS2_PLACEMENT_3D ( 'NONE', #19558, #13201, #14791 ) ;
#12874=DIRECTION ( 'NONE',  ( 0.000000000000000000, 0.9976687691905389288, 0.06824241336467461172 ) ) ;
#12875=DIRECTION ( 'NONE',  ( -1.000000000000000000, -0.000000000000000000, -0.000000000000000000 ) ) ;
#12878=CARTESIAN_POINT ( 'NONE',  ( 0.000000000000000000, -10.77748419466740692, 63.93680186330469439 ) ) ;
#12881=ORIENTED_EDGE ( 'NONE', *, *, #18415, .T. ) ;
#12882=CARTESIAN_POINT ( 'NONE',  ( 0.000000000000000000, -20.34307325858738835, -69.06634035770328239 ) ) ;
#12885=VERTEX_POINT ( 'NONE', #14208 ) ;
#12887=EDGE_CURVE ( 'NONE', #7047, #4467, #20207, .T. ) ;
#12888=EDGE_CURVE ( 'NONE', #20602, #14689, #6999, .T. ) ;
#12899=DIRECTION ( 'NONE',  ( 1.000000000000000000, -0.000000000000000000, -0.000000000000000000 ) ) ;
#12903=EDGE_CURVE ( 'NONE', #12002, #6701, #8370, .T. ) ;
#12905=CIRCLE ( 'NONE', #1395, 27.60000000002759890 ) ;
#12907=CARTESIAN_POINT ( 'NONE',  ( 19.99999999999999645, 0.000000000000000000, 0.000000000000000000 ) ) ;
#12909=ORIENTED_EDGE ( 'NONE', *, *, #18694, .F. ) ;
#12911=DIRECTION ( 'NONE',  ( -1.000000000000000000, -0.000000000000000000, 0.000000000000000000 ) ) ;
#12915=DIRECTION ( 'NONE',  ( 1.000000000000000000, -0.000000000000000000, 0.000000000000000000 ) ) ;
#12917=CARTESIAN_POINT ( 'NONE',  ( 19.99999999999999645, 58.44960523466241398, -28.06621538408611016 ) ) ;
#12922=ORIENTED_EDGE ( 'NONE', *, *, #8684, .T. ) ;
#12923=ADVANCED_FACE ( 'NONE', ( #5059 ), #12926, .F. ) ;
#12924=DIRECTION ( 'NONE',  ( 1.000000000000000000, -0.000000000000000000, -0.000000000000000000 ) ) ;
#12926=CYLINDRICAL_SURFACE ( 'NONE', #12438, 4.000000000000000000 ) ;
#12927=ORIENTED_EDGE ( 'NONE', *, *, #18851, .F. ) ;
#12929=DIRECTION ( 'NONE',  ( -1.000000000000000000, 0.000000000000000000, -0.000000000000000000 ) ) ;
#12934=ORIENTED_EDGE ( 'NONE', *, *, #19695, .T. ) ;
#12936=EDGE_LOOP ( 'NONE', ( #3909, #18905, #13418, #12909 ) ) ;
#12940=LINE ( 'NONE', #19496, #2511 ) ;
#12941=DIRECTION ( 'NONE',  ( -1.000000000000000000, -0.000000000000000000, -0.000000000000000000 ) ) ;
#12945=DIRECTION ( 'NONE',  ( -1.000000000000000000, 0.000000000000000000, 0.000000000000000000 ) ) ;
#12950=FACE_OUTER_BOUND ( 'NONE', #9141, .T. ) ;
#12956=EDGE_LOOP ( 'NONE', ( #2674, #16714, #10796, #6096 ) ) ;
#12959=ORIENTED_EDGE ( 'NONE', *, *, #7903, .F. ) ;
#12960=ORIENTED_EDGE ( 'NONE', *, *, #18054, .F. ) ;
#12962=CIRCLE ( 'NONE', #3791, 65.24900000006525147 ) ;
#12963=EDGE_CURVE ( 'NONE', #18514, #9743, #13029, .T. ) ;
#12964=CIRCLE ( 'NONE', #19053, 27.60000000002759535 ) ;
#12966=DIRECTION ( 'NONE',  ( 0.000000000000000000, 0.000000000000000000, 1.000000000000000000 ) ) ;
#12968=EDGE_CURVE ( 'NONE', #11336, #12652, #14615, .T. ) ;
#12971=CARTESIAN_POINT ( 'NONE',  ( 19.99999999999999645, 14.55863677812122425, 63.60407295269110506 ) ) ;
#12973=CARTESIAN_POINT ( 'NONE',  ( 85.00002539999999840, 5.400000000000000355, 0.000000000000000000 ) ) ;
#12975=AXIS2_PLACEMENT_3D ( 'NONE', #13084, #16057, #11387 ) ;
#12981=FACE_OUTER_BOUND ( 'NONE', #17365, .T. ) ;
#12983=DIRECTION ( 'NONE',  ( -1.000000000000000000, -0.000000000000000000, 0.000000000000000000 ) ) ;
#12987=ADVANCED_FACE ( 'NONE', ( #17806 ), #6546, .T. ) ;
#12988=DIRECTION ( 'NONE',  ( -1.000000000000000000, -0.000000000000000000, -0.000000000000000000 ) ) ;
#12991=CARTESIAN_POINT ( 'NONE',  ( 19.99999999999999645, 48.70996102988680576, 42.79495875147792106 ) ) ;
#12994=CARTESIAN_POINT ( 'NONE',  ( 19.99999999999999645, 0.000000000000000000, 0.000000000000000000 ) ) ;
#12995=DIRECTION ( 'NONE',  ( -1.000000000000000000, -0.000000000000000000, 0.000000000000000000 ) ) ;
#12996=VERTEX_POINT ( 'NONE', #14419 ) ;
#12997=CYLINDRICAL_SURFACE ( 'NONE', #10829, 72.00000000007199219 ) ;
#13002=DIRECTION ( 'NONE',  ( -1.000000000000000000, -0.000000000000000000, -0.000000000000000000 ) ) ;
#13008=VECTOR ( 'NONE', #16458, 1000.000000000000000 ) ;
#13014=ADVANCED_FACE ( 'NONE', ( #1597 ), #8051, .T. ) ;
#13016=CARTESIAN_POINT ( 'NONE',  ( 19.99999999999999645, -27.80658314415271093, 66.41380830714113870 ) ) ;
#13017=DIRECTION ( 'NONE',  ( 0.000000000000000000, 0.000000000000000000, -1.000000000000000000 ) ) ;
#13018=VECTOR ( 'NONE', #341, 1000.000000000000000 ) ;
#13022=CARTESIAN_POINT ( 'NONE',  ( 0.000000000000000000, 0.000000000000000000, 0.000000000000000000 ) ) ;
#13023=CARTESIAN_POINT ( 'NONE',  ( 0.000000000000000000, 0.000000000000000000, 0.000000000000000000 ) ) ;
#13027=CARTESIAN_POINT ( 'NONE',  ( 19.99999999999999645, 35.35772184876879720, 54.34979580218204376 ) ) ;
#13029=LINE ( 'NONE', #17699, #3295 ) ;
#13030=EDGE_LOOP ( 'NONE', ( #1392, #18742, #7946, #9354, #1413, #11766 ) ) ;
#13031=DIRECTION ( 'NONE',  ( 0.000000000000000000, -0.1361666490962538945, 0.9906859460363297565 ) ) ;
#13032=ORIENTED_EDGE ( 'NONE', *, *, #17967, .T. ) ;
#13038=DIRECTION ( 'NONE',  ( 0.000000000000000000, 0.000000000000000000, 1.000000000000000000 ) ) ;
#13046=CIRCLE ( 'NONE', #3884, 27.60000000002759535 ) ;
#13049=DIRECTION ( 'NONE',  ( -1.000000000000000000, 0.000000000000000000, 0.000000000000000000 ) ) ;
#13050=EDGE_LOOP ( 'NONE', ( #9534, #7976, #18974, #16606 ) ) ;
#13051=DIRECTION ( 'NONE',  ( -1.000000000000000000, -0.000000000000000000, 0.000000000000000000 ) ) ;
#13054=ORIENTED_EDGE ( 'NONE', *, *, #18542, .F. ) ;
#13058=DIRECTION ( 'NONE',  ( 0.000000000000000000, 0.000000000000000000, -1.000000000000000000 ) ) ;
#13060=ORIENTED_EDGE ( 'NONE', *, *, #9782, .F. ) ;
#13061=ORIENTED_EDGE ( 'NONE', *, *, #20901, .T. ) ;
#13062=CARTESIAN_POINT ( 'NONE',  ( -10.00000000000000000, 0.000000000000000000, 0.000000000000000000 ) ) ;
#13064=SHAPE_REPRESENTATION ( 'spur gear_iso_ISO - Spur gear 3M 46T 20PA 20FW ---S46C15H150L8.0S1', ( #12461 ), #5631 ) ;
#13066=CARTESIAN_POINT ( 'NONE',  ( 19.99999999999999645, 63.05226888949912478, -15.11556105343395906 ) ) ;
#13069=ORIENTED_EDGE ( 'NONE', *, *, #15009, .F. ) ;
#13072=FACE_OUTER_BOUND ( 'NONE', #13964, .T. ) ;
#13083=ORIENTED_EDGE ( 'NONE', *, *, #2989, .F. ) ;
#13084=CARTESIAN_POINT ( 'NONE',  ( 19.99999999999999645, 64.79224928664386596, 2.456263514198732345 ) ) ;
#13089=CIRCLE ( 'NONE', #4297, 65.24900000006525147 ) ;
#13091=AXIS2_PLACEMENT_3D ( 'NONE', #1125, #2913, #17644 ) ;
#13093=DIRECTION ( 'NONE',  ( -1.000000000000000000, 0.000000000000000000, 0.000000000000000000 ) ) ;
#13095=ORIENTED_EDGE ( 'NONE', *, *, #12344, .T. ) ;
#13103=EDGE_CURVE ( 'NONE', #2180, #16859, #14924, .T. ) ;
#13104=CARTESIAN_POINT ( 'NONE',  ( 19.99999999999999645, 61.72688495901613948, -19.84591825364033468 ) ) ;
#13108=VECTOR ( 'NONE', #12399, 1000.000000000000000 ) ;
#13111=ORIENTED_EDGE ( 'NONE', *, *, #7903, .T. ) ;
#13118=DIRECTION ( 'NONE',  ( 0.000000000000000000, 0.000000000000000000, 1.000000000000000000 ) ) ;
#13127=CARTESIAN_POINT ( 'NONE',  ( 20.00000000000000000, 0.000000000000000000, 0.000000000000000000 ) ) ;
#13128=CARTESIAN_POINT ( 'NONE',  ( 19.99999999999999645, 0.000000000000000000, 0.000000000000000000 ) ) ;
#13131=EDGE_CURVE ( 'NONE', #16859, #9681, #12099, .T. ) ;
#13132=LINE ( 'NONE', #3269, #12270 ) ;
#13133=CIRCLE ( 'NONE', #15838, 72.00000000007199219 ) ;
#13136=FACE_OUTER_BOUND ( 'NONE', #13563, .T. ) ;
#13141=CARTESIAN_POINT ( 'NONE',  ( 19.99999999999999645, 65.23577793412344761, 1.313498510941937036 ) ) ;
#13142=ORIENTED_EDGE ( 'NONE', *, *, #11594, .T. ) ;
#13145=ORIENTED_EDGE ( 'NONE', *, *, #8321, .F. ) ;
#13148=DIRECTION ( 'NONE',  ( 0.000000000000000000, 0.8878852184023731109, 0.4600650377311562012 ) ) ;
#13150=EDGE_CURVE ( 'NONE', #13592, #6079, #9737, .T. ) ;
#13154=LINE ( 'NONE', #14439, #15397 ) ;
#13159=DIRECTION ( 'NONE',  ( -1.000000000000000000, 0.000000000000000000, 0.000000000000000000 ) ) ;
#13167=EDGE_LOOP ( 'NONE', ( #18253, #19075, #13327, #6996 ) ) ;
#13171=CARTESIAN_POINT ( 'NONE',  ( 0.000000000000000000, 0.000000000000000000, 0.000000000000000000 ) ) ;
#13173=ORIENTED_EDGE ( 'NONE', *, *, #16847, .T. ) ;
#13188=CYLINDRICAL_SURFACE ( 'NONE', #5754, 27.60000000002759535 ) ;
#13192=ORIENTED_EDGE ( 'NONE', *, *, #5389, .F. ) ;
#13194=VECTOR ( 'NONE', #7265, 1000.000000000000000 ) ;
#13197=EDGE_LOOP ( 'NONE', ( #9774, #1743, #13293, #9279 ) ) ;
#13200=ORIENTED_EDGE ( 'NONE', *, *, #16316, .F. ) ;
#13201=DIRECTION ( 'NONE',  ( -1.000000000000000000, -0.000000000000000000, -0.000000000000000000 ) ) ;
#13202=EDGE_LOOP ( 'NONE', ( #17987, #1104, #20817, #10835 ) ) ;
#13205=DIRECTION ( 'NONE',  ( 0.000000000000000000, 0.9790840876823234673, -0.2034560130526309185 ) ) ;
#13207=CARTESIAN_POINT ( 'NONE',  ( 19.99999999999999645, -64.52323195238624010, -6.389157729493822657 ) ) ;
#13211=VECTOR ( 'NONE', #6792, 1000.000000000000000 ) ;
#13212=EDGE_LOOP ( 'NONE', ( #18705, #497, #19124, #12552 ) ) ;
#13220=ORIENTED_EDGE ( 'NONE', *, *, #11106, .F. ) ;
#13223=CYLINDRICAL_SURFACE ( 'NONE', #9746, 65.24900000006525147 ) ;
#13239=ADVANCED_FACE ( 'NONE', ( #20422 ), #12156, .T. ) ;
#13241=CARTESIAN_POINT ( 'NONE',  ( 0.000000000000000000, 71.76067541710858677, -5.865617076723870227 ) ) ;
#13243=AXIS2_PLACEMENT_3D ( 'NONE', #14212, #2663, #7837 ) ;
#13244=CARTESIAN_POINT ( 'NONE',  ( 0.000000000000000000, -46.01927912072495275, -45.67597560296436399 ) ) ;
#13246=CARTESIAN_POINT ( 'NONE',  ( 19.99999999999999645, 0.000000000000000000, 0.000000000000000000 ) ) ;
#13247=EDGE_CURVE ( 'NONE', #18653, #19379, #2942, .T. ) ;
#13250=DIRECTION ( 'NONE',  ( 0.000000000000000000, 0.000000000000000000, 1.000000000000000000 ) ) ;
#13252=CIRCLE ( 'NONE', #13955, 65.24900000006525147 ) ;
#13258=AXIS2_PLACEMENT_3D ( 'NONE', #19900, #5376, #10259 ) ;
#13266=ORIENTED_EDGE ( 'NONE', *, *, #3058, .F. ) ;
#13267=EDGE_LOOP ( 'NONE', ( #17931, #4955, #5328, #4563 ) ) ;
#13268=DIRECTION ( 'NONE',  ( -1.000000000000000000, -0.000000000000000000, -0.000000000000000000 ) ) ;
#13269=EDGE_CURVE ( 'NONE', #2640, #3338, #4951, .T. ) ;
#13270=CARTESIAN_POINT ( 'NONE',  ( 9.999999999999998224, 51.96384592647267908, -49.83732252579563493 ) ) ;
#13272=AXIS2_PLACEMENT_3D ( 'NONE', #17752, #3221, #9689 ) ;
#13273=DIRECTION ( 'NONE',  ( -1.000000000000000000, 0.000000000000000000, -0.000000000000000000 ) ) ;
#13276=FACE_OUTER_BOUND ( 'NONE', #16114, .T. ) ;
#13277=CYLINDRICAL_SURFACE ( 'NONE', #7096, 72.00000000007199219 ) ;
#13278=LINE ( 'NONE', #12973, #14040 ) ;
#13287=AXIS2_PLACEMENT_3D ( 'NONE', #1519, #13051, #20785 ) ;
#13288=DIRECTION ( 'NONE',  ( 0.000000000000000000, -0.7308359642781160348, -0.6825531432186625613 ) ) ;
#13290=DIRECTION ( 'NONE',  ( 0.000000000000000000, 0.2697967711570183891, 0.9629172873478009098 ) ) ;
#13293=ORIENTED_EDGE ( 'NONE', *, *, #7241, .T. ) ;
#13296=DIRECTION ( 'NONE',  ( -1.000000000000000000, -0.000000000000000000, -0.000000000000000000 ) ) ;
#13297=CARTESIAN_POINT ( 'NONE',  ( -65.00002539999999840, 0.000000000000000000, 4.000000000000000000 ) ) ;
#13307=ORIENTED_EDGE ( 'NONE', *, *, #19562, .F. ) ;
#13308=DIRECTION ( 'NONE',  ( -1.000000000000000000, -0.000000000000000000, -0.000000000000000000 ) ) ;
#13309=ORIENTED_EDGE ( 'NONE', *, *, #18542, .T. ) ;
#13312=DIRECTION ( 'NONE',  ( 0.000000000000000000, 0.000000000000000000, 1.000000000000000000 ) ) ;
#13318=AXIS2_PLACEMENT_3D ( 'NONE', #12991, #5338, #19444 ) ;
#13321=ORIENTED_EDGE ( 'NONE', *, *, #15191, .F. ) ;
#13323=DIRECTION ( 'NONE',  ( 0.000000000000000000, 0.000000000000000000, 1.000000000000000000 ) ) ;
#13326=AXIS2_PLACEMENT_3D ( 'NONE', #13022, #9732, #8133 ) ;
#13327=ORIENTED_EDGE ( 'NONE', *, *, #3568, .F. ) ;
#13329=DIRECTION ( 'NONE',  ( -1.000000000000000000, -0.000000000000000000, 0.000000000000000000 ) ) ;
#13333=CIRCLE ( 'NONE', #9264, 72.00000000007199219 ) ;
#13343=VECTOR ( 'NONE', #15021, 1000.000000000000000 ) ;
#13346=CARTESIAN_POINT ( 'NONE',  ( 19.99999999999999645, -64.36139404985985379, 32.27399814043853610 ) ) ;
#13350=DIRECTION ( 'NONE',  ( -1.000000000000000000, 0.000000000000000000, 0.000000000000000000 ) ) ;
#13351=EDGE_CURVE ( 'NONE', #11746, #6180, #1636, .T. ) ;
#13354=DIRECTION ( 'NONE',  ( 0.000000000000000000, 0.000000000000000000, -1.000000000000000000 ) ) ;
#13355=FACE_OUTER_BOUND ( 'NONE', #13549, .T. ) ;
#13358=VECTOR ( 'NONE', #5207, 1000.000000000000000 ) ;
#13361=CARTESIAN_POINT ( 'NONE',  ( 19.99999999999999645, 48.70996102988739551, -42.79495875147724604 ) ) ;
#13363=CIRCLE ( 'NONE', #11325, 65.24900000006526568 ) ;
#13369=ORIENTED_EDGE ( 'NONE', *, *, #3142, .T. ) ;
#13372=DIRECTION ( 'NONE',  ( 0.000000000000000000, 0.000000000000000000, -1.000000000000000000 ) ) ;
#13374=EDGE_CURVE ( 'NONE', #18597, #3064, #16563, .T. ) ;
#13377=ORIENTED_EDGE ( 'NONE', *, *, #11371, .T. ) ;
#13385=EDGE_CURVE ( 'NONE', #13609, #2919, #16795, .T. ) ;
#13388=CARTESIAN_POINT ( 'NONE',  ( 0.000000000000000000, -54.08351995568681048, -35.76369202524558233 ) ) ;
#13394=EDGE_CURVE ( 'NONE', #10678, #11409, #17873, .T. ) ;
#13395=EDGE_LOOP ( 'NONE', ( #10084, #9833, #10710, #4899 ) ) ;
#13396=CARTESIAN_POINT ( 'NONE',  ( 19.99999999999999645, 0.000000000000000000, 0.000000000000000000 ) ) ;
#13400=ORIENTED_EDGE ( 'NONE', *, *, #16550, .F. ) ;
#13402=DIRECTION ( 'NONE',  ( 0.000000000000000000, 0.000000000000000000, 1.000000000000000000 ) ) ;
#13403=CARTESIAN_POINT ( 'NONE',  ( 0.000000000000000000, 0.000000000000000000, 0.000000000000000000 ) ) ;
#13408=CIRCLE ( 'NONE', #8636, 27.60000000002759890 ) ;
#13409=DIRECTION ( 'NONE',  ( -1.000000000000000000, -0.000000000000000000, 0.000000000000000000 ) ) ;
#13411=ORIENTED_EDGE ( 'NONE', *, *, #15161, .T. ) ;
#13412=EDGE_CURVE ( 'NONE', #11338, #3544, #20569, .T. ) ;
#13418=ORIENTED_EDGE ( 'NONE', *, *, #17151, .F. ) ;
#13420=DIRECTION ( 'NONE',  ( -1.000000000000000000, 0.000000000000000000, -0.000000000000000000 ) ) ;
#13422=ORIENTED_EDGE ( 'NONE', *, *, #9057, .F. ) ;
#13426=CIRCLE ( 'NONE', #13091, 4.000000000000000000 ) ;
#13428=EDGE_CURVE ( 'NONE', #8227, #20014, #19501, .T. ) ;
#13432=CIRCLE ( 'NONE', #575, 27.60000000002760245 ) ;
#13435=ORIENTED_EDGE ( 'NONE', *, *, #13908, .F. ) ;
#13437=VECTOR ( 'NONE', #9418, 1000.000000000000000 ) ;
#13445=FACE_OUTER_BOUND ( 'NONE', #7014, .T. ) ;
#13449=LINE ( 'NONE', #11636, #12272 ) ;
#13450=EDGE_LOOP ( 'NONE', ( #2848, #16536, #1148, #11244 ) ) ;
#13457=VECTOR ( 'NONE', #5959, 1000.000000000000000 ) ;
#13458=CARTESIAN_POINT ( 'NONE',  ( 19.99999999999999645, 59.31169354540738681, 27.19476070466876649 ) ) ;
#13468=CARTESIAN_POINT ( 'NONE',  ( 19.99999999999999645, 0.000000000000000000, 0.000000000000000000 ) ) ;
#13471=ORIENTED_EDGE ( 'NONE', *, *, #17627, .F. ) ;
#13478=DIRECTION ( 'NONE',  ( -1.000000000000000000, -0.000000000000000000, 0.000000000000000000 ) ) ;
#13479=CYLINDRICAL_SURFACE ( 'NONE', #14777, 65.24900000006525147 ) ;
#13485=EDGE_CURVE ( 'NONE', #15210, #18587, #13133, .T. ) ;
#13486=FACE_OUTER_BOUND ( 'NONE', #12230, .T. ) ;
#13488=CARTESIAN_POINT ( 'NONE',  ( 19.99999999999999645, -36.54710069451090959, 54.05313526368099986 ) ) ;
#13489=ADVANCED_FACE ( 'NONE', ( #5640 ), #10317, .T. ) ;
#13492=DIRECTION ( 'NONE',  ( 0.000000000000000000, -0.2697967711570314897, 0.9629172873477973571 ) ) ;
#13498=VERTEX_POINT ( 'NONE', #10426 ) ;
#13505=FACE_OUTER_BOUND ( 'NONE', #14774, .T. ) ;
#13508=ADVANCED_FACE ( 'NONE', ( #16981 ), #19944, .T. ) ;
#13522=ORIENTED_EDGE ( 'NONE', *, *, #12265, .F. ) ;
#13527=EDGE_LOOP ( 'NONE', ( #3537, #18794, #5252, #4371 ) ) ;
#13530=DIRECTION ( 'NONE',  ( -1.000000000000000000, -0.000000000000000000, -0.000000000000000000 ) ) ;
#13534=FACE_OUTER_BOUND ( 'NONE', #3541, .T. ) ;
#13535=LINE ( 'NONE', #7375, #7088 ) ;
#13536=AXIS2_PLACEMENT_3D ( 'NONE', #1541, #17437, #3013 ) ;
#13539=CARTESIAN_POINT ( 'NONE',  ( -10.00000000000000000, 0.000000000000000000, 0.000000000000000000 ) ) ;
#13540=ORIENTED_EDGE ( 'NONE', *, *, #1611, .T. ) ;
#13545=ORIENTED_EDGE ( 'NONE', *, *, #20724, .F. ) ;
#13546=DIRECTION ( 'NONE',  ( -1.000000000000000000, -0.000000000000000000, 0.000000000000000000 ) ) ;
#13549=EDGE_LOOP ( 'NONE', ( #6650, #18883, #1293, #6748 ) ) ;
#13551=CIRCLE ( 'NONE', #3069, 27.60000000002759890 ) ;
#13555=DIRECTION ( 'NONE',  ( -1.000000000000000000, -0.000000000000000000, -0.000000000000000000 ) ) ;
#13558=EDGE_CURVE ( 'NONE', #12428, #8862, #12416, .T. ) ;
#13563=EDGE_LOOP ( 'NONE', ( #11946, #8001, #16657, #10748 ) ) ;
#13565=CIRCLE ( 'NONE', #702, 72.00000000007199219 ) ;
#13571=CARTESIAN_POINT ( 'NONE',  ( 19.99999999999999645, -23.08379033237309841, -61.02926039941459635 ) ) ;
#13575=ORIENTED_EDGE ( 'NONE', *, *, #6223, .T. ) ;
#13577=CARTESIAN_POINT ( 'NONE',  ( 19.99999999999999645, -49.77519642624036322, 42.18840861821767163 ) ) ;
#13579=AXIS2_PLACEMENT_3D ( 'NONE', #5133, #8318, #18080 ) ;
#13582=AXIS2_PLACEMENT_3D ( 'NONE', #18135, #1823, #6684 ) ;
#13585=LINE ( 'NONE', #20033, #17403 ) ;
#13586=ORIENTED_EDGE ( 'NONE', *, *, #13601, .F. ) ;
#13592=VERTEX_POINT ( 'NONE', #16887 ) ;
#13594=FACE_OUTER_BOUND ( 'NONE', #14831, .T. ) ;
#13596=DIRECTION ( 'NONE',  ( -1.000000000000000000, -0.000000000000000000, 0.000000000000000000 ) ) ;
#13597=DIRECTION ( 'NONE',  ( -1.000000000000000000, 0.000000000000000000, 0.000000000000000000 ) ) ;
#13599=CYLINDRICAL_SURFACE ( 'NONE', #8996, 65.24900000006525147 ) ;
#13601=EDGE_CURVE ( 'NONE', #10695, #9587, #13761, .T. ) ;
#13604=CARTESIAN_POINT ( 'NONE',  ( 0.000000000000000000, 64.36139404985965484, 32.27399814043899084 ) ) ;
#13605=EDGE_CURVE ( 'NONE', #3634, #9449, #15453, .T. ) ;
#13606=CARTESIAN_POINT ( 'NONE',  ( 19.99999999999999645, -35.35772184876915958, 54.34979580218180928 ) ) ;
#13609=VERTEX_POINT ( 'NONE', #13821 ) ;
#13610=DIRECTION ( 'NONE',  ( -1.000000000000000000, 0.000000000000000000, 0.000000000000000000 ) ) ;
#13612=ORIENTED_EDGE ( 'NONE', *, *, #12046, .T. ) ;
#13615=ORIENTED_EDGE ( 'NONE', *, *, #8721, .F. ) ;
#13618=DIRECTION ( 'NONE',  ( 0.000000000000000000, 0.000000000000000000, 1.000000000000000000 ) ) ;
#13630=FACE_OUTER_BOUND ( 'NONE', #16361, .T. ) ;
#13637=DIRECTION ( 'NONE',  ( 0.000000000000000000, 0.7308359642781252496, -0.6825531432186529024 ) ) ;
#13638=VECTOR ( 'NONE', #12995, 1000.000000000000000 ) ;
#13639=EDGE_CURVE ( 'NONE', #4610, #18559, #12437, .T. ) ;
#13641=EDGE_CURVE ( 'NONE', #3544, #5249, #13432, .T. ) ;
#13644=CIRCLE ( 'NONE', #13318, 27.60000000002759890 ) ;
#13646=ORIENTED_EDGE ( 'NONE', *, *, #11064, .T. ) ;
#13650=ORIENTED_EDGE ( 'NONE', *, *, #4617, .F. ) ;
#13655=EDGE_LOOP ( 'NONE', ( #5415, #18808, #5322, #7452 ) ) ;
#13656=CIRCLE ( 'NONE', #7206, 72.00000000007199219 ) ;
#13658=CYLINDRICAL_SURFACE ( 'NONE', #12421, 27.60000000002759890 ) ;
#13659=DIRECTION ( 'NONE',  ( 0.000000000000000000, 0.000000000000000000, 1.000000000000000000 ) ) ;
#13662=DIRECTION ( 'NONE',  ( 1.000000000000000000, 0.000000000000000000, 0.000000000000000000 ) ) ;
#13664=CIRCLE ( 'NONE', #18757, 27.60000000002759890 ) ;
#13665=PRODUCT_DEFINITION_CONTEXT ( 'detailed design', #4399, 'design' ) ;
#13670=AXIS2_PLACEMENT_3D ( 'NONE', #7679, #2908, #9378 ) ;
#13671=DIRECTION ( 'NONE',  ( -1.000000000000000000, -0.000000000000000000, 0.000000000000000000 ) ) ;
#13677=CIRCLE ( 'NONE', #10596, 72.00000000007199219 ) ;
#13680=VERTEX_POINT ( 'NONE', #14456 ) ;
#13684=ORIENTED_EDGE ( 'NONE', *, *, #4356, .T. ) ;
#13686=CYLINDRICAL_SURFACE ( 'NONE', #11391, 65.24900000006525147 ) ;
#13687=EDGE_CURVE ( 'NONE', #12561, #17222, #16810, .T. ) ;
#13688=CIRCLE ( 'NONE', #4550, 72.00000000007199219 ) ;
#13691=CARTESIAN_POINT ( 'NONE',  ( 19.99999999999999645, 0.000000000000000000, 0.000000000000000000 ) ) ;
#13694=FACE_OUTER_BOUND ( 'NONE', #15012, .T. ) ;
#13696=DIRECTION ( 'NONE',  ( -1.000000000000000000, -0.000000000000000000, -0.000000000000000000 ) ) ;
#13704=ORIENTED_EDGE ( 'NONE', *, *, #10802, .T. ) ;
#13705=CARTESIAN_POINT ( 'NONE',  ( 19.99999999999999645, 64.79224928664392280, -2.456263514197840614 ) ) ;
#13706=DIRECTION ( 'NONE',  ( 1.000000000000000000, 0.000000000000000000, 0.000000000000000000 ) ) ;
#13708=VERTEX_POINT ( 'NONE', #10945 ) ;
#13720=CARTESIAN_POINT ( 'NONE',  ( 19.99999999999999645, 63.85430960833490843, -11.25592921604860663 ) ) ;
#13728=CARTESIAN_POINT ( 'NONE',  ( 19.99999999999999645, 24.01204443665271882, -60.22865198596099390 ) ) ;
#13731=ORIENTED_EDGE ( 'NONE', *, *, #20511, .F. ) ;
#13733=EDGE_LOOP ( 'NONE', ( #3517, #2582, #17525, #14672 ) ) ;
#13735=AXIS2_PLACEMENT_3D ( 'NONE', #7551, #12767, #5962 ) ;
#13737=CARTESIAN_POINT ( 'NONE',  ( 0.000000000000000000, 68.15657073222466522, -23.20952102120210725 ) ) ;
#13744=CARTESIAN_POINT ( 'NONE',  ( 9.999999999999998224, -46.17500197033096043, 55.24372537266381755 ) ) ;
#13746=CARTESIAN_POINT ( 'NONE',  ( 19.99999999999999645, -53.26727847779503833, -48.44168704307685402 ) ) ;
#13749=CARTESIAN_POINT ( 'NONE',  ( 19.99999999999999645, 27.80658314415318699, -66.41380830714092554 ) ) ;
#13751=CIRCLE ( 'NONE', #20565, 27.60000000002759890 ) ;
#13752=CIRCLE ( 'NONE', #10030, 65.24900000006525147 ) ;
#13753=ORIENTED_EDGE ( 'NONE', *, *, #10644, .T. ) ;
#13757=FACE_OUTER_BOUND ( 'NONE', #2234, .T. ) ;
#13758=ORIENTED_EDGE ( 'NONE', *, *, #5355, .T. ) ;
#13759=DIRECTION ( 'NONE',  ( 0.000000000000000000, 0.000000000000000000, -1.000000000000000000 ) ) ;
#13761=CIRCLE ( 'NONE', #18852, 27.60000000002760245 ) ;
#13762=VERTEX_POINT ( 'NONE', #7658 ) ;
#13763=VERTEX_POINT ( 'NONE', #14137 ) ;
#13765=EDGE_CURVE ( 'NONE', #11920, #2829, #3273, .T. ) ;
#13766=CIRCLE ( 'NONE', #6639, 27.60000000002759890 ) ;
#13767=DIRECTION ( 'NONE',  ( -1.000000000000000000, 0.000000000000000000, 0.000000000000000000 ) ) ;
#13768=CIRCLE ( 'NONE', #12067, 27.60000000002760245 ) ;
#13773=VECTOR ( 'NONE', #2307, 1000.000000000000000 ) ;
#13776=CARTESIAN_POINT ( 'NONE',  ( 19.99999999999999645, 46.17500197033132281, -55.24372537266349781 ) ) ;
#13781=AXIS2_PLACEMENT_3D ( 'NONE', #9438, #9121, #12732 ) ;
#13782=CARTESIAN_POINT ( 'NONE',  ( 19.99999999999999645, 63.17103598352126426, 16.33561182745161844 ) ) ;
#13785=CIRCLE ( 'NONE', #10750, 72.00000000007199219 ) ;
#13787=LINE ( 'NONE', #851, #17171 ) ;
#13788=VERTEX_POINT ( 'NONE', #4787 ) ;
#13789=FACE_OUTER_BOUND ( 'NONE', #18260, .T. ) ;
#13792=CARTESIAN_POINT ( 'NONE',  ( 9.999999999999998224, -20.34307325858738835, -69.06634035770328239 ) ) ;
#13794=CIRCLE ( 'NONE', #3303, 72.00000000007199219 ) ;
#13798=EDGE_CURVE ( 'NONE', #5677, #9154, #5198, .T. ) ;
#13799=AXIS2_PLACEMENT_3D ( 'NONE', #15131, #11945, #18418 ) ;
#13802=AXIS2_PLACEMENT_3D ( 'NONE', #3230, #12988, #8202 ) ;
#13803=CARTESIAN_POINT ( 'NONE',  ( 85.00002539999999840, 0.000000000000000000, 0.000000000000000000 ) ) ;
#13804=CIRCLE ( 'NONE', #16506, 65.24900000006525147 ) ;
#13807=CARTESIAN_POINT ( 'NONE',  ( 0.000000000000000000, 27.80658314415226329, 66.41380830714133765 ) ) ;
#13810=EDGE_LOOP ( 'NONE', ( #1028, #20505, #16278, #13095 ) ) ;
#13813=ORIENTED_EDGE ( 'NONE', *, *, #10392, .T. ) ;
#13817=FACE_OUTER_BOUND ( 'NONE', #12346, .T. ) ;
#13818=ORIENTED_EDGE ( 'NONE', *, *, #9840, .T. ) ;
#13820=CARTESIAN_POINT ( 'NONE',  ( 0.000000000000000000, -20.34307325858834048, 69.06634035770301239 ) ) ;
#13821=CARTESIAN_POINT ( 'NONE',  ( 0.000000000000000000, -71.76067541710847308, -5.865617076725382795 ) ) ;
#13822=VECTOR ( 'NONE', #4049, 1000.000000000000000 ) ;
#13825=DIRECTION ( 'NONE',  ( 0.000000000000000000, 0.000000000000000000, -1.000000000000000000 ) ) ;
#13827=FACE_OUTER_BOUND ( 'NONE', #11658, .T. ) ;
#13828=DIRECTION ( 'NONE',  ( -1.000000000000000000, 0.000000000000000000, 0.000000000000000000 ) ) ;
#13830=ORIENTED_EDGE ( 'NONE', *, *, #19688, .F. ) ;
#13831=CYLINDRICAL_SURFACE ( 'NONE', #2386, 72.00000000007199219 ) ;
#13835=EDGE_CURVE ( 'NONE', #18949, #19322, #3606, .T. ) ;
#13848=VERTEX_POINT ( 'NONE', #19412 ) ;
#13851=CARTESIAN_POINT ( 'NONE',  ( 19.99999999999999645, 63.17103598352126426, 16.33561182745161844 ) ) ;
#13854=CARTESIAN_POINT ( 'NONE',  ( 0.000000000000000000, 0.000000000000000000, 0.000000000000000000 ) ) ;
#13855=ORIENTED_EDGE ( 'NONE', *, *, #12625, .T. ) ;
#13859=EDGE_CURVE ( 'NONE', #9479, #17758, #16464, .T. ) ;
#13861=ORIENTED_EDGE ( 'NONE', *, *, #5836, .F. ) ;
#13862=CARTESIAN_POINT ( 'NONE',  ( 0.000000000000000000, 0.000000000000000000, 0.000000000000000000 ) ) ;
#13868=FACE_OUTER_BOUND ( 'NONE', #5956, .T. ) ;
#13871=EDGE_CURVE ( 'NONE', #7712, #19326, #1268, .T. ) ;
#13878=ORIENTED_EDGE ( 'NONE', *, *, #20155, .F. ) ;
#13897=EDGE_CURVE ( 'NONE', #645, #17111, #7315, .T. ) ;
#13899=DIRECTION ( 'NONE',  ( 0.000000000000000000, 0.000000000000000000, 1.000000000000000000 ) ) ;
#13902=AXIS2_PLACEMENT_3D ( 'NONE', #14865, #3925, #339 ) ;
#13903=LINE ( 'NONE', #12104, #5787 ) ;
#13904=FACE_OUTER_BOUND ( 'NONE', #16128, .T. ) ;
#13905=EDGE_CURVE ( 'NONE', #4471, #8788, #214, .T. ) ;
#13906=CARTESIAN_POINT ( 'NONE',  ( 19.99999999999999645, 51.96384592647266487, -49.83732252579562783 ) ) ;
#13907=DIRECTION ( 'NONE',  ( 0.000000000000000000, 0.6310879443260540844, -0.7757112907044187988 ) ) ;
#13908=EDGE_CURVE ( 'NONE', #16884, #8077, #19179, .T. ) ;
#13910=DIRECTION ( 'NONE',  ( -1.000000000000000000, -0.000000000000000000, -0.000000000000000000 ) ) ;
#13914=ORIENTED_EDGE ( 'NONE', *, *, #19809, .F. ) ;
#13915=DIRECTION ( 'NONE',  ( 0.000000000000000000, 0.000000000000000000, 1.000000000000000000 ) ) ;
#13918=DIRECTION ( 'NONE',  ( -1.000000000000000000, -0.000000000000000000, -0.000000000000000000 ) ) ;
#13919=DIRECTION ( 'NONE',  ( 0.000000000000000000, 0.000000000000000000, 1.000000000000000000 ) ) ;
#13920=DIRECTION ( 'NONE',  ( 0.000000000000000000, 0.000000000000000000, 1.000000000000000000 ) ) ;
#13921=ADVANCED_FACE ( 'NONE', ( #2436 ), #13479, .T. ) ;
#13928=AXIS2_PLACEMENT_3D ( 'NONE', #18560, #6889, #13372 ) ;
#13929=VERTEX_POINT ( 'NONE', #15062 ) ;
#13930=SURFACE_STYLE_USAGE ( .BOTH. , #9155 ) ;
#13931=CARTESIAN_POINT ( 'NONE',  ( 0.000000000000000000, 63.85430960833475211, 11.25592921604948948 ) ) ;
#13932=ORIENTED_EDGE ( 'NONE', *, *, #14431, .T. ) ;
#13935=DIRECTION ( 'NONE',  ( 0.000000000000000000, -1.000000000000000000, 0.000000000000000000 ) ) ;
#13941=EDGE_LOOP ( 'NONE', ( #11777, #6940, #8311, #7591 ) ) ;
#13943=CARTESIAN_POINT ( 'NONE',  ( 19.99999999999999645, 27.62776854598856602, 58.65812137499012380 ) ) ;
#13947=VERTEX_POINT ( 'NONE', #2129 ) ;
#13948=AXIS2_PLACEMENT_3D ( 'NONE', #8409, #4641, #14881 ) ;
#13949=DIRECTION ( 'NONE',  ( -1.000000000000000000, -0.000000000000000000, 0.000000000000000000 ) ) ;
#13954=AXIS2_PLACEMENT_3D ( 'NONE', #4296, #5887, #1018 ) ;
#13955=AXIS2_PLACEMENT_3D ( 'NONE', #11480, #6593, #8099 ) ;
#13957=DIRECTION ( 'NONE',  ( 0.000000000000000000, -0.7308359642781160348, -0.6825531432186625613 ) ) ;
#13959=VERTEX_POINT ( 'NONE', #9015 ) ;
#13962=CARTESIAN_POINT ( 'NONE',  ( 19.99999999999999645, 68.15657073222466522, -23.20952102120210370 ) ) ;
#13963=CARTESIAN_POINT ( 'NONE',  ( 19.99999999999999645, -3.141410481201533322, 65.17333458706184501 ) ) ;
#13964=EDGE_LOOP ( 'NONE', ( #18384, #16335, #15620, #16771 ) ) ;
#13975=ORIENTED_EDGE ( 'NONE', *, *, #2819, .F. ) ;
#13979=CYLINDRICAL_SURFACE ( 'NONE', #8515, 65.24900000006525147 ) ;
#13980=DIRECTION ( 'NONE',  ( -1.000000000000000000, -0.000000000000000000, 0.000000000000000000 ) ) ;
#13982=AXIS2_PLACEMENT_3D ( 'NONE', #20520, #8969, #2712 ) ;
#13986=CIRCLE ( 'NONE', #1784, 72.00000000007199219 ) ;
#13987=DIRECTION ( 'NONE',  ( -1.000000000000000000, 0.000000000000000000, 0.000000000000000000 ) ) ;
#13989=VECTOR ( 'NONE', #12924, 1000.000000000000000 ) ;
#13993=CARTESIAN_POINT ( 'NONE',  ( 19.99999999999999645, 0.000000000000000000, 0.000000000000000000 ) ) ;
#13996=AXIS2_PLACEMENT_3D ( 'NONE', #14727, #11230, #19279 ) ;
#14000=DIRECTION ( 'NONE',  ( -1.000000000000000000, -0.000000000000000000, 0.000000000000000000 ) ) ;
#14002=DIRECTION ( 'NONE',  ( -1.000000000000000000, 0.000000000000000000, 0.000000000000000000 ) ) ;
#14007=CIRCLE ( 'NONE', #4856, 27.60000000002760245 ) ;
#14010=DIRECTION ( 'NONE',  ( -1.000000000000000000, 0.000000000000000000, 0.000000000000000000 ) ) ;
#14014=AXIS2_PLACEMENT_3D ( 'NONE', #18920, #7678, #15839 ) ;
#14019=CARTESIAN_POINT ( 'NONE',  ( 19.99999999999999645, 0.000000000000000000, 0.000000000000000000 ) ) ;
#14020=AXIS2_PLACEMENT_3D ( 'NONE', #20261, #2887, #5738 ) ;
#14023=CARTESIAN_POINT ( 'NONE',  ( -10.00000000000000000, 0.000000000000000000, 0.000000000000000000 ) ) ;
#14025=EDGE_CURVE ( 'NONE', #11443, #20609, #2602, .T. ) ;
#14028=EDGE_CURVE ( 'NONE', #19208, #1859, #17391, .T. ) ;
#14031=VERTEX_POINT ( 'NONE', #9223 ) ;
#14040=VECTOR ( 'NONE', #8095, 1000.000000000000000 ) ;
#14041=DIRECTION ( 'NONE',  ( -1.000000000000000000, 0.000000000000000000, 0.000000000000000000 ) ) ;
#14042=ADVANCED_FACE ( 'NONE', ( #1295 ), #15685, .T. ) ;
#14045=EDGE_LOOP ( 'NONE', ( #1678, #12411, #15730, #10492 ) ) ;
#14048=CARTESIAN_POINT ( 'NONE',  ( 19.99999999999999645, 0.000000000000000000, 0.000000000000000000 ) ) ;
#14049=ORIENTED_EDGE ( 'NONE', *, *, #13351, .F. ) ;
#14050=CARTESIAN_POINT ( 'NONE',  ( 19.99999999999999645, -24.01204443665145405, -60.22865198596149838 ) ) ;
#14056=DIRECTION ( 'NONE',  ( 0.000000000000000000, 0.000000000000000000, 1.000000000000000000 ) ) ;
#14057=EDGE_LOOP ( 'NONE', ( #11246, #13173, #20424, #2552 ) ) ;
#14058=CARTESIAN_POINT ( 'NONE',  ( 19.99999999999999645, 0.000000000000000000, 0.000000000000000000 ) ) ;
#14059=ORIENTED_EDGE ( 'NONE', *, *, #10612, .T. ) ;
#14064=ADVANCED_FACE ( 'NONE', ( #4669 ), #18978, .T. ) ;
#14065=DIRECTION ( 'NONE',  ( 0.000000000000000000, 0.9422609221188191775, 0.3348796121709899376 ) ) ;
#14071=CARTESIAN_POINT ( 'NONE',  ( 19.99999999999999645, 14.55863677812212131, -63.60407295269091321 ) ) ;
#14075=ORIENTED_EDGE ( 'NONE', *, *, #15550, .F. ) ;
#14081=DIRECTION ( 'NONE',  ( 0.000000000000000000, 0.000000000000000000, 1.000000000000000000 ) ) ;
#14089=LINE ( 'NONE', #3998, #6835 ) ;
#14097=AXIS2_PLACEMENT_3D ( 'NONE', #9958, #14541, #3300 ) ;
#14101=EDGE_CURVE ( 'NONE', #7589, #10176, #2664, .T. ) ;
#14106=ORIENTED_EDGE ( 'NONE', *, *, #2323, .F. ) ;
#14107=DIRECTION ( 'NONE',  ( -1.000000000000000000, 0.000000000000000000, 0.000000000000000000 ) ) ;
#14108=ORIENTED_EDGE ( 'NONE', *, *, #7638, .F. ) ;
#14115=CIRCLE ( 'NONE', #1589, 65.24900000006526568 ) ;
#14116=CIRCLE ( 'NONE', #3266, 4.000000000000000000 ) ;
#14118=DIRECTION ( 'NONE',  ( 0.000000000000000000, 0.000000000000000000, 1.000000000000000000 ) ) ;
#14125=CARTESIAN_POINT ( 'NONE',  ( 19.99999999999999645, 64.44931368725534071, -10.18420179740539666 ) ) ;
#14126=CIRCLE ( 'NONE', #14799, 72.00000000007199219 ) ;
#14127=ORIENTED_EDGE ( 'NONE', *, *, #5026, .F. ) ;
#14128=CARTESIAN_POINT ( 'NONE',  ( 19.99999999999999645, 0.000000000000000000, 0.000000000000000000 ) ) ;
#14132=ORIENTED_EDGE ( 'NONE', *, *, #2912, .T. ) ;
#14136=DIRECTION ( 'NONE',  ( -1.000000000000000000, -0.000000000000000000, -0.000000000000000000 ) ) ;
#14137=CARTESIAN_POINT ( 'NONE',  ( 19.99999999999999645, 64.36139404986009538, -32.27399814043807424 ) ) ;
#14139=ORIENTED_EDGE ( 'NONE', *, *, #12244, .T. ) ;
#14145=DIRECTION ( 'NONE',  ( -1.000000000000000000, -0.000000000000000000, -0.000000000000000000 ) ) ;
#14146=DIRECTION ( 'NONE',  ( -1.000000000000000000, 0.000000000000000000, 0.000000000000000000 ) ) ;
#14148=VECTOR ( 'NONE', #17796, 1000.000000000000000 ) ;
#14152=DIRECTION ( 'NONE',  ( -1.000000000000000000, 0.000000000000000000, 0.000000000000000000 ) ) ;
#14153=CARTESIAN_POINT ( 'NONE',  ( 19.99999999999999645, -11.98658579560543025, -64.13855129306480762 ) ) ;
#14164=EDGE_CURVE ( 'NONE', #13959, #16282, #18388, .T. ) ;
#14165=VECTOR ( 'NONE', #17900, 1000.000000000000000 ) ;
#14166=CARTESIAN_POINT ( 'NONE',  ( 19.99999999999999645, -35.35772184876843482, -54.34979580218228534 ) ) ;
#14167=ORIENTED_EDGE ( 'NONE', *, *, #14681, .F. ) ;
#14168=CARTESIAN_POINT ( 'NONE',  ( 0.000000000000000000, 0.000000000000000000, 0.000000000000000000 ) ) ;
#14170=EDGE_CURVE ( 'NONE', #13763, #5352, #14675, .T. ) ;
#14173=EDGE_CURVE ( 'NONE', #5249, #14524, #11284, .T. ) ;
#14174=FACE_OUTER_BOUND ( 'NONE', #6351, .T. ) ;
#14177=VERTEX_POINT ( 'NONE', #1390 ) ;
#14178=FACE_OUTER_BOUND ( 'NONE', #15518, .T. ) ;
#14191=DIRECTION ( 'NONE',  ( 0.000000000000000000, 0.9422609221188191775, 0.3348796121709901041 ) ) ;
#14201=DIRECTION ( 'NONE',  ( -1.000000000000000000, 0.000000000000000000, 0.000000000000000000 ) ) ;
#14203=DIRECTION ( 'NONE',  ( 1.000000000000000000, -0.000000000000000000, -0.000000000000000000 ) ) ;
#14206=CARTESIAN_POINT ( 'NONE',  ( 19.99999999999999645, -59.31169354540756444, 27.19476070466835438 ) ) ;
#14208=CARTESIAN_POINT ( 'NONE',  ( 0.000000000000000000, -71.89099403602357086, 3.960426305688539816 ) ) ;
#14212=CARTESIAN_POINT ( 'NONE',  ( 19.99999999999999645, -54.08351995568681048, -35.76369202524558233 ) ) ;
#14214=ORIENTED_EDGE ( 'NONE', *, *, #18820, .F. ) ;
#14218=EDGE_CURVE ( 'NONE', #16683, #15235, #16016, .T. ) ;
#14220=CARTESIAN_POINT ( 'NONE',  ( 19.99999999999999645, 63.85430960833490843, 16.34407078397899227 ) ) ;
#14224=DIRECTION ( 'NONE',  ( 0.000000000000000000, -0.8878852184023793281, 0.4600650377311439887 ) ) ;
#14226=ORIENTED_EDGE ( 'NONE', *, *, #16875, .T. ) ;
#14230=CARTESIAN_POINT ( 'NONE',  ( 0.000000000000000000, -62.46228066917775834, -18.86519267363519958 ) ) ;
#14231=ORIENTED_EDGE ( 'NONE', *, *, #15323, .T. ) ;
#14233=ORIENTED_EDGE ( 'NONE', *, *, #9885, .F. ) ;
#14235=DIRECTION ( 'NONE',  ( -1.000000000000000000, 0.000000000000000000, -0.000000000000000000 ) ) ;
#14237=AXIS2_PLACEMENT_3D ( 'NONE', #7143, #20186, #3971 ) ;
#14239=DIRECTION ( 'NONE',  ( -1.000000000000000000, 0.000000000000000000, -0.000000000000000000 ) ) ;
#14240=CARTESIAN_POINT ( 'NONE',  ( 19.99999999999999645, -64.80702306891100761, 7.581672767546201008 ) ) ;
#14243=AXIS2_PLACEMENT_3D ( 'NONE', #6288, #11475, #19228 ) ;
#14245=VERTEX_POINT ( 'NONE', #3471 ) ;
#14247=DIRECTION ( 'NONE',  ( 1.000000000000000000, 0.000000000000000000, 0.000000000000000000 ) ) ;
#14249=ORIENTED_EDGE ( 'NONE', *, *, #3531, .F. ) ;
#14254=EDGE_LOOP ( 'NONE', ( #4319, #16645, #171, #7437 ) ) ;
#14258=ORIENTED_EDGE ( 'NONE', *, *, #934, .T. ) ;
#14259=DIRECTION ( 'NONE',  ( -1.000000000000000000, 0.000000000000000000, 0.000000000000000000 ) ) ;
#14260=VERTEX_POINT ( 'NONE', #1795 ) ;
#14261=DIRECTION ( 'NONE',  ( 0.000000000000000000, 0.000000000000000000, 1.000000000000000000 ) ) ;
#14264=EDGE_CURVE ( 'NONE', #15500, #13708, #9257, .T. ) ;
#14267=CARTESIAN_POINT ( 'NONE',  ( 19.99999999999999645, 51.43306257653197378, -40.15061736769512635 ) ) ;
#14269=VERTEX_POINT ( 'NONE', #96 ) ;
#14271=CARTESIAN_POINT ( 'NONE',  ( 0.000000000000000000, 58.44960523466241398, -28.06621538408611016 ) ) ;
#14273=CIRCLE ( 'NONE', #11546, 72.00000000007199219 ) ;
#14275=EDGE_CURVE ( 'NONE', #10180, #5437, #450, .T. ) ;
#14276=CIRCLE ( 'NONE', #5117, 65.24900000006525147 ) ;
#14278=DIRECTION ( 'NONE',  ( -1.000000000000000000, -0.000000000000000000, 0.000000000000000000 ) ) ;
#14279=CARTESIAN_POINT ( 'NONE',  ( 19.99999999999999645, -71.89099403602357086, 3.960426305688543369 ) ) ;
#14281=EDGE_CURVE ( 'NONE', #6859, #788, #6355, .T. ) ;
#14284=CARTESIAN_POINT ( 'NONE',  ( 19.99999999999999645, 11.98658579560678206, -64.13855129306456604 ) ) ;
#14285=AXIS2_PLACEMENT_3D ( 'NONE', #4029, #867, #1085 ) ;
#14302=CARTESIAN_POINT ( 'NONE',  ( -65.00002539999999840, 0.000000000000000000, 0.000000000000000000 ) ) ;
#14303=VERTEX_POINT ( 'NONE', #12815 ) ;
#14307=FACE_OUTER_BOUND ( 'NONE', #854, .T. ) ;
#14315=AXIS2_PLACEMENT_3D ( 'NONE', #10574, #12264, #15341 ) ;
#14319=DIRECTION ( 'NONE',  ( 0.000000000000000000, -0.8169698930104354329, -0.5766803221148764091 ) ) ;
#14326=CYLINDRICAL_SURFACE ( 'NONE', #8560, 27.60000000002760245 ) ;
#14328=AXIS2_PLACEMENT_3D ( 'NONE', #1887, #15209, #2497 ) ;
#14329=AXIS2_PLACEMENT_3D ( 'NONE', #11031, #10730, #15901 ) ;
#14336=CYLINDRICAL_SURFACE ( 'NONE', #12038, 7.500000000000000000 ) ;
#14339=ORIENTED_EDGE ( 'NONE', *, *, #15063, .F. ) ;
#14342=VECTOR ( 'NONE', #9899, 1000.000000000000000 ) ;
#14346=ORIENTED_EDGE ( 'NONE', *, *, #18258, .F. ) ;
#14351=EDGE_CURVE ( 'NONE', #18356, #14556, #13656, .T. ) ;
#14353=LINE ( 'NONE', #9561, #7292 ) ;
#14357=CIRCLE ( 'NONE', #16702, 7.500000000000000000 ) ;
#14361=LINE ( 'NONE', #12775, #529 ) ;
#14362=DIRECTION ( 'NONE',  ( -1.000000000000000000, -0.000000000000000000, -0.000000000000000000 ) ) ;
#14366=EDGE_LOOP ( 'NONE', ( #10358, #16954, #3683, #19217 ) ) ;
#14368=FACE_OUTER_BOUND ( 'NONE', #20692, .T. ) ;
#14370=AXIS2_PLACEMENT_3D ( 'NONE', #3927, #13696, #8488 ) ;
#14371=ORIENTED_EDGE ( 'NONE', *, *, #8305, .T. ) ;
#14372=CIRCLE ( 'NONE', #18403, 65.24900000006525147 ) ;
#14373=CARTESIAN_POINT ( 'NONE',  ( 19.99999999999999645, 0.000000000000000000, 0.000000000000000000 ) ) ;
#14375=CARTESIAN_POINT ( 'NONE',  ( 0.000000000000000000, -29.55812890831937878, -65.65300461859717984 ) ) ;
#14377=ORIENTED_EDGE ( 'NONE', *, *, #16263, .T. ) ;
#14378=VECTOR ( 'NONE', #9992, 1000.000000000000000 ) ;
#14379=CYLINDRICAL_SURFACE ( 'NONE', #15824, 27.60000000002760245 ) ;
#14381=FACE_OUTER_BOUND ( 'NONE', #6135, .T. ) ;
#14385=ORIENTED_EDGE ( 'NONE', *, *, #16550, .T. ) ;
#14394=DIRECTION ( 'NONE',  ( 0.000000000000000000, 0.000000000000000000, 1.000000000000000000 ) ) ;
#14399=CARTESIAN_POINT ( 'NONE',  ( 19.99999999999999645, 64.79224928664392280, -2.456263514197840614 ) ) ;
#14402=DIRECTION ( 'NONE',  ( 0.000000000000000000, 0.000000000000000000, 1.000000000000000000 ) ) ;
#14404=FACE_OUTER_BOUND ( 'NONE', #8903, .T. ) ;
#14414=FACE_OUTER_BOUND ( 'NONE', #7733, .T. ) ;
#14415=CIRCLE ( 'NONE', #6280, 72.00000000007199219 ) ;
#14417=DIRECTION ( 'NONE',  ( -1.000000000000000000, 0.000000000000000000, -0.000000000000000000 ) ) ;
#14419=CARTESIAN_POINT ( 'NONE',  ( 19.99999999999999645, -18.50424539729796791, -69.58155576219134275 ) ) ;
#14431=EDGE_CURVE ( 'NONE', #6278, #833, #9922, .T. ) ;
#14434=ADVANCED_FACE ( 'NONE', ( #9160 ), #18921, .T. ) ;
#14438=CARTESIAN_POINT ( 'NONE',  ( 0.000000000000000000, 3.141410481201071914, 65.17333458706188765 ) ) ;
#14439=CARTESIAN_POINT ( 'NONE',  ( 19.99999999999999645, 3.141410481201988070, -65.17333458706183080 ) ) ;
#14440=CARTESIAN_POINT ( 'NONE',  ( 0.000000000000000000, -63.05226888949880504, -15.11556105343524514 ) ) ;
#14442=ORIENTED_EDGE ( 'NONE', *, *, #2705, .F. ) ;
#14444=CIRCLE ( 'NONE', #15109, 27.60000000002760245 ) ;
#14447=DIRECTION ( 'NONE',  ( -1.000000000000000000, 0.000000000000000000, -0.000000000000000000 ) ) ;
#14450=FACE_OUTER_BOUND ( 'NONE', #13941, .T. ) ;
#14452=EDGE_LOOP ( 'NONE', ( #15274, #2525, #4436, #15139 ) ) ;
#14454=CARTESIAN_POINT ( 'NONE',  ( 19.99999999999999645, -58.26603306961934692, -42.29739224042532442 ) ) ;
#14456=CARTESIAN_POINT ( 'NONE',  ( 0.000000000000000000, -59.36728637277992249, -40.73727173906846843 ) ) ;
#14457=EDGE_LOOP ( 'NONE', ( #7371, #15868, #19817, #11207 ) ) ;
#14459=EDGE_CURVE ( 'NONE', #12652, #10139, #17549, .T. ) ;
#14462=DIRECTION ( 'NONE',  ( -1.000000000000000000, 0.000000000000000000, -0.000000000000000000 ) ) ;
#14469=( GEOMETRIC_REPRESENTATION_CONTEXT ( 3 ) GLOBAL_UNCERTAINTY_ASSIGNED_CONTEXT ( ( #4337 ) ) GLOBAL_UNIT_ASSIGNED_CONTEXT ( ( #4024, #3920, #10404 ) ) REPRESENTATION_CONTEXT ( 'NONE', 'WORKASPACE' ) );
#14470=CARTESIAN_POINT ( 'NONE',  ( 19.99999999999999645, -3.141410481200616278, -65.17333458706190186 ) ) ;
#14472=CARTESIAN_POINT ( 'NONE',  ( 19.99999999999999645, 42.42902769288603082, -49.02903636734153281 ) ) ;
#14473=CARTESIAN_POINT ( 'NONE',  ( 19.99999999999999645, -60.35829202194891252, 24.78524934717529504 ) ) ;
#14474=ORIENTED_EDGE ( 'NONE', *, *, #381, .F. ) ;
#14476=DIRECTION ( 'NONE',  ( 0.000000000000000000, 0.6310879443260485333, 0.7757112907044232397 ) ) ;
#14477=DIRECTION ( 'NONE',  ( -1.000000000000000000, -0.000000000000000000, -0.000000000000000000 ) ) ;
#14481=ORIENTED_EDGE ( 'NONE', *, *, #7927, .T. ) ;
#14488=AXIS2_PLACEMENT_3D ( 'NONE', #5786, #18846, #15760 ) ;
#14490=EDGE_CURVE ( 'NONE', #10560, #17270, #1119, .T. ) ;
#14491=VERTEX_POINT ( 'NONE', #1229 ) ;
#14494=VECTOR ( 'NONE', #13949, 1000.000000000000000 ) ;
#14496=VERTEX_POINT ( 'NONE', #9270 ) ;
#14501=DIRECTION ( 'NONE',  ( 0.000000000000000000, 0.6310879443260485333, 0.7757112907044232397 ) ) ;
#14502=VERTEX_POINT ( 'NONE', #5875 ) ;
#14507=DIRECTION ( 'NONE',  ( 1.000000000000000000, -0.000000000000000000, 0.000000000000000000 ) ) ;
#14509=ORIENTED_EDGE ( 'NONE', *, *, #769, .T. ) ;
#14510=FACE_OUTER_BOUND ( 'NONE', #676, .T. ) ;
#14511=CARTESIAN_POINT ( 'NONE',  ( 9.999999999999998224, -70.68211945903179583, -13.71269443944282607 ) ) ;
#14514=EDGE_LOOP ( 'NONE', ( #16507, #13111, #16521, #6544 ) ) ;
#14515=CARTESIAN_POINT ( 'NONE',  ( 85.00002539999999840, 9.184850993605147944E-16, -7.500000000000000000 ) ) ;
#14516=CARTESIAN_POINT ( 'NONE',  ( 19.99999999999999645, 0.000000000000000000, 0.000000000000000000 ) ) ;
#14519=EDGE_CURVE ( 'NONE', #15789, #8899, #17027, .T. ) ;
#14520=ORIENTED_EDGE ( 'NONE', *, *, #5463, .F. ) ;
#14521=LINE ( 'NONE', #8620, #13989 ) ;
#14523=DIRECTION ( 'NONE',  ( 1.000000000000000000, -0.000000000000000000, -0.000000000000000000 ) ) ;
#14524=VERTEX_POINT ( 'NONE', #15840 ) ;
#14527=CARTESIAN_POINT ( 'NONE',  ( 19.99999999999999645, 64.79224928664392280, -2.456263514197840614 ) ) ;
#14528=CARTESIAN_POINT ( 'NONE',  ( 9.999999999999998224, -36.59093685910671212, 62.00889726308019334 ) ) ;
#14532=CARTESIAN_POINT ( 'NONE',  ( 19.99999999999999645, 0.000000000000000000, 0.000000000000000000 ) ) ;
#14533=EDGE_CURVE ( 'NONE', #4467, #10293, #19098, .T. ) ;
#14540=CYLINDRICAL_SURFACE ( 'NONE', #10847, 65.24900000006525147 ) ;
#14541=DIRECTION ( 'NONE',  ( 1.000000000000000000, 0.000000000000000000, 0.000000000000000000 ) ) ;
#14542=EDGE_CURVE ( 'NONE', #17883, #19366, #16451, .T. ) ;
#14545=EDGE_CURVE ( 'NONE', #12799, #15624, #11633, .T. ) ;
#14550=CARTESIAN_POINT ( 'NONE',  ( 19.99999999999999645, 0.000000000000000000, 0.000000000000000000 ) ) ;
#14551=ORIENTED_EDGE ( 'NONE', *, *, #2294, .T. ) ;
#14556=VERTEX_POINT ( 'NONE', #14763 ) ;
#14557=CARTESIAN_POINT ( 'NONE',  ( 0.000000000000000000, -63.48283426024875808, 33.96954156735347397 ) ) ;
#14558=DIRECTION ( 'NONE',  ( 0.000000000000000000, 0.000000000000000000, 1.000000000000000000 ) ) ;
#14559=DIRECTION ( 'NONE',  ( -1.000000000000000000, 0.000000000000000000, 0.000000000000000000 ) ) ;
#14562=EDGE_CURVE ( 'NONE', #9460, #4144, #5528, .T. ) ;
#14563=AXIS2_PLACEMENT_3D ( 'NONE', #15956, #6003, #20934 ) ;
#14571=DIRECTION ( 'NONE',  ( -1.000000000000000000, 0.000000000000000000, -0.000000000000000000 ) ) ;
#14572=CARTESIAN_POINT ( 'NONE',  ( 19.99999999999999645, -31.17893654894269773, 57.31758819669160232 ) ) ;
#14573=VERTEX_POINT ( 'NONE', #14473 ) ;
#14578=AXIS2_PLACEMENT_3D ( 'NONE', #19931, #1935, #2348 ) ;
#14579=CARTESIAN_POINT ( 'NONE',  ( 19.99999999999999645, 38.69327817041845918, -52.53819777490596010 ) ) ;
#14581=CIRCLE ( 'NONE', #20305, 27.60000000002760245 ) ;
#14589=CARTESIAN_POINT ( 'NONE',  ( -65.00002539999999840, 5.400000000000000355, -1.000000000000000000 ) ) ;
#14590=CARTESIAN_POINT ( 'NONE',  ( 0.000000000000000000, 0.000000000000000000, 0.000000000000000000 ) ) ;
#14591=ORIENTED_EDGE ( 'NONE', *, *, #10129, .F. ) ;
#14592=DIRECTION ( 'NONE',  ( 0.000000000000000000, 0.000000000000000000, -1.000000000000000000 ) ) ;
#14594=ORIENTED_EDGE ( 'NONE', *, *, #13269, .F. ) ;
#14600=CARTESIAN_POINT ( 'NONE',  ( 19.99999999999999645, 59.36728637278018539, 40.73727173906806343 ) ) ;
#14601=CARTESIAN_POINT ( 'NONE',  ( 9.999999999999998224, 29.55812890831981932, 65.65300461859698089 ) ) ;
#14605=CARTESIAN_POINT ( 'NONE',  ( 0.000000000000000000, -63.85430960833497949, 11.25592921604817676 ) ) ;
#14606=CIRCLE ( 'NONE', #2070, 27.60000000002760245 ) ;
#14607=DIRECTION ( 'NONE',  ( -1.000000000000000000, 0.000000000000000000, -0.000000000000000000 ) ) ;
#14609=FACE_OUTER_BOUND ( 'NONE', #372, .T. ) ;
#14613=FACE_OUTER_BOUND ( 'NONE', #19945, .T. ) ;
#14615=LINE ( 'NONE', #91, #15821 ) ;
#14617=LINE ( 'NONE', #19380, #756 ) ;
#14618=AXIS2_PLACEMENT_3D ( 'NONE', #12878, #19323, #11274 ) ;
#14625=DIRECTION ( 'NONE',  ( 0.000000000000000000, 0.000000000000000000, 1.000000000000000000 ) ) ;
#14633=CARTESIAN_POINT ( 'NONE',  ( 19.99999999999999645, 0.000000000000000000, 0.000000000000000000 ) ) ;
#14638=CARTESIAN_POINT ( 'NONE',  ( 19.99999999999999645, -31.98952867950285395, -56.39803944231618971 ) ) ;
#14641=ORIENTED_EDGE ( 'NONE', *, *, #12066, .T. ) ;
#14644=EDGE_LOOP ( 'NONE', ( #6370, #16896, #4555, #12858 ) ) ;
#14648=AXIS2_PLACEMENT_3D ( 'NONE', #3859, #10336, #1440 ) ;
#14649=EDGE_CURVE ( 'NONE', #6079, #12885, #18746, .T. ) ;
#14653=ADVANCED_FACE ( 'NONE', ( #14663 ), #16049, .T. ) ;
#14654=EDGE_CURVE ( 'NONE', #7362, #6859, #9601, .T. ) ;
#14656=ORIENTED_EDGE ( 'NONE', *, *, #12846, .F. ) ;
#14662=DIRECTION ( 'NONE',  ( 0.000000000000000000, 0.000000000000000000, 1.000000000000000000 ) ) ;
#14663=FACE_OUTER_BOUND ( 'NONE', #3937, .T. ) ;
#14664=AXIS2_PLACEMENT_3D ( 'NONE', #9386, #15847, #20706 ) ;
#14665=ORIENTED_EDGE ( 'NONE', *, *, #16366, .F. ) ;
#14672=ORIENTED_EDGE ( 'NONE', *, *, #11286, .T. ) ;
#14673=DIRECTION ( 'NONE',  ( -1.000000000000000000, 0.000000000000000000, 0.000000000000000000 ) ) ;
#14675=CIRCLE ( 'NONE', #10948, 72.00000000007199219 ) ;
#14676=EDGE_LOOP ( 'NONE', ( #14139, #6795, #9924, #17551 ) ) ;
#14678=DIRECTION ( 'NONE',  ( 0.000000000000000000, -6.982962677686266711E-15, 1.000000000000000000 ) ) ;
#14680=AXIS2_PLACEMENT_3D ( 'NONE', #8784, #18558, #18337 ) ;
#14681=EDGE_CURVE ( 'NONE', #15235, #5163, #8191, .T. ) ;
#14685=ORIENTED_EDGE ( 'NONE', *, *, #16466, .F. ) ;
#14689=VERTEX_POINT ( 'NONE', #870 ) ;
#14699=ORIENTED_EDGE ( 'NONE', *, *, #5420, .T. ) ;
#14704=VECTOR ( 'NONE', #7770, 1000.000000000000000 ) ;
#14706=CARTESIAN_POINT ( 'NONE',  ( 19.99999999999999645, 1.971042061629218356, -64.80882494896104618 ) ) ;
#14709=VECTOR ( 'NONE', #137, 1000.000000000000000 ) ;
#14711=ORIENTED_EDGE ( 'NONE', *, *, #12340, .F. ) ;
#14716=EDGE_CURVE ( 'NONE', #17222, #3247, #13585, .T. ) ;
#14719=CARTESIAN_POINT ( 'NONE',  ( 19.99999999999999645, -15.58726123847806200, -62.93731870009420959 ) ) ;
#14721=DIRECTION ( 'NONE',  ( 0.000000000000000000, 0.000000000000000000, 1.000000000000000000 ) ) ;
#14722=VERTEX_POINT ( 'NONE', #11883 ) ;
#14725=MECHANICAL_DESIGN_GEOMETRIC_PRESENTATION_REPRESENTATION('',(#162),#8640);
#14727=CARTESIAN_POINT ( 'NONE',  ( 0.000000000000000000, 56.63599015375715595, -31.56633360682406675 ) ) ;
#14730=CARTESIAN_POINT ( 'NONE',  ( 19.99999999999999645, 0.000000000000000000, 0.000000000000000000 ) ) ;
#14738=EDGE_CURVE ( 'NONE', #19110, #12652, #761, .T. ) ;
#14740=DIRECTION ( 'NONE',  ( 0.000000000000000000, -0.6310879443260593025, 0.7757112907044145800 ) ) ;
#14742=DIRECTION ( 'NONE',  ( 0.000000000000000000, 0.8878852184023764416, -0.4600650377311500394 ) ) ;
#14745=ORIENTED_EDGE ( 'NONE', *, *, #13859, .F. ) ;
#14750=AXIS2_PLACEMENT_3D ( 'NONE', #12541, #20903, #4478 ) ;
#14752=ORIENTED_EDGE ( 'NONE', *, *, #10122, .T. ) ;
#14753=CYLINDRICAL_SURFACE ( 'NONE', #18839, 72.00000000007199219 ) ;
#14754=AXIS2_PLACEMENT_3D ( 'NONE', #14440, #13049, #14740 ) ;
#14756=CARTESIAN_POINT ( 'NONE',  ( 19.99999999999999645, -49.77519642623978058, -42.18840861821836796 ) ) ;
#14759=DIRECTION ( 'NONE',  ( 0.000000000000000000, 0.000000000000000000, 1.000000000000000000 ) ) ;
#14760=DIRECTION ( 'NONE',  ( 0.000000000000000000, 0.9976687691905394839, -0.06824241336466768670 ) ) ;
#14761=DIRECTION ( 'NONE',  ( 0.000000000000000000, 0.000000000000000000, 1.000000000000000000 ) ) ;
#14763=CARTESIAN_POINT ( 'NONE',  ( 19.99999999999999645, 64.36139404985964063, 32.27399814043896953 ) ) ;
#14764=AXIS2_PLACEMENT_3D ( 'NONE', #11914, #10544, #3855 ) ;
#14765=AXIS2_PLACEMENT_3D ( 'NONE', #17882, #165, #17975 ) ;
#14771=ORIENTED_EDGE ( 'NONE', *, *, #109, .F. ) ;
#14774=EDGE_LOOP ( 'NONE', ( #19840, #19770, #19487, #160 ) ) ;
#14777=AXIS2_PLACEMENT_3D ( 'NONE', #3705, #8692, #643 ) ;
#14779=CIRCLE ( 'NONE', #19184, 27.60000000002760245 ) ;
#14780=EDGE_CURVE ( 'NONE', #12132, #3634, #11296, .T. ) ;
#14782=AXIS2_PLACEMENT_3D ( 'NONE', #20205, #16604, #12055 ) ;
#14783=VECTOR ( 'NONE', #10334, 1000.000000000000000 ) ;
#14786=ORIENTED_EDGE ( 'NONE', *, *, #20119, .F. ) ;
#14787=DIRECTION ( 'NONE',  ( 0.000000000000000000, 0.8169698930104430934, -0.5766803221148655290 ) ) ;
#14791=DIRECTION ( 'NONE',  ( 0.000000000000000000, 0.000000000000000000, 1.000000000000000000 ) ) ;
#14792=EDGE_CURVE ( 'NONE', #4671, #20034, #812, .T. ) ;
#14793=EDGE_LOOP ( 'NONE', ( #3904, #10102, #20401, #8748 ) ) ;
#14799=AXIS2_PLACEMENT_3D ( 'NONE', #4321, #17146, #15759 ) ;
#14801=AXIS2_PLACEMENT_3D ( 'NONE', #2655, #16182, #17172 ) ;
#14804=ORIENTED_EDGE ( 'NONE', *, *, #3891, .T. ) ;
#14809=ORIENTED_EDGE ( 'NONE', *, *, #13131, .T. ) ;
#14811=VECTOR ( 'NONE', #6405, 1000.000000000000000 ) ;
#14812=CARTESIAN_POINT ( 'NONE',  ( 19.99999999999999645, 64.52323195238628273, 6.389157729493382121 ) ) ;
#14818=EDGE_CURVE ( 'NONE', #5904, #19715, #18076, .T. ) ;
#14819=EDGE_CURVE ( 'NONE', #11622, #17731, #16700, .T. ) ;
#14830=FACE_OUTER_BOUND ( 'NONE', #17787, .T. ) ;
#14831=EDGE_LOOP ( 'NONE', ( #12540, #3402, #337, #7055 ) ) ;
#14832=CARTESIAN_POINT ( 'NONE',  ( 19.99999999999999645, 0.000000000000000000, 0.000000000000000000 ) ) ;
#14835=ORIENTED_EDGE ( 'NONE', *, *, #11424, .F. ) ;
#14836=CARTESIAN_POINT ( 'NONE',  ( 19.99999999999999645, 6.872116855664026858, -64.47358224882410127 ) ) ;
#14837=CARTESIAN_POINT ( 'NONE',  ( 19.99999999999999645, -64.52323195238632536, 6.389157729492951354 ) ) ;
#14850=FACE_OUTER_BOUND ( 'NONE', #3551, .T. ) ;
#14860=CARTESIAN_POINT ( 'NONE',  ( 0.000000000000000000, 28.84646472442533494, -58.52617768068405013 ) ) ;
#14865=CARTESIAN_POINT ( 'NONE',  ( 19.99999999999999645, 0.000000000000000000, 0.000000000000000000 ) ) ;
#14868=VERTEX_POINT ( 'NONE', #13604 ) ;
#14869=CARTESIAN_POINT ( 'NONE',  ( 0.000000000000000000, 0.000000000000000000, 0.000000000000000000 ) ) ;
#14870=ORIENTED_EDGE ( 'NONE', *, *, #4356, .F. ) ;
#14872=CARTESIAN_POINT ( 'NONE',  ( 0.000000000000000000, 36.59093685910711002, -62.00889726307995176 ) ) ;
#14873=ORIENTED_EDGE ( 'NONE', *, *, #19370, .T. ) ;
#14874=FACE_OUTER_BOUND ( 'NONE', #8428, .T. ) ;
#14875=ORIENTED_EDGE ( 'NONE', *, *, #10070, .T. ) ;
#14880=CYLINDRICAL_SURFACE ( 'NONE', #4661, 27.60000000002760245 ) ;
#14881=DIRECTION ( 'NONE',  ( 0.000000000000000000, 0.000000000000000000, 1.000000000000000000 ) ) ;
#14883=DIRECTION ( 'NONE',  ( 0.000000000000000000, 0.000000000000000000, 1.000000000000000000 ) ) ;
#14885=EDGE_CURVE ( 'NONE', #15935, #14689, #4164, .T. ) ;
#14890=ORIENTED_EDGE ( 'NONE', *, *, #6716, .T. ) ;
#14891=CYLINDRICAL_SURFACE ( 'NONE', #17605, 27.60000000002759535 ) ;
#14892=ORIENTED_EDGE ( 'NONE', *, *, #1714, .T. ) ;
#14894=DIRECTION ( 'NONE',  ( -1.000000000000000000, -0.000000000000000000, -0.000000000000000000 ) ) ;
#14897=EDGE_LOOP ( 'NONE', ( #20295, #20529, #13975, #2865 ) ) ;
#14898=CARTESIAN_POINT ( 'NONE',  ( 9.999999999999998224, 46.17500197033058384, 55.24372537266413730 ) ) ;
#14901=DIRECTION ( 'NONE',  ( -1.000000000000000000, 0.000000000000000000, 0.000000000000000000 ) ) ;
#14904=DIRECTION ( 'NONE',  ( 0.000000000000000000, 0.000000000000000000, 1.000000000000000000 ) ) ;
#14906=CARTESIAN_POINT ( 'NONE',  ( -10.00000000000000000, 0.000000000000000000, 0.000000000000000000 ) ) ;
#14911=EDGE_CURVE ( 'NONE', #17275, #16351, #10296, .T. ) ;
#14912=CIRCLE ( 'NONE', #19296, 65.24900000006526568 ) ;
#14913=DIRECTION ( 'NONE',  ( 0.000000000000000000, 0.000000000000000000, -1.000000000000000000 ) ) ;
#14915=CARTESIAN_POINT ( 'NONE',  ( 0.000000000000000000, 0.000000000000000000, 0.000000000000000000 ) ) ;
#14919=EDGE_CURVE ( 'NONE', #3519, #10526, #2172, .T. ) ;
#14924=LINE ( 'NONE', #10255, #1944 ) ;
#14929=ORIENTED_EDGE ( 'NONE', *, *, #1490, .F. ) ;
#14936=CIRCLE ( 'NONE', #13928, 27.60000000002759535 ) ;
#14940=ADVANCED_FACE ( 'NONE', ( #13827 ), #7124, .T. ) ;
#14944=DIRECTION ( 'NONE',  ( -1.000000000000000000, -0.000000000000000000, 0.000000000000000000 ) ) ;
#14948=ORIENTED_EDGE ( 'NONE', *, *, #986, .T. ) ;
#14949=DIRECTION ( 'NONE',  ( -1.000000000000000000, 0.000000000000000000, 0.000000000000000000 ) ) ;
#14951=FACE_OUTER_BOUND ( 'NONE', #20627, .T. ) ;
#14952=AXIS2_PLACEMENT_3D ( 'NONE', #14832, #8250, #3470 ) ;
#14953=EDGE_LOOP ( 'NONE', ( #12149, #17298, #16173, #3084 ) ) ;
#14956=DIRECTION ( 'NONE',  ( 1.000000000000000000, -0.000000000000000000, -0.000000000000000000 ) ) ;
#14960=EDGE_LOOP ( 'NONE', ( #5819, #8148, #6353, #11603 ) ) ;
#14966=CARTESIAN_POINT ( 'NONE',  ( 0.000000000000000000, 55.05624179292029652, -35.01774179823726740 ) ) ;
#14967=VECTOR ( 'NONE', #12929, 1000.000000000000000 ) ;
#14977=DIRECTION ( 'NONE',  ( -1.000000000000000000, -0.000000000000000000, 0.000000000000000000 ) ) ;
#14980=CIRCLE ( 'NONE', #17344, 27.60000000002761311 ) ;
#14985=ORIENTED_EDGE ( 'NONE', *, *, #8593, .F. ) ;
#14986=AXIS2_PLACEMENT_3D ( 'NONE', #12148, #18408, #387 ) ;
#14990=CYLINDRICAL_SURFACE ( 'NONE', #4508, 72.00000000007199219 ) ;
#14993=CIRCLE ( 'NONE', #3792, 65.24900000006526568 ) ;
#14995=FACE_OUTER_BOUND ( 'NONE', #712, .T. ) ;
#14997=CARTESIAN_POINT ( 'NONE',  ( 19.99999999999999645, 0.000000000000000000, 0.000000000000000000 ) ) ;
#14998=VERTEX_POINT ( 'NONE', #18804 ) ;
#15002=FACE_OUTER_BOUND ( 'NONE', #4683, .T. ) ;
#15009=EDGE_CURVE ( 'NONE', #10935, #7472, #17755, .T. ) ;
#15010=DIRECTION ( 'NONE',  ( -1.000000000000000000, 0.000000000000000000, 0.000000000000000000 ) ) ;
#15011=CIRCLE ( 'NONE', #8906, 72.00000000007199219 ) ;
#15012=EDGE_LOOP ( 'NONE', ( #1297, #5776, #8075, #16692 ) ) ;
#15013=DIRECTION ( 'NONE',  ( 1.000000000000000000, 0.000000000000000000, -0.000000000000000000 ) ) ;
#15014=DIRECTION ( 'NONE',  ( -1.000000000000000000, -0.000000000000000000, -0.000000000000000000 ) ) ;
#15016=AXIS2_PLACEMENT_3D ( 'NONE', #5105, #1542, #16250 ) ;
#15020=EDGE_LOOP ( 'NONE', ( #5266, #10811, #13878, #17285 ) ) ;
#15021=DIRECTION ( 'NONE',  ( -1.000000000000000000, 0.000000000000000000, 0.000000000000000000 ) ) ;
#15022=CIRCLE ( 'NONE', #4523, 27.60000000002759535 ) ;
#15026=LINE ( 'NONE', #16713, #19009 ) ;
#15032=ADVANCED_FACE ( 'NONE', ( #4698 ), #19121, .T. ) ;
#15034=ORIENTED_EDGE ( 'NONE', *, *, #4725, .F. ) ;
#15035=CARTESIAN_POINT ( 'NONE',  ( 0.000000000000000000, 0.000000000000000000, 0.000000000000000000 ) ) ;
#15040=DIRECTION ( 'NONE',  ( -1.000000000000000000, 0.000000000000000000, 0.000000000000000000 ) ) ;
#15041=VECTOR ( 'NONE', #19109, 1000.000000000000000 ) ;
#15053=VERTEX_POINT ( 'NONE', #1420 ) ;
#15060=ORIENTED_EDGE ( 'NONE', *, *, #5355, .F. ) ;
#15062=CARTESIAN_POINT ( 'NONE',  ( 0.000000000000000000, -64.36139404985986801, 32.27399814043853610 ) ) ;
#15063=EDGE_CURVE ( 'NONE', #10906, #7485, #485, .T. ) ;
#15065=ORIENTED_EDGE ( 'NONE', *, *, #18611, .T. ) ;
#15069=DIRECTION ( 'NONE',  ( 0.000000000000000000, 0.000000000000000000, 1.000000000000000000 ) ) ;
#15070=AXIS2_PLACEMENT_3D ( 'NONE', #19341, #6094, #9705 ) ;
#15074=CARTESIAN_POINT ( 'NONE',  ( 0.000000000000000000, -63.17103598352115057, -16.33561182745204476 ) ) ;
#15077=ORIENTED_EDGE ( 'NONE', *, *, #17774, .T. ) ;
#15078=DIRECTION ( 'NONE',  ( 0.000000000000000000, 0.000000000000000000, 1.000000000000000000 ) ) ;
#15082=ORIENTED_EDGE ( 'NONE', *, *, #3767, .F. ) ;
#15090=DIRECTION ( 'NONE',  ( -1.000000000000000000, 0.000000000000000000, 0.000000000000000000 ) ) ;
#15099=VECTOR ( 'NONE', #4363, 1000.000000000000000 ) ;
#15102=DIRECTION ( 'NONE',  ( -1.000000000000000000, 0.000000000000000000, -0.000000000000000000 ) ) ;
#15105=AXIS2_PLACEMENT_3D ( 'NONE', #5527, #15400, #12330 ) ;
#15109=AXIS2_PLACEMENT_3D ( 'NONE', #16646, #16956, #18565 ) ;
#15113=AXIS2_PLACEMENT_3D ( 'NONE', #14590, #18187, #13312 ) ;
#15115=CARTESIAN_POINT ( 'NONE',  ( 19.99999999999999645, 19.38316218894295417, -61.87375713200968619 ) ) ;
#15117=EDGE_CURVE ( 'NONE', #2692, #3661, #2792, .T. ) ;
#15123=AXIS2_PLACEMENT_3D ( 'NONE', #8062, #3286, #14625 ) ;
#15128=DIRECTION ( 'NONE',  ( 0.000000000000000000, -0.1361666490962330778, -0.9906859460363326431 ) ) ;
#15130=CARTESIAN_POINT ( 'NONE',  ( 0.000000000000000000, 0.000000000000000000, 0.000000000000000000 ) ) ;
#15131=CARTESIAN_POINT ( 'NONE',  ( 0.000000000000000000, -64.79224928664389438, -2.456263514198281150 ) ) ;
#15132=AXIS2_PLACEMENT_3D ( 'NONE', #18235, #2329, #2430 ) ;
#15138=ORIENTED_EDGE ( 'NONE', *, *, #19552, .T. ) ;
#15139=ORIENTED_EDGE ( 'NONE', *, *, #6078, .T. ) ;
#15142=AXIS2_PLACEMENT_3D ( 'NONE', #16530, #19810, #11763 ) ;
#15143=CARTESIAN_POINT ( 'NONE',  ( 19.99999999999999645, 0.000000000000000000, 0.000000000000000000 ) ) ;
#15148=AXIS2_PLACEMENT_3D ( 'NONE', #2633, #826, #15650 ) ;
#15154=CARTESIAN_POINT ( 'NONE',  ( 9.999999999999998224, -10.74906464462068456, -71.19310085447979475 ) ) ;
#15157=CYLINDRICAL_SURFACE ( 'NONE', #10223, 65.24900000006525147 ) ;
#15159=DIRECTION ( 'NONE',  ( 0.000000000000000000, 0.000000000000000000, 1.000000000000000000 ) ) ;
#15161=EDGE_CURVE ( 'NONE', #4150, #2016, #17425, .T. ) ;
#15167=ORIENTED_EDGE ( 'NONE', *, *, #14275, .F. ) ;
#15171=CARTESIAN_POINT ( 'NONE',  ( 19.99999999999999645, 70.68211945903189530, 13.71269443944231980 ) ) ;
#15176=CARTESIAN_POINT ( 'NONE',  ( 19.99999999999999645, -45.48683723007244595, 46.78012013466202035 ) ) ;
#15178=DIRECTION ( 'NONE',  ( -1.000000000000000000, 0.000000000000000000, 0.000000000000000000 ) ) ;
#15179=ORIENTED_EDGE ( 'NONE', *, *, #7961, .T. ) ;
#15182=ADVANCED_FACE ( 'NONE', ( #8090 ), #9872, .T. ) ;
#15185=VERTEX_POINT ( 'NONE', #6693 ) ;
#15190=ORIENTED_EDGE ( 'NONE', *, *, #11530, .F. ) ;
#15191=EDGE_CURVE ( 'NONE', #10498, #17301, #1845, .T. ) ;
#15194=DIRECTION ( 'NONE',  ( -1.000000000000000000, 0.000000000000000000, 0.000000000000000000 ) ) ;
#15196=CARTESIAN_POINT ( 'NONE',  ( 19.99999999999999645, 24.01204443665271882, -60.22865198596099390 ) ) ;
#15199=DIRECTION ( 'NONE',  ( 0.000000000000000000, 0.000000000000000000, 1.000000000000000000 ) ) ;
#15200=EDGE_CURVE ( 'NONE', #14722, #9681, #13688, .T. ) ;
#15202=EDGE_LOOP ( 'NONE', ( #4095, #8614, #11266, #6204 ) ) ;
#15208=ORIENTED_EDGE ( 'NONE', *, *, #648, .T. ) ;
#15209=DIRECTION ( 'NONE',  ( -1.000000000000000000, 0.000000000000000000, 0.000000000000000000 ) ) ;
#15210=VERTEX_POINT ( 'NONE', #19619 ) ;
#15220=CARTESIAN_POINT ( 'NONE',  ( 0.000000000000000000, 27.62776854598856602, 58.65812137499012380 ) ) ;
#15222=VECTOR ( 'NONE', #3037, 1000.000000000000000 ) ;
#15224=CYLINDRICAL_SURFACE ( 'NONE', #7477, 72.00000000007199219 ) ;
#15235=VERTEX_POINT ( 'NONE', #4902 ) ;
#15239=CYLINDRICAL_SURFACE ( 'NONE', #6981, 72.00000000007199219 ) ;
#15240=CARTESIAN_POINT ( 'NONE',  ( 19.99999999999999645, -31.17893654894190902, -57.31758819669202865 ) ) ;
#15246=LINE ( 'NONE', #729, #2643 ) ;
#15248=LINE ( 'NONE', #10709, #17519 ) ;
#15251=ADVANCED_FACE ( 'NONE', ( #18040 ), #11372, .T. ) ;
#15252=CARTESIAN_POINT ( 'NONE',  ( 0.000000000000000000, 23.08379033237438094, -61.02926039941409897 ) ) ;
#15258=ORIENTED_EDGE ( 'NONE', *, *, #10209, .T. ) ;
#15259=DIRECTION ( 'NONE',  ( -1.000000000000000000, 0.000000000000000000, -0.000000000000000000 ) ) ;
#15260=CARTESIAN_POINT ( 'NONE',  ( 19.99999999999999645, 0.000000000000000000, 0.000000000000000000 ) ) ;
#15262=AXIS2_PLACEMENT_3D ( 'NONE', #5500, #12186, #15374 ) ;
#15264=DIRECTION ( 'NONE',  ( 1.000000000000000000, 0.000000000000000000, 0.000000000000000000 ) ) ;
#15266=FILL_AREA_STYLE ('',( #4357 ) ) ;
#15267=LINE ( 'NONE', #2442, #4853 ) ;
#15270=DIRECTION ( 'NONE',  ( -1.000000000000000000, -0.000000000000000000, -0.000000000000000000 ) ) ;
#15271=DIRECTION ( 'NONE',  ( 0.000000000000000000, 0.000000000000000000, -1.000000000000000000 ) ) ;
#15274=ORIENTED_EDGE ( 'NONE', *, *, #10528, .F. ) ;
#15276=ORIENTED_EDGE ( 'NONE', *, *, #12963, .T. ) ;
#15279=CIRCLE ( 'NONE', #2075, 27.60000000002760245 ) ;
#15281=CYLINDRICAL_SURFACE ( 'NONE', #4170, 27.60000000002760245 ) ;
#15283=CYLINDRICAL_SURFACE ( 'NONE', #4435, 27.60000000002760245 ) ;
#15286=DIRECTION ( 'NONE',  ( -1.000000000000000000, 0.000000000000000000, 0.000000000000000000 ) ) ;
#15287=AXIS2_PLACEMENT_3D ( 'NONE', #9588, #2811, #6403 ) ;
#15290=ADVANCED_FACE ( 'NONE', ( #235 ), #1727, .T. ) ;
#15296=EDGE_CURVE ( 'NONE', #8436, #18021, #9975, .T. ) ;
#15299=ORIENTED_EDGE ( 'NONE', *, *, #6830, .T. ) ;
#15300=DIRECTION ( 'NONE',  ( -1.000000000000000000, -0.000000000000000000, -0.000000000000000000 ) ) ;
#15301=DIRECTION ( 'NONE',  ( -1.000000000000000000, 0.000000000000000000, 0.000000000000000000 ) ) ;
#15305=CIRCLE ( 'NONE', #9891, 72.00000000007199219 ) ;
#15308=AXIS2_PLACEMENT_3D ( 'NONE', #1600, #17910, #13031 ) ;
#15310=DIRECTION ( 'NONE',  ( 0.000000000000000000, 0.000000000000000000, 1.000000000000000000 ) ) ;
#15312=EDGE_CURVE ( 'NONE', #2829, #18621, #1928, .T. ) ;
#15313=CARTESIAN_POINT ( 'NONE',  ( 19.99999999999999645, 53.26727847779603309, -48.44168704307575979 ) ) ;
#15314=VERTEX_POINT ( 'NONE', #14860 ) ;
#15316=CIRCLE ( 'NONE', #9569, 27.60000000002759535 ) ;
#15318=ORIENTED_EDGE ( 'NONE', *, *, #18694, .T. ) ;
#15319=FACE_OUTER_BOUND ( 'NONE', #14953, .T. ) ;
#15321=EDGE_CURVE ( 'NONE', #10201, #8657, #496, .T. ) ;
#15323=EDGE_CURVE ( 'NONE', #8227, #18180, #10656, .T. ) ;
#15324=AXIS2_PLACEMENT_3D ( 'NONE', #1, #12941, #9757 ) ;
#15328=ORIENTED_EDGE ( 'NONE', *, *, #5239, .T. ) ;
#15329=CARTESIAN_POINT ( 'NONE',  ( 19.99999999999999645, 60.40676135667438729, 23.56039007469059143 ) ) ;
#15333=CARTESIAN_POINT ( 'NONE',  ( 0.000000000000000000, -15.58726123847806200, -62.93731870009420959 ) ) ;
#15334=AXIS2_PLACEMENT_3D ( 'NONE', #12685, #20615, #14065 ) ;
#15335=CIRCLE ( 'NONE', #1807, 27.60000000002759890 ) ;
#15341=DIRECTION ( 'NONE',  ( 0.000000000000000000, 0.000000000000000000, 1.000000000000000000 ) ) ;
#15342=ORIENTED_EDGE ( 'NONE', *, *, #6225, .T. ) ;
#15343=CYLINDRICAL_SURFACE ( 'NONE', #5118, 27.60000000002759890 ) ;
#15348=CARTESIAN_POINT ( 'NONE',  ( 19.99999999999999645, -60.40676135667455071, 23.56039007469017221 ) ) ;
#15349=VECTOR ( 'NONE', #18119, 1000.000000000000000 ) ;
#15351=DIRECTION ( 'NONE',  ( 0.000000000000000000, 0.3984010898462361783, 0.9172113015054552676 ) ) ;
#15354=AXIS2_PLACEMENT_3D ( 'NONE', #19313, #11472, #19526 ) ;
#15357=ADVANCED_FACE ( 'NONE', ( #7000 ), #5618, .T. ) ;
#15358=CARTESIAN_POINT ( 'NONE',  ( 19.99999999999999645, -64.36139404985942747, -32.27399814043940296 ) ) ;
#15363=DIRECTION ( 'NONE',  ( -1.000000000000000000, 0.000000000000000000, 0.000000000000000000 ) ) ;
#15369=VECTOR ( 'NONE', #12194, 1000.000000000000000 ) ;
#15370=ORIENTED_EDGE ( 'NONE', *, *, #7638, .T. ) ;
#15371=DIRECTION ( 'NONE',  ( 0.000000000000000000, 0.000000000000000000, 1.000000000000000000 ) ) ;
#15372=ORIENTED_EDGE ( 'NONE', *, *, #1243, .F. ) ;
#15373=AXIS2_PLACEMENT_3D ( 'NONE', #4916, #6399, #9691 ) ;
#15374=DIRECTION ( 'NONE',  ( 0.000000000000000000, -0.5195839500354404450, 0.8544194045464843512 ) ) ;
#15381=CARTESIAN_POINT ( 'NONE',  ( 19.99999999999999645, 60.35829202194874910, 24.78524934717571426 ) ) ;
#15384=DIRECTION ( 'NONE',  ( 0.000000000000000000, 0.000000000000000000, 1.000000000000000000 ) ) ;
#15387=CARTESIAN_POINT ( 'NONE',  ( 19.99999999999999645, 0.000000000000000000, 0.000000000000000000 ) ) ;
#15395=CARTESIAN_POINT ( 'NONE',  ( 19.99999999999999645, 0.000000000000000000, 0.000000000000000000 ) ) ;
#15396=ORIENTED_EDGE ( 'NONE', *, *, #673, .T. ) ;
#15397=VECTOR ( 'NONE', #8161, 1000.000000000000000 ) ;
#15400=DIRECTION ( 'NONE',  ( -1.000000000000000000, 0.000000000000000000, 0.000000000000000000 ) ) ;
#15401=ORIENTED_EDGE ( 'NONE', *, *, #2090, .T. ) ;
#15403=AXIS2_PLACEMENT_3D ( 'NONE', #6310, #10590, #8997 ) ;
#15404=FACE_OUTER_BOUND ( 'NONE', #5142, .T. ) ;
#15416=EDGE_CURVE ( 'NONE', #7037, #3825, #18661, .T. ) ;
#15421=CARTESIAN_POINT ( 'NONE',  ( 19.99999999999999645, 5.762283366692075859, -64.99406197038663890 ) ) ;
#15424=ADVANCED_FACE ( 'NONE', ( #12100 ), #647, .T. ) ;
#15425=ORIENTED_EDGE ( 'NONE', *, *, #11479, .F. ) ;
#15426=CIRCLE ( 'NONE', #3245, 65.24900000006526568 ) ;
#15432=ADVANCED_FACE ( 'NONE', ( #11988 ), #3812, .T. ) ;
#15434=LINE ( 'NONE', #7704, #9624 ) ;
#15435=ORIENTED_EDGE ( 'NONE', *, *, #12765, .F. ) ;
#15436=DIRECTION ( 'NONE',  ( -1.000000000000000000, 0.000000000000000000, 0.000000000000000000 ) ) ;
#15439=EDGE_CURVE ( 'NONE', #11338, #12564, #16867, .T. ) ;
#15443=ORIENTED_EDGE ( 'NONE', *, *, #5097, .T. ) ;
#15444=AXIS2_PLACEMENT_3D ( 'NONE', #5839, #17611, #9342 ) ;
#15445=EDGE_CURVE ( 'NONE', #19491, #1793, #2139, .T. ) ;
#15446=DIRECTION ( 'NONE',  ( -1.000000000000000000, 0.000000000000000000, -0.000000000000000000 ) ) ;
#15450=VERTEX_POINT ( 'NONE', #16648 ) ;
#15451=CARTESIAN_POINT ( 'NONE',  ( 0.000000000000000000, 59.31169354540775629, -27.19476070466793871 ) ) ;
#15453=CIRCLE ( 'NONE', #16144, 65.24900000006526568 ) ;
#15457=AXIS2_PLACEMENT_3D ( 'NONE', #20158, #14145, #10844 ) ;
#15461=CARTESIAN_POINT ( 'NONE',  ( 0.000000000000000000, 0.000000000000000000, 0.000000000000000000 ) ) ;
#15465=EDGE_CURVE ( 'NONE', #1870, #5904, #15267, .T. ) ;
#15472=AXIS2_PLACEMENT_3D ( 'NONE', #4347, #10814, #17596 ) ;
#15479=CARTESIAN_POINT ( 'NONE',  ( 0.000000000000000000, 0.000000000000000000, 0.000000000000000000 ) ) ;
#15484=ORIENTED_EDGE ( 'NONE', *, *, #16216, .T. ) ;
#15485=EDGE_LOOP ( 'NONE', ( #18238, #5320, #12834, #4978 ) ) ;
#15491=CARTESIAN_POINT ( 'NONE',  ( 19.99999999999999645, 42.42902769288536291, 49.02903636734212967 ) ) ;
#15492=DIRECTION ( 'NONE',  ( -1.000000000000000000, -0.000000000000000000, 0.000000000000000000 ) ) ;
#15493=DIRECTION ( 'NONE',  ( 0.000000000000000000, -0.9790840876823205807, -0.2034560130526446575 ) ) ;
#15494=CARTESIAN_POINT ( 'NONE',  ( 9.999999999999998224, -58.26603306961936113, -42.29739224042532442 ) ) ;
#15496=CARTESIAN_POINT ( 'NONE',  ( -10.00000000000000000, 0.000000000000000000, 0.000000000000000000 ) ) ;
#15500=VERTEX_POINT ( 'NONE', #2136 ) ;
#15502=ORIENTED_EDGE ( 'NONE', *, *, #12715, .T. ) ;
#15505=CARTESIAN_POINT ( 'NONE',  ( 19.99999999999999645, 0.000000000000000000, 0.000000000000000000 ) ) ;
#15508=DIRECTION ( 'NONE',  ( 0.000000000000000000, 0.9790840876823220240, 0.2034560130526376631 ) ) ;
#15512=CYLINDRICAL_SURFACE ( 'NONE', #6557, 65.24900000006525147 ) ;
#15513=ORIENTED_EDGE ( 'NONE', *, *, #14264, .T. ) ;
#15515=VERTEX_POINT ( 'NONE', #20134 ) ;
#15517=DIRECTION ( 'NONE',  ( -1.000000000000000000, 0.000000000000000000, 0.000000000000000000 ) ) ;
#15518=EDGE_LOOP ( 'NONE', ( #20178, #12751, #19650, #6785 ) ) ;
#15521=CARTESIAN_POINT ( 'NONE',  ( 19.99999999999999645, 60.35829202194874910, 24.78524934717571426 ) ) ;
#15524=VERTEX_POINT ( 'NONE', #13577 ) ;
#15526=ADVANCED_FACE ( 'NONE', ( #20024 ), #15900, .T. ) ;
#15527=ORIENTED_EDGE ( 'NONE', *, *, #8702, .F. ) ;
#15529=ADVANCED_FACE ( 'NONE', ( #10823 ), #14326, .T. ) ;
#15533=DIRECTION ( 'NONE',  ( -1.000000000000000000, -0.000000000000000000, -0.000000000000000000 ) ) ;
#15539=CARTESIAN_POINT ( 'NONE',  ( 19.99999999999999645, 62.46228066917787203, 18.86519267363478036 ) ) ;
#15543=ORIENTED_EDGE ( 'NONE', *, *, #11936, .F. ) ;
#15545=CARTESIAN_POINT ( 'NONE',  ( 19.99999999999999645, 0.000000000000000000, 0.000000000000000000 ) ) ;
#15547=ORIENTED_EDGE ( 'NONE', *, *, #12308, .T. ) ;
#15548=ORIENTED_EDGE ( 'NONE', *, *, #9135, .F. ) ;
#15550=EDGE_CURVE ( 'NONE', #5709, #12561, #18066, .T. ) ;
#15551=DIRECTION ( 'NONE',  ( 0.000000000000000000, 0.000000000000000000, 1.000000000000000000 ) ) ;
#15554=DIRECTION ( 'NONE',  ( -1.000000000000000000, -0.000000000000000000, -0.000000000000000000 ) ) ;
#15557=CIRCLE ( 'NONE', #6416, 65.24900000006525147 ) ;
#15559=ADVANCED_FACE ( 'NONE', ( #7746 ), #17606, .T. ) ;
#15561=ADVANCED_FACE ( 'NONE', ( #9127 ), #5828, .T. ) ;
#15562=ORIENTED_EDGE ( 'NONE', *, *, #13905, .T. ) ;
#15567=VERTEX_POINT ( 'NONE', #19194 ) ;
#15568=CYLINDRICAL_SURFACE ( 'NONE', #2788, 65.24900000006525147 ) ;
#15570=DIRECTION ( 'NONE',  ( 0.000000000000000000, 0.9976687691905394839, -0.06824241336466758956 ) ) ;
#15572=ORIENTED_EDGE ( 'NONE', *, *, #2631, .F. ) ;
#15574=DIRECTION ( 'NONE',  ( -1.000000000000000000, -0.000000000000000000, -0.000000000000000000 ) ) ;
#15576=DIRECTION ( 'NONE',  ( 0.000000000000000000, 0.9976687691905389288, 0.06824241336467461172 ) ) ;
#15577=CARTESIAN_POINT ( 'NONE',  ( 19.99999999999999645, -54.08351995568730786, 35.76369202524482915 ) ) ;
#15580=ORIENTED_EDGE ( 'NONE', *, *, #3453, .T. ) ;
#15583=AXIS2_PLACEMENT_3D ( 'NONE', #8499, #14673, #9998 ) ;
#15584=CARTESIAN_POINT ( 'NONE',  ( 19.99999999999999645, 0.000000000000000000, 0.000000000000000000 ) ) ;
#15596=CARTESIAN_POINT ( 'NONE',  ( 20.00000000000000355, 9.184850993605147944E-16, -7.500000000000000000 ) ) ;
#15597=ORIENTED_EDGE ( 'NONE', *, *, #14025, .T. ) ;
#15598=EDGE_CURVE ( 'NONE', #17111, #14031, #10726, .T. ) ;
#15599=DIRECTION ( 'NONE',  ( -0.000000000000000000, 1.000000000000000000, 0.000000000000000000 ) ) ;
#15604=ORIENTED_EDGE ( 'NONE', *, *, #15550, .T. ) ;
#15605=DIRECTION ( 'NONE',  ( -1.000000000000000000, 0.000000000000000000, 0.000000000000000000 ) ) ;
#15611=AXIS2_PLACEMENT_3D ( 'NONE', #3203, #17935, #9864 ) ;
#15613=( NAMED_UNIT ( * ) SI_UNIT ( $, .STERADIAN. ) SOLID_ANGLE_UNIT ( ) );
#15615=LINE ( 'NONE', #14153, #9822 ) ;
#15620=ORIENTED_EDGE ( 'NONE', *, *, #17713, .T. ) ;
#15624=VERTEX_POINT ( 'NONE', #7637 ) ;
#15626=DIRECTION ( 'NONE',  ( 0.000000000000000000, 0.6310879443260486443, 0.7757112907044232397 ) ) ;
#15627=VERTEX_POINT ( 'NONE', #20462 ) ;
#15628=CARTESIAN_POINT ( 'NONE',  ( -65.00002539999999840, 0.000000000000000000, -1.000000000000000000 ) ) ;
#15630=ORIENTED_EDGE ( 'NONE', *, *, #15640, .T. ) ;
#15632=AXIS2_PLACEMENT_3D ( 'NONE', #1160, #20540, #6427 ) ;
#15637=AXIS2_PLACEMENT_3D ( 'NONE', #11918, #10667, #802 ) ;
#15640=EDGE_CURVE ( 'NONE', #6966, #5326, #1142, .T. ) ;
#15642=CIRCLE ( 'NONE', #18689, 27.60000000002759890 ) ;
#15643=ORIENTED_EDGE ( 'NONE', *, *, #12482, .T. ) ;
#15649=DIRECTION ( 'NONE',  ( -1.000000000000000000, 0.000000000000000000, 0.000000000000000000 ) ) ;
#15650=DIRECTION ( 'NONE',  ( 0.000000000000000000, -6.982962677686266711E-15, 1.000000000000000000 ) ) ;
#15651=VERTEX_POINT ( 'NONE', #5941 ) ;
#15652=AXIS2_PLACEMENT_3D ( 'NONE', #12496, #11000, #18957 ) ;
#15654=CIRCLE ( 'NONE', #10924, 27.60000000002760245 ) ;
#15655=DIRECTION ( 'NONE',  ( -1.000000000000000000, 0.000000000000000000, 0.000000000000000000 ) ) ;
#15657=CIRCLE ( 'NONE', #4481, 27.60000000002759180 ) ;
#15659=ORIENTED_EDGE ( 'NONE', *, *, #18148, .F. ) ;
#15661=DIRECTION ( 'NONE',  ( -1.000000000000000000, 0.000000000000000000, 0.000000000000000000 ) ) ;
#15667=ORIENTED_EDGE ( 'NONE', *, *, #9002, .T. ) ;
#15668=AXIS2_PLACEMENT_3D ( 'NONE', #11926, #3868, #8750 ) ;
#15669=DIRECTION ( 'NONE',  ( -1.000000000000000000, -0.000000000000000000, -0.000000000000000000 ) ) ;
#15673=EDGE_CURVE ( 'NONE', #16021, #11056, #4358, .T. ) ;
#15675=DIRECTION ( 'NONE',  ( -1.000000000000000000, -0.000000000000000000, -0.000000000000000000 ) ) ;
#15677=CARTESIAN_POINT ( 'NONE',  ( 19.99999999999999645, -65.23577793412343340, -1.313498510942392450 ) ) ;
#15678=CARTESIAN_POINT ( 'NONE',  ( 9.999999999999998224, 68.15657073222466522, -23.20952102120210725 ) ) ;
#15681=AXIS2_PLACEMENT_3D ( 'NONE', #16757, #11780, #15069 ) ;
#15685=CYLINDRICAL_SURFACE ( 'NONE', #20191, 27.60000000002759890 ) ;
#15688=VERTEX_POINT ( 'NONE', #19599 ) ;
#15690=AXIS2_PLACEMENT_3D ( 'NONE', #3534, #13409, #9796 ) ;
#15691=CIRCLE ( 'NONE', #14680, 7.500000000000000000 ) ;
#15693=DIRECTION ( 'NONE',  ( 0.000000000000000000, 0.000000000000000000, -1.000000000000000000 ) ) ;
#15695=EDGE_CURVE ( 'NONE', #16351, #19634, #9939, .T. ) ;
#15699=CARTESIAN_POINT ( 'NONE',  ( 19.99999999999999645, -15.58726123847806200, -62.93731870009420959 ) ) ;
#15706=EDGE_CURVE ( 'NONE', #10182, #9751, #5531, .T. ) ;
#15710=EDGE_LOOP ( 'NONE', ( #5474, #15892, #5193, #12881 ) ) ;
#15711=CARTESIAN_POINT ( 'NONE',  ( 0.000000000000000000, 0.000000000000000000, 0.000000000000000000 ) ) ;
#15712=ORIENTED_EDGE ( 'NONE', *, *, #3400, .F. ) ;
#15713=DIRECTION ( 'NONE',  ( 0.000000000000000000, -0.1361666490962330778, -0.9906859460363326431 ) ) ;
#15714=DIRECTION ( 'NONE',  ( 0.000000000000000000, 0.9790840876823234673, -0.2034560130526309185 ) ) ;
#15722=AXIS2_PLACEMENT_3D ( 'NONE', #17855, #9685, #3323 ) ;
#15724=CIRCLE ( 'NONE', #20107, 27.60000000002759890 ) ;
#15726=VERTEX_POINT ( 'NONE', #8259 ) ;
#15728=DIRECTION ( 'NONE',  ( 0.000000000000000000, 0.000000000000000000, -1.000000000000000000 ) ) ;
#15729=CARTESIAN_POINT ( 'NONE',  ( 0.000000000000000000, -28.84646472442415543, -58.52617768068463278 ) ) ;
#15730=ORIENTED_EDGE ( 'NONE', *, *, #10127, .T. ) ;
#15739=DIRECTION ( 'NONE',  ( 0.000000000000000000, 0.000000000000000000, 1.000000000000000000 ) ) ;
#15742=DIRECTION ( 'NONE',  ( 0.000000000000000000, 0.000000000000000000, 1.000000000000000000 ) ) ;
#15746=DIRECTION ( 'NONE',  ( 0.000000000000000000, 0.000000000000000000, 1.000000000000000000 ) ) ;
#15750=AXIS2_PLACEMENT_3D ( 'NONE', #18809, #16788, #5435 ) ;
#15751=CARTESIAN_POINT ( 'NONE',  ( 0.000000000000000000, 27.62776854598936538, -58.65812137498974721 ) ) ;
#15756=LINE ( 'NONE', #12580, #12414 ) ;
#15757=ORIENTED_EDGE ( 'NONE', *, *, #9769, .T. ) ;
#15759=DIRECTION ( 'NONE',  ( 0.000000000000000000, 0.000000000000000000, 1.000000000000000000 ) ) ;
#15760=DIRECTION ( 'NONE',  ( 0.000000000000000000, 0.000000000000000000, 1.000000000000000000 ) ) ;
#15763=EDGE_CURVE ( 'NONE', #3682, #8629, #12940, .T. ) ;
#15767=EDGE_CURVE ( 'NONE', #4451, #19589, #2839, .T. ) ;
#15769=CARTESIAN_POINT ( 'NONE',  ( 19.99999999999999645, -62.46228066917801414, 18.86519267363435048 ) ) ;
#15772=DIRECTION ( 'NONE',  ( 0.000000000000000000, -0.9422609221188167350, -0.3348796121709969875 ) ) ;
#15777=DIRECTION ( 'NONE',  ( -1.000000000000000000, -0.000000000000000000, 0.000000000000000000 ) ) ;
#15778=AXIS2_PLACEMENT_3D ( 'NONE', #593, #17441, #10965 ) ;
#15779=AXIS2_PLACEMENT_3D ( 'NONE', #7378, #2220, #6980 ) ;
#15782=CARTESIAN_POINT ( 'NONE',  ( 19.99999999999999645, 31.98952867950324830, 56.39803944231596944 ) ) ;
#15786=ORIENTED_EDGE ( 'NONE', *, *, #11479, .T. ) ;
#15787=DIRECTION ( 'NONE',  ( 0.000000000000000000, 0.000000000000000000, 1.000000000000000000 ) ) ;
#15789=VERTEX_POINT ( 'NONE', #9846 ) ;
#15790=DIRECTION ( 'NONE',  ( 0.000000000000000000, 0.7308359642781208088, 0.6825531432186576763 ) ) ;
#15792=ORIENTED_EDGE ( 'NONE', *, *, #2227, .F. ) ;
#15800=FACE_OUTER_BOUND ( 'NONE', #18218, .T. ) ;
#15803=CIRCLE ( 'NONE', #19199, 27.60000000002759890 ) ;
#15805=CYLINDRICAL_SURFACE ( 'NONE', #10115, 65.24900000006525147 ) ;
#15809=ORIENTED_EDGE ( 'NONE', *, *, #20864, .F. ) ;
#15812=ORIENTED_EDGE ( 'NONE', *, *, #19971, .F. ) ;
#15815=ORIENTED_EDGE ( 'NONE', *, *, #7338, .F. ) ;
#15821=VECTOR ( 'NONE', #3063, 1000.000000000000000 ) ;
#15824=AXIS2_PLACEMENT_3D ( 'NONE', #16262, #17764, #4719 ) ;
#15832=DIRECTION ( 'NONE',  ( -1.000000000000000000, -0.000000000000000000, 0.000000000000000000 ) ) ;
#15834=LINE ( 'NONE', #7987, #6601 ) ;
#15835=EDGE_CURVE ( 'NONE', #17178, #17883, #14372, .T. ) ;
#15836=DIRECTION ( 'NONE',  ( -1.000000000000000000, -0.000000000000000000, -0.000000000000000000 ) ) ;
#15838=AXIS2_PLACEMENT_3D ( 'NONE', #15505, #20154, #16777 ) ;
#15839=DIRECTION ( 'NONE',  ( 0.000000000000000000, 0.9790840876823220240, 0.2034560130526376631 ) ) ;
#15840=CARTESIAN_POINT ( 'NONE',  ( 19.99999999999999645, -45.48683723007179225, -46.78012013466265273 ) ) ;
#15844=DIRECTION ( 'NONE',  ( 0.000000000000000000, 0.000000000000000000, 1.000000000000000000 ) ) ;
#15846=ORIENTED_EDGE ( 'NONE', *, *, #2503, .T. ) ;
#15847=DIRECTION ( 'NONE',  ( -1.000000000000000000, 0.000000000000000000, 0.000000000000000000 ) ) ;
#15848=ORIENTED_EDGE ( 'NONE', *, *, #8210, .T. ) ;
#15849=CARTESIAN_POINT ( 'NONE',  ( 19.99999999999999645, 24.01204443665187327, 60.22865198596132785 ) ) ;
#15851=EDGE_LOOP ( 'NONE', ( #8252, #9750, #6581, #18927 ) ) ;
#15852=EDGE_CURVE ( 'NONE', #297, #3604, #11635, .T. ) ;
#15855=DIRECTION ( 'NONE',  ( 1.000000000000000000, 0.000000000000000000, 0.000000000000000000 ) ) ;
#15858=ORIENTED_EDGE ( 'NONE', *, *, #18229, .T. ) ;
#15860=CARTESIAN_POINT ( 'NONE',  ( 150.0000507999999968, 0.000000000000000000, 4.000000000000000000 ) ) ;
#15868=ORIENTED_EDGE ( 'NONE', *, *, #20511, .T. ) ;
#15869=CYLINDRICAL_SURFACE ( 'NONE', #17364, 72.00000000007199219 ) ;
#15874=DIRECTION ( 'NONE',  ( -1.000000000000000000, -0.000000000000000000, 0.000000000000000000 ) ) ;
#15881=CIRCLE ( 'NONE', #2340, 27.60000000002759890 ) ;
#15882=LINE ( 'NONE', #9519, #17180 ) ;
#15887=DIRECTION ( 'NONE',  ( 0.000000000000000000, 0.000000000000000000, 1.000000000000000000 ) ) ;
#15892=ORIENTED_EDGE ( 'NONE', *, *, #16344, .T. ) ;
#15895=VERTEX_POINT ( 'NONE', #18432 ) ;
#15896=EDGE_LOOP ( 'NONE', ( #10220, #4299 ) ) ;
#15898=AXIS2_PLACEMENT_3D ( 'NONE', #19869, #1759, #16178 ) ;
#15900=CYLINDRICAL_SURFACE ( 'NONE', #5173, 65.24900000006525147 ) ;
#15901=DIRECTION ( 'NONE',  ( 0.000000000000000000, 0.000000000000000000, -1.000000000000000000 ) ) ;
#15905=ADVANCED_FACE ( 'NONE', ( #13355 ), #5383, .T. ) ;
#15907=DIRECTION ( 'NONE',  ( -1.000000000000000000, 0.000000000000000000, 0.000000000000000000 ) ) ;
#15908=CARTESIAN_POINT ( 'NONE',  ( 0.000000000000000000, 63.05226888949891162, 15.11556105343481882 ) ) ;
#15915=EDGE_CURVE ( 'NONE', #659, #13680, #5208, .T. ) ;
#15917=ORIENTED_EDGE ( 'NONE', *, *, #4617, .T. ) ;
#15918=CARTESIAN_POINT ( 'NONE',  ( 19.99999999999999645, 55.05624179292029652, -35.01774179823726740 ) ) ;
#15921=AXIS2_PLACEMENT_3D ( 'NONE', #7009, #8486, #18459 ) ;
#15922=ORIENTED_EDGE ( 'NONE', *, *, #2562, .F. ) ;
#15926=CIRCLE ( 'NONE', #19640, 72.00000000007199219 ) ;
#15932=ORIENTED_EDGE ( 'NONE', *, *, #16035, .F. ) ;
#15935=VERTEX_POINT ( 'NONE', #16525 ) ;
#15941=CARTESIAN_POINT ( 'NONE',  ( 19.99999999999999645, -59.36728637277991538, -40.73727173906846843 ) ) ;
#15948=DIRECTION ( 'NONE',  ( -1.000000000000000000, 0.000000000000000000, -0.000000000000000000 ) ) ;
#15951=ORIENTED_EDGE ( 'NONE', *, *, #8194, .T. ) ;
#15956=CARTESIAN_POINT ( 'NONE',  ( 0.000000000000000000, -60.40676135667420965, -23.56039007469101421 ) ) ;
#15957=EDGE_CURVE ( 'NONE', #12350, #4610, #14357, .T. ) ;
#15971=ADVANCED_FACE ( 'NONE', ( #19367, #4855 ), #1780, .F. ) ;
#15972=CARTESIAN_POINT ( 'NONE',  ( 19.99999999999999645, 0.000000000000000000, 0.000000000000000000 ) ) ;
#15974=DIRECTION ( 'NONE',  ( -1.000000000000000000, 0.000000000000000000, 0.000000000000000000 ) ) ;
#15978=DIRECTION ( 'NONE',  ( 1.000000000000000000, -0.000000000000000000, -0.000000000000000000 ) ) ;
#15984=FACE_OUTER_BOUND ( 'NONE', #17813, .T. ) ;
#15985=EDGE_CURVE ( 'NONE', #10946, #125, #16198, .T. ) ;
#15989=AXIS2_PLACEMENT_3D ( 'NONE', #10076, #10387, #1913 ) ;
#15996=ORIENTED_EDGE ( 'NONE', *, *, #6233, .F. ) ;
#15998=ORIENTED_EDGE ( 'NONE', *, *, #4130, .T. ) ;
#16001=ORIENTED_EDGE ( 'NONE', *, *, #12887, .T. ) ;
#16002=VECTOR ( 'NONE', #17242, 1000.000000000000000 ) ;
#16010=AXIS2_PLACEMENT_3D ( 'NONE', #2669, #2870, #15693 ) ;
#16015=DIRECTION ( 'NONE',  ( 0.000000000000000000, 0.5195839500354344498, -0.8544194045464880150 ) ) ;
#16016=CIRCLE ( 'NONE', #3815, 27.60000000002759890 ) ;
#16017=DIRECTION ( 'NONE',  ( 0.000000000000000000, 0.9790840876823220240, 0.2034560130526374133 ) ) ;
#16021=VERTEX_POINT ( 'NONE', #4746 ) ;
#16024=VECTOR ( 'NONE', #6306, 1000.000000000000000 ) ;
#16028=ORIENTED_EDGE ( 'NONE', *, *, #2976, .T. ) ;
#16031=DIRECTION ( 'NONE',  ( 1.000000000000000000, -0.000000000000000000, -0.000000000000000000 ) ) ;
#16035=EDGE_CURVE ( 'NONE', #9551, #5163, #8247, .T. ) ;
#16042=CIRCLE ( 'NONE', #9926, 27.60000000002759890 ) ;
#16043=AXIS2_PLACEMENT_3D ( 'NONE', #17094, #2680, #13915 ) ;
#16045=CARTESIAN_POINT ( 'NONE',  ( 0.000000000000000000, -56.63599015375694989, 31.56633360682443268 ) ) ;
#16047=ORIENTED_EDGE ( 'NONE', *, *, #12819, .F. ) ;
#16049=CYLINDRICAL_SURFACE ( 'NONE', #6873, 27.60000000002759890 ) ;
#16050=ORIENTED_EDGE ( 'NONE', *, *, #19971, .T. ) ;
#16052=CYLINDRICAL_SURFACE ( 'NONE', #19838, 72.00000000007199219 ) ;
#16053=FACE_OUTER_BOUND ( 'NONE', #1309, .T. ) ;
#16054=AXIS2_PLACEMENT_3D ( 'NONE', #1641, #9778, #10089 ) ;
#16056=AXIS2_PLACEMENT_3D ( 'NONE', #1250, #7797, #12473 ) ;
#16057=DIRECTION ( 'NONE',  ( -1.000000000000000000, 0.000000000000000000, -0.000000000000000000 ) ) ;
#16060=VERTEX_POINT ( 'NONE', #6537 ) ;
#16062=FACE_OUTER_BOUND ( 'NONE', #6243, .T. ) ;
#16065=EDGE_CURVE ( 'NONE', #10739, #1628, #5051, .T. ) ;
#16066=EDGE_CURVE ( 'NONE', #4449, #17301, #20083, .T. ) ;
#16068=CARTESIAN_POINT ( 'NONE',  ( 0.000000000000000000, 0.000000000000000000, 0.000000000000000000 ) ) ;
#16069=EDGE_CURVE ( 'NONE', #18310, #2694, #6222, .T. ) ;
#16070=DIRECTION ( 'NONE',  ( -1.000000000000000000, -0.000000000000000000, -0.000000000000000000 ) ) ;
#16071=ORIENTED_EDGE ( 'NONE', *, *, #8476, .F. ) ;
#16074=DIRECTION ( 'NONE',  ( 0.000000000000000000, 0.000000000000000000, 1.000000000000000000 ) ) ;
#16080=CARTESIAN_POINT ( 'NONE',  ( 9.999999999999998224, -51.96384592647165590, -49.83732252579670075 ) ) ;
#16081=DIRECTION ( 'NONE',  ( 0.000000000000000000, -0.3984010898462296835, -0.9172113015054581542 ) ) ;
#16083=VERTEX_POINT ( 'NONE', #14515 ) ;
#16084=CARTESIAN_POINT ( 'NONE',  ( 0.000000000000000000, 23.08379033237351408, 61.02926039941444003 ) ) ;
#16085=DIRECTION ( 'NONE',  ( -1.000000000000000000, 0.000000000000000000, 0.000000000000000000 ) ) ;
#16088=DIRECTION ( 'NONE',  ( -1.000000000000000000, -0.000000000000000000, 0.000000000000000000 ) ) ;
#16089=CIRCLE ( 'NONE', #17773, 65.24900000006526568 ) ;
#16090=DIRECTION ( 'NONE',  ( -1.000000000000000000, -0.000000000000000000, 0.000000000000000000 ) ) ;
#16104=DIRECTION ( 'NONE',  ( -1.000000000000000000, 0.000000000000000000, 0.000000000000000000 ) ) ;
#16105=DIRECTION ( 'NONE',  ( -1.000000000000000000, 0.000000000000000000, -0.000000000000000000 ) ) ;
#16108=LINE ( 'NONE', #8143, #9896 ) ;
#16109=ORIENTED_EDGE ( 'NONE', *, *, #19203, .F. ) ;
#16113=EDGE_CURVE ( 'NONE', #13788, #9017, #9603, .T. ) ;
#16114=EDGE_LOOP ( 'NONE', ( #10512, #1697, #16369, #20479 ) ) ;
#16116=EDGE_CURVE ( 'NONE', #2965, #16270, #7156, .T. ) ;
#16121=EDGE_CURVE ( 'NONE', #12516, #10498, #3668, .T. ) ;
#16128=EDGE_LOOP ( 'NONE', ( #9134, #9995, #3099, #18060 ) ) ;
#16129=CARTESIAN_POINT ( 'NONE',  ( 9.999999999999998224, 64.36139404986010959, -32.27399814043808846 ) ) ;
#16130=AXIS2_PLACEMENT_3D ( 'NONE', #10294, #4021, #2236 ) ;
#16135=DIRECTION ( 'NONE',  ( -1.000000000000000000, -0.000000000000000000, -0.000000000000000000 ) ) ;
#16143=CARTESIAN_POINT ( 'NONE',  ( 19.99999999999999645, -58.26603306961992246, 42.29739224042451440 ) ) ;
#16144=AXIS2_PLACEMENT_3D ( 'NONE', #5742, #13597, #20045 ) ;
#16145=LINE ( 'NONE', #5282, #7523 ) ;
#16146=CARTESIAN_POINT ( 'NONE',  ( 9.999999999999998224, -0.9548212943370527617, 71.99366858485716136 ) ) ;
#16147=CIRCLE ( 'NONE', #15123, 72.00000000007199219 ) ;
#16149=ORIENTED_EDGE ( 'NONE', *, *, #13871, .F. ) ;
#16150=AXIS2_PLACEMENT_3D ( 'NONE', #493, #18284, #18796 ) ;
#16152=COLOUR_RGB ( '', 0.08235294, 0.09019608, 0.10196078) ;
#16154=CARTESIAN_POINT ( 'NONE',  ( 0.000000000000000000, 24.01204443665187327, 60.22865198596132785 ) ) ;
#16157=EDGE_CURVE ( 'NONE', #19080, #5222, #19711, .T. ) ;
#16161=AXIS2_PLACEMENT_3D ( 'NONE', #10713, #17177, #2659 ) ;
#16167=AXIS2_PLACEMENT_3D ( 'NONE', #12917, #19268, #11215 ) ;
#16169=CARTESIAN_POINT ( 'NONE',  ( 19.99999999999999645, -20.60847369612940128, -61.90898814327737654 ) ) ;
#16170=CARTESIAN_POINT ( 'NONE',  ( 19.99999999999999645, -63.48283426024874387, 33.96954156735347397 ) ) ;
#16173=ORIENTED_EDGE ( 'NONE', *, *, #10701, .F. ) ;
#16176=DIRECTION ( 'NONE',  ( -1.000000000000000000, -0.000000000000000000, -0.000000000000000000 ) ) ;
#16177=EDGE_LOOP ( 'NONE', ( #9841, #20941, #20562, #15848 ) ) ;
#16178=DIRECTION ( 'NONE',  ( 0.000000000000000000, 0.000000000000000000, 1.000000000000000000 ) ) ;
#16180=ADVANCED_FACE ( 'NONE', ( #13534 ), #18296, .T. ) ;
#16182=DIRECTION ( 'NONE',  ( -1.000000000000000000, 0.000000000000000000, 0.000000000000000000 ) ) ;
#16183=CARTESIAN_POINT ( 'NONE',  ( 19.99999999999999645, -51.96384592647164880, -49.83732252579670075 ) ) ;
#16186=CYLINDRICAL_SURFACE ( 'NONE', #9054, 27.60000000002759535 ) ;
#16188=EDGE_CURVE ( 'NONE', #4706, #6580, #15316, .T. ) ;
#16189=CARTESIAN_POINT ( 'NONE',  ( 19.99999999999999645, -10.77748419466653651, -63.93680186330482940 ) ) ;
#16193=FACE_OUTER_BOUND ( 'NONE', #3234, .T. ) ;
#16194=DIRECTION ( 'NONE',  ( 0.000000000000000000, 0.000000000000000000, 1.000000000000000000 ) ) ;
#16197=ORIENTED_EDGE ( 'NONE', *, *, #2752, .T. ) ;
#16198=LINE ( 'NONE', #8042, #10969 ) ;
#16199=CARTESIAN_POINT ( 'NONE',  ( 19.99999999999999645, -36.54710069451017063, -54.05313526368150434 ) ) ;
#16201=DIRECTION ( 'NONE',  ( 0.000000000000000000, 0.000000000000000000, 1.000000000000000000 ) ) ;
#16208=DIRECTION ( 'NONE',  ( -1.000000000000000000, -0.000000000000000000, -0.000000000000000000 ) ) ;
#16212=EDGE_CURVE ( 'NONE', #20215, #2640, #816, .T. ) ;
#16215=DIRECTION ( 'NONE',  ( 0.000000000000000000, 0.000000000000000000, 1.000000000000000000 ) ) ;
#16216=EDGE_CURVE ( 'NONE', #5396, #14177, #2189, .T. ) ;
#16220=DIRECTION ( 'NONE',  ( -1.000000000000000000, 0.000000000000000000, 0.000000000000000000 ) ) ;
#16222=FACE_OUTER_BOUND ( 'NONE', #4375, .T. ) ;
#16225=CARTESIAN_POINT ( 'NONE',  ( 19.99999999999999645, -53.26727847779570624, 48.44168704307610795 ) ) ;
#16229=CARTESIAN_POINT ( 'NONE',  ( -10.00000000000000000, 0.000000000000000000, 0.000000000000000000 ) ) ;
#16231=FACE_OUTER_BOUND ( 'NONE', #19940, .T. ) ;
#16234=DIRECTION ( 'NONE',  ( -1.000000000000000000, -0.000000000000000000, -0.000000000000000000 ) ) ;
#16237=DIRECTION ( 'NONE',  ( 0.000000000000000000, -0.2697967711570115612, -0.9629172873478027972 ) ) ;
#16241=FACE_OUTER_BOUND ( 'NONE', #4339, .T. ) ;
#16242=EDGE_CURVE ( 'NONE', #1429, #8808, #4140, .T. ) ;
#16244=FACE_OUTER_BOUND ( 'NONE', #13810, .T. ) ;
#16245=ORIENTED_EDGE ( 'NONE', *, *, #288, .F. ) ;
#16250=DIRECTION ( 'NONE',  ( 0.000000000000000000, 0.000000000000000000, 1.000000000000000000 ) ) ;
#16253=CARTESIAN_POINT ( 'NONE',  ( 85.00002539999999840, 9.184850993605147944E-16, -7.500000000000000000 ) ) ;
#16259=CYLINDRICAL_SURFACE ( 'NONE', #1036, 27.60000000002759890 ) ;
#16260=EDGE_LOOP ( 'NONE', ( #2195, #10475, #4255, #12095 ) ) ;
#16261=AXIS2_PLACEMENT_3D ( 'NONE', #19014, #2797, #4489 ) ;
#16262=CARTESIAN_POINT ( 'NONE',  ( 19.99999999999999645, -6.872116855663586321, 64.47358224882414390 ) ) ;
#16263=EDGE_CURVE ( 'NONE', #7264, #18514, #8218, .T. ) ;
#16265=AXIS2_PLACEMENT_3D ( 'NONE', #9031, #15492, #8915 ) ;
#16270=VERTEX_POINT ( 'NONE', #5676 ) ;
#16271=DIRECTION ( 'NONE',  ( 0.000000000000000000, 0.3984010898462422845, -0.9172113015054527141 ) ) ;
#16272=DIRECTION ( 'NONE',  ( -1.000000000000000000, -0.000000000000000000, -0.000000000000000000 ) ) ;
#16275=ORIENTED_EDGE ( 'NONE', *, *, #19216, .T. ) ;
#16277=AXIS2_PLACEMENT_3D ( 'NONE', #13705, #18584, #9044 ) ;
#16278=ORIENTED_EDGE ( 'NONE', *, *, #5598, .T. ) ;
#16280=LINE ( 'NONE', #3448, #20494 ) ;
#16282=VERTEX_POINT ( 'NONE', #19782 ) ;
#16284=EDGE_CURVE ( 'NONE', #15627, #12643, #17025, .T. ) ;
#16285=CARTESIAN_POINT ( 'NONE',  ( 19.99999999999999645, 0.000000000000000000, 0.000000000000000000 ) ) ;
#16292=DIRECTION ( 'NONE',  ( 0.000000000000000000, 0.000000000000000000, 1.000000000000000000 ) ) ;
#16295=CIRCLE ( 'NONE', #3098, 65.24900000006525147 ) ;
#16297=CARTESIAN_POINT ( 'NONE',  ( 0.000000000000000000, -54.08351995568730786, 35.76369202524482915 ) ) ;
#16302=DIRECTION ( 'NONE',  ( -1.000000000000000000, -0.000000000000000000, 0.000000000000000000 ) ) ;
#16304=ORIENTED_EDGE ( 'NONE', *, *, #1831, .F. ) ;
#16307=ORIENTED_EDGE ( 'NONE', *, *, #6369, .F. ) ;
#16309=VERTEX_POINT ( 'NONE', #9289 ) ;
#16316=EDGE_CURVE ( 'NONE', #19366, #10081, #17011, .T. ) ;
#16322=DIRECTION ( 'NONE',  ( -1.000000000000000000, -0.000000000000000000, -0.000000000000000000 ) ) ;
#16325=DIRECTION ( 'NONE',  ( -1.000000000000000000, -0.000000000000000000, -0.000000000000000000 ) ) ;
#16327=CARTESIAN_POINT ( 'NONE',  ( 19.99999999999999645, -23.08379033237394395, 61.02926039941428371 ) ) ;
#16329=ORIENTED_EDGE ( 'NONE', *, *, #18044, .T. ) ;
#16335=ORIENTED_EDGE ( 'NONE', *, *, #19593, .F. ) ;
#16338=VECTOR ( 'NONE', #8762, 1000.000000000000000 ) ;
#16340=EDGE_CURVE ( 'NONE', #17345, #2098, #2451, .T. ) ;
#16342=CIRCLE ( 'NONE', #12640, 27.60000000002759890 ) ;
#16343=VERTEX_POINT ( 'NONE', #12573 ) ;
#16344=EDGE_CURVE ( 'NONE', #10009, #9276, #10982, .T. ) ;
#16346=EDGE_CURVE ( 'NONE', #1099, #20364, #12369, .T. ) ;
#16351=VERTEX_POINT ( 'NONE', #4200 ) ;
#16354=EDGE_CURVE ( 'NONE', #17620, #6859, #5838, .T. ) ;
#16357=EDGE_LOOP ( 'NONE', ( #7365, #7132, #494, #5165 ) ) ;
#16361=EDGE_LOOP ( 'NONE', ( #9600, #11503, #4207, #8032 ) ) ;
#16364=AXIS2_PLACEMENT_3D ( 'NONE', #7557, #12773, #4596 ) ;
#16366=EDGE_CURVE ( 'NONE', #1411, #19744, #9236, .T. ) ;
#16369=ORIENTED_EDGE ( 'NONE', *, *, #19092, .T. ) ;
#16371=ADVANCED_FACE ( 'NONE', ( #9179 ), #17346, .T. ) ;
#16376=AXIS2_PLACEMENT_3D ( 'NONE', #14605, #8340, #82 ) ;
#16377=ORIENTED_EDGE ( 'NONE', *, *, #4562, .F. ) ;
#16379=DIRECTION ( 'NONE',  ( 1.000000000000000000, 0.000000000000000000, -0.000000000000000000 ) ) ;
#16380=CYLINDRICAL_SURFACE ( 'NONE', #1244, 72.00000000007199219 ) ;
#16381=VECTOR ( 'NONE', #2343, 1000.000000000000000 ) ;
#16383=AXIS2_PLACEMENT_3D ( 'NONE', #20702, #11174, #18818 ) ;
#16387=AXIS2_PLACEMENT_3D ( 'NONE', #1002, #15194, #782 ) ;
#16393=CIRCLE ( 'NONE', #17431, 65.24900000006525147 ) ;
#16400=ORIENTED_EDGE ( 'NONE', *, *, #6078, .F. ) ;
#16401=EDGE_CURVE ( 'NONE', #4706, #3596, #15434, .T. ) ;
#16402=DIRECTION ( 'NONE',  ( 0.000000000000000000, 0.000000000000000000, 1.000000000000000000 ) ) ;
#16403=DIRECTION ( 'NONE',  ( 0.000000000000000000, 0.5195839500354344498, -0.8544194045464880150 ) ) ;
#16405=ORIENTED_EDGE ( 'NONE', *, *, #16354, .T. ) ;
#16408=CIRCLE ( 'NONE', #16740, 72.00000000007199219 ) ;
#16409=DIRECTION ( 'NONE',  ( 0.000000000000000000, 0.000000000000000000, 1.000000000000000000 ) ) ;
#16410=DIRECTION ( 'NONE',  ( 1.000000000000000000, -0.000000000000000000, -0.000000000000000000 ) ) ;
#16412=ORIENTED_EDGE ( 'NONE', *, *, #20714, .T. ) ;
#16422=CARTESIAN_POINT ( 'NONE',  ( 19.99999999999999645, 0.000000000000000000, 0.000000000000000000 ) ) ;
#16424=EDGE_CURVE ( 'NONE', #11920, #13947, #16673, .T. ) ;
#16425=CARTESIAN_POINT ( 'NONE',  ( 19.99999999999999645, 19.38316218894212639, 61.87375713200996330 ) ) ;
#16428=ORIENTED_EDGE ( 'NONE', *, *, #16316, .T. ) ;
#16432=CARTESIAN_POINT ( 'NONE',  ( 9.999999999999998224, 58.26603306962022089, -42.29739224042413070 ) ) ;
#16433=CIRCLE ( 'NONE', #17464, 27.60000000002759890 ) ;
#16436=ORIENTED_EDGE ( 'NONE', *, *, #4320, .F. ) ;
#16438=ADVANCED_FACE ( 'NONE', ( #5777 ), #20410, .T. ) ;
#16440=CARTESIAN_POINT ( 'NONE',  ( 19.99999999999999645, 63.85430960833490843, -11.25592921604860663 ) ) ;
#16441=CARTESIAN_POINT ( 'NONE',  ( 19.99999999999999645, 58.44960523466241398, -28.06621538408611016 ) ) ;
#16444=ORIENTED_EDGE ( 'NONE', *, *, #381, .T. ) ;
#16447=AXIS2_PLACEMENT_3D ( 'NONE', #4592, #1418, #11057 ) ;
#16448=CYLINDRICAL_SURFACE ( 'NONE', #14578, 27.60000000002760245 ) ;
#16451=LINE ( 'NONE', #8292, #10620 ) ;
#16452=CIRCLE ( 'NONE', #8328, 27.60000000002759535 ) ;
#16456=ORIENTED_EDGE ( 'NONE', *, *, #4230, .T. ) ;
#16457=CARTESIAN_POINT ( 'NONE',  ( 19.99999999999999645, 0.000000000000000000, 0.000000000000000000 ) ) ;
#16458=DIRECTION ( 'NONE',  ( -1.000000000000000000, -0.000000000000000000, 0.000000000000000000 ) ) ;
#16459=ORIENTED_EDGE ( 'NONE', *, *, #1243, .T. ) ;
#16464=CIRCLE ( 'NONE', #6634, 27.60000000002760245 ) ;
#16466=EDGE_CURVE ( 'NONE', #9191, #2016, #12334, .T. ) ;
#16468=AXIS2_PLACEMENT_3D ( 'NONE', #17604, #10822, #5940 ) ;
#16474=EDGE_CURVE ( 'NONE', #1539, #4998, #16342, .T. ) ;
#16479=ORIENTED_EDGE ( 'NONE', *, *, #16121, .T. ) ;
#16481=DIRECTION ( 'NONE',  ( -1.000000000000000000, 0.000000000000000000, 0.000000000000000000 ) ) ;
#16487=CARTESIAN_POINT ( 'NONE',  ( 9.999999999999998224, 20.34307325858883431, -69.06634035770285607 ) ) ;
#16493=LINE ( 'NONE', #14898, #10754 ) ;
#16495=DIRECTION ( 'NONE',  ( 0.000000000000000000, 0.8878852184023763305, -0.4600650377311499284 ) ) ;
#16499=VERTEX_POINT ( 'NONE', #6512 ) ;
#16503=DIRECTION ( 'NONE',  ( -1.000000000000000000, -0.000000000000000000, -0.000000000000000000 ) ) ;
#16506=AXIS2_PLACEMENT_3D ( 'NONE', #14516, #9315, #7730 ) ;
#16507=ORIENTED_EDGE ( 'NONE', *, *, #5420, .F. ) ;
#16513=CARTESIAN_POINT ( 'NONE',  ( 19.99999999999999645, 0.000000000000000000, 0.000000000000000000 ) ) ;
#16517=ORIENTED_EDGE ( 'NONE', *, *, #4456, .F. ) ;
#16521=ORIENTED_EDGE ( 'NONE', *, *, #15985, .F. ) ;
#16522=CARTESIAN_POINT ( 'NONE',  ( 19.99999999999999645, -14.55863677812166124, 63.60407295269099137 ) ) ;
#16523=CARTESIAN_POINT ( 'NONE',  ( 0.000000000000000000, 39.37110852956814000, 51.51683813304883586 ) ) ;
#16525=CARTESIAN_POINT ( 'NONE',  ( 19.99999999999999645, 8.857208570069795783, 71.45313048675087941 ) ) ;
#16526=EDGE_CURVE ( 'NONE', #2438, #2694, #9599, .T. ) ;
#16530=CARTESIAN_POINT ( 'NONE',  ( 0.000000000000000000, 0.000000000000000000, 0.000000000000000000 ) ) ;
#16532=ORIENTED_EDGE ( 'NONE', *, *, #8694, .F. ) ;
#16536=ORIENTED_EDGE ( 'NONE', *, *, #11804, .T. ) ;
#16545=DIRECTION ( 'NONE',  ( 0.000000000000000000, 0.000000000000000000, -1.000000000000000000 ) ) ;
#16547=DIRECTION ( 'NONE',  ( 0.000000000000000000, 0.000000000000000000, 1.000000000000000000 ) ) ;
#16550=EDGE_CURVE ( 'NONE', #2694, #10147, #19978, .T. ) ;
#16556=ORIENTED_EDGE ( 'NONE', *, *, #13601, .T. ) ;
#16561=ORIENTED_EDGE ( 'NONE', *, *, #5463, .T. ) ;
#16562=DIRECTION ( 'NONE',  ( -1.000000000000000000, 0.000000000000000000, 0.000000000000000000 ) ) ;
#16563=LINE ( 'NONE', #14284, #602 ) ;
#16566=VECTOR ( 'NONE', #20200, 1000.000000000000000 ) ;
#16569=ORIENTED_EDGE ( 'NONE', *, *, #19576, .T. ) ;
#16570=CARTESIAN_POINT ( 'NONE',  ( 0.000000000000000000, 0.000000000000000000, 0.000000000000000000 ) ) ;
#16571=CARTESIAN_POINT ( 'NONE',  ( 0.000000000000000000, 63.85430960833490843, -11.25592921604860663 ) ) ;
#16574=EDGE_CURVE ( 'NONE', #20260, #5709, #13565, .T. ) ;
#16576=EDGE_CURVE ( 'NONE', #3596, #16499, #18295, .T. ) ;
#16578=FACE_OUTER_BOUND ( 'NONE', #16691, .T. ) ;
#16586=DIRECTION ( 'NONE',  ( -1.000000000000000000, 0.000000000000000000, 0.000000000000000000 ) ) ;
#16588=DIRECTION ( 'NONE',  ( -1.000000000000000000, 0.000000000000000000, 0.000000000000000000 ) ) ;
#16591=EDGE_CURVE ( 'NONE', #16060, #8227, #587, .T. ) ;
#16594=CARTESIAN_POINT ( 'NONE',  ( 19.99999999999999645, 0.000000000000000000, 0.000000000000000000 ) ) ;
#16600=DIRECTION ( 'NONE',  ( 0.000000000000000000, -0.9790840876823205807, -0.2034560130526446575 ) ) ;
#16604=DIRECTION ( 'NONE',  ( -1.000000000000000000, -0.000000000000000000, -0.000000000000000000 ) ) ;
#16606=ORIENTED_EDGE ( 'NONE', *, *, #20737, .T. ) ;
#16608=ORIENTED_EDGE ( 'NONE', *, *, #10901, .T. ) ;
#16609=FACE_OUTER_BOUND ( 'NONE', #9075, .T. ) ;
#16613=DIRECTION ( 'NONE',  ( 0.000000000000000000, 0.000000000000000000, 1.000000000000000000 ) ) ;
#16620=EDGE_CURVE ( 'NONE', #15651, #3116, #4427, .T. ) ;
#16621=ADVANCED_FACE ( 'NONE', ( #14995 ), #18489, .T. ) ;
#16627=EDGE_CURVE ( 'NONE', #2326, #1075, #8513, .T. ) ;
#16631=VECTOR ( 'NONE', #9884, 1000.000000000000000 ) ;
#16633=LINE ( 'NONE', #5083, #6836 ) ;
#16635=CARTESIAN_POINT ( 'NONE',  ( 0.000000000000000000, 0.000000000000000000, 0.000000000000000000 ) ) ;
#16636=CIRCLE ( 'NONE', #6152, 27.60000000002759890 ) ;
#16637=ORIENTED_EDGE ( 'NONE', *, *, #17627, .T. ) ;
#16645=ORIENTED_EDGE ( 'NONE', *, *, #19092, .F. ) ;
#16646=CARTESIAN_POINT ( 'NONE',  ( 19.99999999999999645, -31.98952867950285395, -56.39803944231618971 ) ) ;
#16648=CARTESIAN_POINT ( 'NONE',  ( 19.99999999999999645, -63.17103598352137794, 16.33561182745118501 ) ) ;
#16650=AXIS2_PLACEMENT_3D ( 'NONE', #114, #11145, #9665 ) ;
#16651=DIRECTION ( 'NONE',  ( -1.000000000000000000, -0.000000000000000000, -0.000000000000000000 ) ) ;
#16655=LINE ( 'NONE', #8800, #10177 ) ;
#16656=CARTESIAN_POINT ( 'NONE',  ( 19.99999999999999645, -48.70996102988652154, -42.79495875147824790 ) ) ;
#16657=ORIENTED_EDGE ( 'NONE', *, *, #10683, .F. ) ;
#16673=CIRCLE ( 'NONE', #11933, 65.24900000006526568 ) ;
#16676=DIRECTION ( 'NONE',  ( -1.000000000000000000, 0.000000000000000000, 0.000000000000000000 ) ) ;
#16677=CARTESIAN_POINT ( 'NONE',  ( 19.99999999999999645, -43.56693332842820610, 48.57318520917490190 ) ) ;
#16683=VERTEX_POINT ( 'NONE', #6816 ) ;
#16690=AXIS2_PLACEMENT_3D ( 'NONE', #17192, #19094, #13899 ) ;
#16691=EDGE_LOOP ( 'NONE', ( #10856, #17981, #19707, #14551 ) ) ;
#16692=ORIENTED_EDGE ( 'NONE', *, *, #2964, .T. ) ;
#16694=CARTESIAN_POINT ( 'NONE',  ( 19.99999999999999645, 31.98952867950324830, 56.39803944231596944 ) ) ;
#16695=AXIS2_PLACEMENT_3D ( 'NONE', #15395, #10521, #13288 ) ;
#16697=CARTESIAN_POINT ( 'NONE',  ( 0.000000000000000000, 10.77748419466781726, -63.93680186330462334 ) ) ;
#16700=CIRCLE ( 'NONE', #2493, 72.00000000007199219 ) ;
#16702=AXIS2_PLACEMENT_3D ( 'NONE', #14302, #14201, #2740 ) ;
#16705=DIRECTION ( 'NONE',  ( 1.000000000000000000, 0.000000000000000000, 0.000000000000000000 ) ) ;
#16706=ORIENTED_EDGE ( 'NONE', *, *, #19954, .F. ) ;
#16708=EDGE_CURVE ( 'NONE', #8862, #12428, #6116, .T. ) ;
#16710=AXIS2_PLACEMENT_3D ( 'NONE', #20897, #4784, #11978 ) ;
#16713=CARTESIAN_POINT ( 'NONE',  ( 9.999999999999998224, 51.96384592647199696, 49.83732252579632416 ) ) ;
#16714=ORIENTED_EDGE ( 'NONE', *, *, #8322, .F. ) ;
#16715=CARTESIAN_POINT ( 'NONE',  ( 0.000000000000000000, -70.29359119158496583, 15.58239511117263554 ) ) ;
#16720=ORIENTED_EDGE ( 'NONE', *, *, #11064, .F. ) ;
#16723=ORIENTED_EDGE ( 'NONE', *, *, #11240, .T. ) ;
#16724=ORIENTED_EDGE ( 'NONE', *, *, #13765, .T. ) ;
#16726=FACE_OUTER_BOUND ( 'NONE', #3152, .T. ) ;
#16730=CARTESIAN_POINT ( 'NONE',  ( 19.99999999999999645, 70.29359119158506530, -15.58239511117215059 ) ) ;
#16734=DIRECTION ( 'NONE',  ( 0.000000000000000000, 0.000000000000000000, 1.000000000000000000 ) ) ;
#16738=DIRECTION ( 'NONE',  ( 0.000000000000000000, 0.000000000000000000, 1.000000000000000000 ) ) ;
#16740=AXIS2_PLACEMENT_3D ( 'NONE', #2011, #11964, #16734 ) ;
#16741=ORIENTED_EDGE ( 'NONE', *, *, #9769, .F. ) ;
#16744=CARTESIAN_POINT ( 'NONE',  ( 9.999999999999998224, 27.80658314415226684, 66.41380830714133765 ) ) ;
#16747=EDGE_CURVE ( 'NONE', #19634, #9479, #15615, .T. ) ;
#16749=ORIENTED_EDGE ( 'NONE', *, *, #19203, .T. ) ;
#16755=FACE_OUTER_BOUND ( 'NONE', #7222, .T. ) ;
#16757=CARTESIAN_POINT ( 'NONE',  ( 19.99999999999999645, 19.38316218894212639, 61.87375713200996330 ) ) ;
#16759=LINE ( 'NONE', #5722, #16381 ) ;
#16761=DIRECTION ( 'NONE',  ( -1.000000000000000000, 0.000000000000000000, -0.000000000000000000 ) ) ;
#16764=DIRECTION ( 'NONE',  ( 0.000000000000000000, 0.000000000000000000, 1.000000000000000000 ) ) ;
#16770=DIRECTION ( 'NONE',  ( -1.000000000000000000, -0.000000000000000000, -0.000000000000000000 ) ) ;
#16771=ORIENTED_EDGE ( 'NONE', *, *, #18699, .T. ) ;
#16773=VERTEX_POINT ( 'NONE', #2593 ) ;
#16774=VECTOR ( 'NONE', #533, 1000.000000000000000 ) ;
#16777=DIRECTION ( 'NONE',  ( 0.000000000000000000, 0.000000000000000000, 1.000000000000000000 ) ) ;
#16782=CIRCLE ( 'NONE', #6302, 65.24900000006525147 ) ;
#16783=CARTESIAN_POINT ( 'NONE',  ( 19.99999999999999645, 27.80658314415225973, 66.41380830714133765 ) ) ;
#16788=DIRECTION ( 'NONE',  ( 1.000000000000000000, -0.000000000000000000, -0.000000000000000000 ) ) ;
#16790=CARTESIAN_POINT ( 'NONE',  ( 19.99999999999999645, -24.01204443665229604, 60.22865198596116443 ) ) ;
#16791=ORIENTED_EDGE ( 'NONE', *, *, #18268, .T. ) ;
#16795=CIRCLE ( 'NONE', #2634, 72.00000000007199219 ) ;
#16798=EDGE_LOOP ( 'NONE', ( #18091, #14752, #10769, #2043 ) ) ;
#16799=CARTESIAN_POINT ( 'NONE',  ( 0.000000000000000000, -24.01204443665229604, 60.22865198596116443 ) ) ;
#16805=AXIS2_PLACEMENT_3D ( 'NONE', #1888, #16105, #16403 ) ;
#16810=CIRCLE ( 'NONE', #11058, 65.24900000006525147 ) ;
#16811=CARTESIAN_POINT ( 'NONE',  ( 0.000000000000000000, 0.000000000000000000, 0.000000000000000000 ) ) ;
#16815=CIRCLE ( 'NONE', #11402, 27.60000000002759535 ) ;
#16816=EDGE_CURVE ( 'NONE', #12290, #857, #12546, .T. ) ;
#16821=CIRCLE ( 'NONE', #3288, 7.500000000000000000 ) ;
#16824=EDGE_CURVE ( 'NONE', #3130, #6711, #15926, .T. ) ;
#16826=CARTESIAN_POINT ( 'NONE',  ( 19.99999999999999645, -31.17893654894269773, 57.31758819669160232 ) ) ;
#16829=EDGE_LOOP ( 'NONE', ( #15328, #13704, #662, #19966 ) ) ;
#16830=DIRECTION ( 'NONE',  ( 0.000000000000000000, -1.000000000000000000, -0.000000000000000000 ) ) ;
#16836=DIRECTION ( 'NONE',  ( 0.000000000000000000, -0.3984010898462486683, 0.9172113015054499385 ) ) ;
#16837=AXIS2_PLACEMENT_3D ( 'NONE', #13207, #11611, #18086 ) ;
#16842=CARTESIAN_POINT ( 'NONE',  ( 0.000000000000000000, -35.35772184876843482, -54.34979580218228534 ) ) ;
#16847=EDGE_CURVE ( 'NONE', #13848, #17803, #12197, .T. ) ;
#16848=AXIS2_PLACEMENT_3D ( 'NONE', #7367, #6090, #17235 ) ;
#16851=CIRCLE ( 'NONE', #19888, 72.00000000007199219 ) ;
#16852=ORIENTED_EDGE ( 'NONE', *, *, #4192, .F. ) ;
#16854=EDGE_CURVE ( 'NONE', #1518, #10611, #13551, .T. ) ;
#16856=CARTESIAN_POINT ( 'NONE',  ( 19.99999999999999645, 38.22257254261820947, -61.01667762370099979 ) ) ;
#16859=VERTEX_POINT ( 'NONE', #2693 ) ;
#16860=FACE_OUTER_BOUND ( 'NONE', #6965, .T. ) ;
#16863=ADVANCED_FACE ( 'NONE', ( #20384 ), #12345, .T. ) ;
#16864=ORIENTED_EDGE ( 'NONE', *, *, #4009, .T. ) ;
#16867=LINE ( 'NONE', #19828, #20414 ) ;
#16869=EDGE_CURVE ( 'NONE', #9681, #5222, #4384, .T. ) ;
#16872=FACE_OUTER_BOUND ( 'NONE', #1602, .T. ) ;
#16874=DIRECTION ( 'NONE',  ( -1.000000000000000000, -0.000000000000000000, -0.000000000000000000 ) ) ;
#16875=EDGE_CURVE ( 'NONE', #1099, #11750, #4412, .T. ) ;
#16878=ADVANCED_FACE ( 'NONE', ( #12129 ), #17320, .T. ) ;
#16881=DIRECTION ( 'NONE',  ( -1.000000000000000000, 0.000000000000000000, 0.000000000000000000 ) ) ;
#16884=VERTEX_POINT ( 'NONE', #15729 ) ;
#16885=EDGE_CURVE ( 'NONE', #2292, #1859, #7101, .T. ) ;
#16887=CARTESIAN_POINT ( 'NONE',  ( 0.000000000000000000, -65.23577793412343340, -1.313498510942392450 ) ) ;
#16888=VERTEX_POINT ( 'NONE', #17435 ) ;
#16896=ORIENTED_EDGE ( 'NONE', *, *, #14919, .T. ) ;
#16897=ADVANCED_FACE ( 'NONE', ( #4056 ), #13831, .T. ) ;
#16898=DIRECTION ( 'NONE',  ( 1.000000000000000000, 0.000000000000000000, 0.000000000000000000 ) ) ;
#16912=ORIENTED_EDGE ( 'NONE', *, *, #7299, .T. ) ;
#16921=ORIENTED_EDGE ( 'NONE', *, *, #3170, .F. ) ;
#16923=DIRECTION ( 'NONE',  ( 0.000000000000000000, 0.000000000000000000, 1.000000000000000000 ) ) ;
#16924=VERTEX_POINT ( 'NONE', #1538 ) ;
#16925=CYLINDRICAL_SURFACE ( 'NONE', #14315, 72.00000000007199219 ) ;
#16927=CYLINDRICAL_SURFACE ( 'NONE', #1762, 72.00000000007199219 ) ;
#16932=FACE_OUTER_BOUND ( 'NONE', #12649, .T. ) ;
#16933=AXIS2_PLACEMENT_3D ( 'NONE', #8945, #7676, #10959 ) ;
#16934=DIRECTION ( 'NONE',  ( -1.000000000000000000, 0.000000000000000000, 0.000000000000000000 ) ) ;
#16935=LINE ( 'NONE', #8877, #18014 ) ;
#16941=CYLINDRICAL_SURFACE ( 'NONE', #20561, 27.60000000002760245 ) ;
#16944=CARTESIAN_POINT ( 'NONE',  ( 19.99999999999999645, 0.000000000000000000, 0.000000000000000000 ) ) ;
#16945=VERTEX_POINT ( 'NONE', #14470 ) ;
#16952=CARTESIAN_POINT ( 'NONE',  ( 0.000000000000000000, -19.38316218894255627, 61.87375713200982119 ) ) ;
#16954=ORIENTED_EDGE ( 'NONE', *, *, #14351, .T. ) ;
#16955=ORIENTED_EDGE ( 'NONE', *, *, #9604, .T. ) ;
#16956=DIRECTION ( 'NONE',  ( -1.000000000000000000, 0.000000000000000000, 0.000000000000000000 ) ) ;
#16959=DIRECTION ( 'NONE',  ( -1.000000000000000000, -0.000000000000000000, 0.000000000000000000 ) ) ;
#16966=EDGE_CURVE ( 'NONE', #5273, #17663, #20804, .T. ) ;
#16969=CARTESIAN_POINT ( 'NONE',  ( 19.99999999999999645, -60.40676135667455071, 23.56039007469017221 ) ) ;
#16970=ORIENTED_EDGE ( 'NONE', *, *, #18571, .T. ) ;
#16971=CYLINDRICAL_SURFACE ( 'NONE', #16986, 65.24900000006525147 ) ;
#16975=AXIS2_PLACEMENT_3D ( 'NONE', #17474, #12386, #1271 ) ;
#16977=DIRECTION ( 'NONE',  ( 0.000000000000000000, 0.000000000000000000, 1.000000000000000000 ) ) ;
#16980=FACE_OUTER_BOUND ( 'NONE', #1667, .T. ) ;
#16981=FACE_OUTER_BOUND ( 'NONE', #14254, .T. ) ;
#16986=AXIS2_PLACEMENT_3D ( 'NONE', #14128, #2570, #5733 ) ;
#16996=ADVANCED_FACE ( 'NONE', ( #13072 ), #5014, .T. ) ;
#16997=DIRECTION ( 'NONE',  ( 1.000000000000000000, -0.000000000000000000, -0.000000000000000000 ) ) ;
#17004=CIRCLE ( 'NONE', #12637, 27.60000000002759535 ) ;
#17005=DIRECTION ( 'NONE',  ( -1.000000000000000000, -0.000000000000000000, -0.000000000000000000 ) ) ;
#17007=VERTEX_POINT ( 'NONE', #1837 ) ;
#17011=CIRCLE ( 'NONE', #8879, 27.60000000002759890 ) ;
#17014=CARTESIAN_POINT ( 'NONE',  ( 19.99999999999999645, 0.000000000000000000, 72.00000000007199219 ) ) ;
#17018=AXIS2_PLACEMENT_3D ( 'NONE', #15782, #89, #15887 ) ;
#17024=EDGE_LOOP ( 'NONE', ( #11663, #7053, #18462, #15792 ) ) ;
#17025=LINE ( 'NONE', #8435, #12279 ) ;
#17026=ORIENTED_EDGE ( 'NONE', *, *, #2976, .F. ) ;
#17027=CIRCLE ( 'NONE', #13670, 27.60000000002760601 ) ;
#17043=AXIS2_PLACEMENT_3D ( 'NONE', #6489, #5016, #138 ) ;
#17046=AXIS2_PLACEMENT_3D ( 'NONE', #1586, #3562, #6740 ) ;
#17048=DIRECTION ( 'NONE',  ( -1.000000000000000000, -0.000000000000000000, 0.000000000000000000 ) ) ;
#17049=CARTESIAN_POINT ( 'NONE',  ( 19.99999999999999645, -65.23577793412343340, -1.313498510942392450 ) ) ;
#17053=DIRECTION ( 'NONE',  ( 1.000000000000000000, 0.000000000000000000, 0.000000000000000000 ) ) ;
#17055=DIRECTION ( 'NONE',  ( 0.000000000000000000, 0.000000000000000000, 1.000000000000000000 ) ) ;
#17060=CARTESIAN_POINT ( 'NONE',  ( 19.99999999999999645, 11.98658579560587789, 64.13855129306472236 ) ) ;
#17061=VECTOR ( 'NONE', #6206, 1000.000000000000000 ) ;
#17062=EDGE_LOOP ( 'NONE', ( #12188, #14132, #11684, #12838 ) ) ;
#17066=CIRCLE ( 'NONE', #11643, 27.60000000002759535 ) ;
#17068=LINE ( 'NONE', #7738, #20709 ) ;
#17071=CARTESIAN_POINT ( 'NONE',  ( 19.99999999999999645, 31.98952867950403345, -56.39803944231551469 ) ) ;
#17077=PRESENTATION_STYLE_ASSIGNMENT (( #10617 ) ) ;
#17084=DIRECTION ( 'NONE',  ( 0.000000000000000000, 0.5195839500354290097, 0.8544194045464913456 ) ) ;
#17086=LINE ( 'NONE', #15494, #1230 ) ;
#17094=CARTESIAN_POINT ( 'NONE',  ( 19.99999999999999645, 0.000000000000000000, 0.000000000000000000 ) ) ;
#17095=ORIENTED_EDGE ( 'NONE', *, *, #4820, .T. ) ;
#17100=FACE_OUTER_BOUND ( 'NONE', #17286, .T. ) ;
#17101=AXIS2_PLACEMENT_3D ( 'NONE', #8313, #5341, #14787 ) ;
#17106=DIRECTION ( 'NONE',  ( 0.000000000000000000, 0.000000000000000000, 1.000000000000000000 ) ) ;
#17108=EDGE_LOOP ( 'NONE', ( #20617, #15547 ) ) ;
#17111=VERTEX_POINT ( 'NONE', #13488 ) ;
#17114=VECTOR ( 'NONE', #14146, 1000.000000000000000 ) ;
#17118=DIRECTION ( 'NONE',  ( 0.000000000000000000, 0.000000000000000000, 1.000000000000000000 ) ) ;
#17122=ORIENTED_EDGE ( 'NONE', *, *, #9082, .T. ) ;
#17124=ADVANCED_FACE ( 'NONE', ( #13276 ), #16448, .T. ) ;
#17127=EDGE_CURVE ( 'NONE', #17270, #20602, #14912, .T. ) ;
#17128=EDGE_CURVE ( 'NONE', #1644, #18621, #20315, .T. ) ;
#17134=ORIENTED_EDGE ( 'NONE', *, *, #20714, .F. ) ;
#17138=CARTESIAN_POINT ( 'NONE',  ( 0.000000000000000000, 14.55863677812122425, 63.60407295269110506 ) ) ;
#17142=DIRECTION ( 'NONE',  ( 0.000000000000000000, 0.000000000000000000, -1.000000000000000000 ) ) ;
#17144=VERTEX_POINT ( 'NONE', #5623 ) ;
#17145=ADVANCED_FACE ( 'NONE', ( #4461 ), #10929, .T. ) ;
#17146=DIRECTION ( 'NONE',  ( -1.000000000000000000, -0.000000000000000000, -0.000000000000000000 ) ) ;
#17151=EDGE_CURVE ( 'NONE', #9587, #8741, #13903, .T. ) ;
#17155=EDGE_CURVE ( 'NONE', #3220, #3544, #17406, .T. ) ;
#17158=CIRCLE ( 'NONE', #15457, 72.00000000007199219 ) ;
#17159=DIRECTION ( 'NONE',  ( 0.000000000000000000, 0.000000000000000000, -1.000000000000000000 ) ) ;
#17160=AXIS2_PLACEMENT_3D ( 'NONE', #8359, #17814, #16215 ) ;
#17161=DIRECTION ( 'NONE',  ( -1.000000000000000000, -0.000000000000000000, 0.000000000000000000 ) ) ;
#17162=DIRECTION ( 'NONE',  ( -1.000000000000000000, -0.000000000000000000, -0.000000000000000000 ) ) ;
#17164=AXIS2_PLACEMENT_3D ( 'NONE', #9091, #5906, #6214 ) ;
#17167=ORIENTED_EDGE ( 'NONE', *, *, #4652, .F. ) ;
#17168=CARTESIAN_POINT ( 'NONE',  ( 19.99999999999999645, 0.000000000000000000, 0.000000000000000000 ) ) ;
#17169=EDGE_CURVE ( 'NONE', #2557, #10176, #11219, .T. ) ;
#17171=VECTOR ( 'NONE', #5495, 1000.000000000000000 ) ;
#17172=DIRECTION ( 'NONE',  ( 0.000000000000000000, 0.000000000000000000, 1.000000000000000000 ) ) ;
#17174=CARTESIAN_POINT ( 'NONE',  ( 0.000000000000000000, 5.762283366692075859, -64.99406197038663890 ) ) ;
#17177=DIRECTION ( 'NONE',  ( -1.000000000000000000, 0.000000000000000000, 0.000000000000000000 ) ) ;
#17178=VERTEX_POINT ( 'NONE', #20467 ) ;
#17180=VECTOR ( 'NONE', #19170, 1000.000000000000000 ) ;
#17181=ORIENTED_EDGE ( 'NONE', *, *, #5149, .F. ) ;
#17187=VERTEX_POINT ( 'NONE', #7208 ) ;
#17188=DIRECTION ( 'NONE',  ( 0.000000000000000000, 0.000000000000000000, 1.000000000000000000 ) ) ;
#17189=EDGE_CURVE ( 'NONE', #11808, #11920, #20351, .T. ) ;
#17192=CARTESIAN_POINT ( 'NONE',  ( 19.99999999999999645, 63.05226888949891162, 15.11556105343481882 ) ) ;
#17193=CIRCLE ( 'NONE', #20572, 27.60000000002759535 ) ;
#17195=VECTOR ( 'NONE', #8776, 1000.000000000000000 ) ;
#17200=ORIENTED_EDGE ( 'NONE', *, *, #13150, .T. ) ;
#17201=CARTESIAN_POINT ( 'NONE',  ( 19.99999999999999645, -11.98658579560631843, 64.13855129306463709 ) ) ;
#17202=ORIENTED_EDGE ( 'NONE', *, *, #13605, .T. ) ;
#17206=LINE ( 'NONE', #6161, #7915 ) ;
#17214=DIRECTION ( 'NONE',  ( -1.000000000000000000, 0.000000000000000000, -0.000000000000000000 ) ) ;
#17219=FILL_AREA_STYLE ('',( #12343 ) ) ;
#17221=DIRECTION ( 'NONE',  ( 0.000000000000000000, 0.000000000000000000, -1.000000000000000000 ) ) ;
#17222=VERTEX_POINT ( 'NONE', #6051 ) ;
#17228=DIRECTION ( 'NONE',  ( 0.000000000000000000, 0.000000000000000000, -1.000000000000000000 ) ) ;
#17231=DIRECTION ( 'NONE',  ( -1.000000000000000000, 0.000000000000000000, 0.000000000000000000 ) ) ;
#17232=ORIENTED_EDGE ( 'NONE', *, *, #9866, .F. ) ;
#17235=DIRECTION ( 'NONE',  ( 0.000000000000000000, 0.000000000000000000, 1.000000000000000000 ) ) ;
#17239=ADVANCED_FACE ( 'NONE', ( #5945 ), #2671, .T. ) ;
#17242=DIRECTION ( 'NONE',  ( -1.000000000000000000, 0.000000000000000000, 0.000000000000000000 ) ) ;
#17249=ORIENTED_EDGE ( 'NONE', *, *, #20228, .F. ) ;
#17250=LINE ( 'NONE', #8979, #19528 ) ;
#17253=ORIENTED_EDGE ( 'NONE', *, *, #12765, .T. ) ;
#17258=CYLINDRICAL_SURFACE ( 'NONE', #18515, 27.60000000002759890 ) ;
#17259=EDGE_CURVE ( 'NONE', #14491, #18356, #18325, .T. ) ;
#17270=VERTEX_POINT ( 'NONE', #14438 ) ;
#17275=VERTEX_POINT ( 'NONE', #12847 ) ;
#17282=EDGE_CURVE ( 'NONE', #16924, #14502, #15279, .T. ) ;
#17285=ORIENTED_EDGE ( 'NONE', *, *, #8593, .T. ) ;
#17286=EDGE_LOOP ( 'NONE', ( #14249, #16706, #7220, #16561 ) ) ;
#17298=ORIENTED_EDGE ( 'NONE', *, *, #1907, .T. ) ;
#17300=LINE ( 'NONE', #9242, #60 ) ;
#17301=VERTEX_POINT ( 'NONE', #6459 ) ;
#17304=VECTOR ( 'NONE', #6499, 1000.000000000000000 ) ;
#17307=VERTEX_POINT ( 'NONE', #19101 ) ;
#17319=LINE ( 'NONE', #6072, #7621 ) ;
#17320=CYLINDRICAL_SURFACE ( 'NONE', #16261, 65.24900000006525147 ) ;
#17322=AXIS2_PLACEMENT_3D ( 'NONE', #2534, #2644, #18955 ) ;
#17325=EDGE_CURVE ( 'NONE', #9479, #15726, #11889, .T. ) ;
#17333=CIRCLE ( 'NONE', #10559, 65.24900000006525147 ) ;
#17334=DIRECTION ( 'NONE',  ( 0.000000000000000000, -0.9790840876823206917, -0.2034560130526446298 ) ) ;
#17335=EDGE_LOOP ( 'NONE', ( #9482, #4446, #11360, #5716 ) ) ;
#17336=FACE_OUTER_BOUND ( 'NONE', #13450, .T. ) ;
#17337=CIRCLE ( 'NONE', #8183, 65.24900000006526568 ) ;
#17339=AXIS2_PLACEMENT_3D ( 'NONE', #20847, #15874, #1371 ) ;
#17341=LINE ( 'NONE', #19337, #5505 ) ;
#17343=CIRCLE ( 'NONE', #18702, 27.60000000002759535 ) ;
#17344=AXIS2_PLACEMENT_3D ( 'NONE', #19813, #18233, #6983 ) ;
#17345=VERTEX_POINT ( 'NONE', #6151 ) ;
#17346=CYLINDRICAL_SURFACE ( 'NONE', #16056, 72.00000000007199219 ) ;
#17348=ORIENTED_EDGE ( 'NONE', *, *, #4704, .T. ) ;
#17351=DIRECTION ( 'NONE',  ( -1.000000000000000000, 0.000000000000000000, 0.000000000000000000 ) ) ;
#17357=AXIS2_PLACEMENT_3D ( 'NONE', #16811, #2393, #5894 ) ;
#17364=AXIS2_PLACEMENT_3D ( 'NONE', #3248, #19052, #17468 ) ;
#17365=EDGE_LOOP ( 'NONE', ( #19403, #11104, #15667, #12081 ) ) ;
#17366=DIRECTION ( 'NONE',  ( -1.000000000000000000, 0.000000000000000000, 0.000000000000000000 ) ) ;
#17369=CARTESIAN_POINT ( 'NONE',  ( 9.999999999999998224, 53.26727847779604019, -48.44168704307576689 ) ) ;
#17371=AXIS2_PLACEMENT_3D ( 'NONE', #8856, #5459, #5363 ) ;
#17376=VECTOR ( 'NONE', #7792, 1000.000000000000000 ) ;
#17378=AXIS2_PLACEMENT_3D ( 'NONE', #13943, #4394, #20398 ) ;
#17382=FACE_OUTER_BOUND ( 'NONE', #13267, .T. ) ;
#17384=LINE ( 'NONE', #9010, #938 ) ;
#17391=LINE ( 'NONE', #2975, #11078 ) ;
#17392=ADVANCED_FACE ( 'NONE', ( #12165 ), #19060, .T. ) ;
#17393=ORIENTED_EDGE ( 'NONE', *, *, #12672, .F. ) ;
#17397=AXIS2_PLACEMENT_3D ( 'NONE', #12534, #7544, #18998 ) ;
#17398=EDGE_CURVE ( 'NONE', #20061, #11443, #16295, .T. ) ;
#17401=CARTESIAN_POINT ( 'NONE',  ( 85.00002539999999840, 0.000000000000000000, 4.000000000000000000 ) ) ;
#17403=VECTOR ( 'NONE', #2036, 1000.000000000000000 ) ;
#17406=LINE ( 'NONE', #4361, #728 ) ;
#17407=ADVANCED_FACE ( 'NONE', ( #2951 ), #9419, .T. ) ;
#17413=ORIENTED_EDGE ( 'NONE', *, *, #13150, .F. ) ;
#17415=ORIENTED_EDGE ( 'NONE', *, *, #9976, .F. ) ;
#17420=VERTEX_POINT ( 'NONE', #950 ) ;
#17425=CIRCLE ( 'NONE', #18090, 27.60000000002760245 ) ;
#17430=DIRECTION ( 'NONE',  ( -1.000000000000000000, 0.000000000000000000, -0.000000000000000000 ) ) ;
#17431=AXIS2_PLACEMENT_3D ( 'NONE', #6680, #13159, #5086 ) ;
#17435=CARTESIAN_POINT ( 'NONE',  ( 0.000000000000000000, 51.43306257653197378, -40.15061736769512635 ) ) ;
#17436=ORIENTED_EDGE ( 'NONE', *, *, #15445, .T. ) ;
#17437=DIRECTION ( 'NONE',  ( -1.000000000000000000, 0.000000000000000000, -0.000000000000000000 ) ) ;
#17439=ORIENTED_EDGE ( 'NONE', *, *, #17774, .F. ) ;
#17441=DIRECTION ( 'NONE',  ( -1.000000000000000000, 0.000000000000000000, 0.000000000000000000 ) ) ;
#17445=CLOSED_SHELL ( 'NONE', ( #3788, #10515, #4771, #10538, #1967, #7583, #19600, #19029, #12923, #267, #20840, #19520, #15971, #17841, #7149, #30, #2374, #16897, #2369, #20092, #7750, #1024, #15357, #431, #19946, #4942, #16863, #16438, #17593, #3326, #6387, #12687, #2796, #11577, #17799, #9316, #8059, #8459, #10143, #7675, #7562, #2427, #2221, #2878, #956, #5003, #5697, #3028, #8766, #3512, #15905, #247, #11433, #3639, #5726, #925, #3209, #8063, #10362, #16371, #20851, #20359, #15561, #7268, #3765, #9673, #15529, #4528, #16996, #1640, #4556, #9640, #5859, #9978, #5212, #7778, #4836, #1397, #6603, #15032, #7790, #18586, #15251, #11929, #3615, #14653, #6947, #18830, #14042, #18807, #10728, #1955, #14434, #11306, #6128, #5615, #20551, #19148, #20886, #3806, #2729, #20393, #17452, #8308, #7697, #15290, #5719, #16180, #3090, #20148, #5964, #6359, #3759, #3005, #15424, #20356, #11396, #17483, #7163, #12987, #6364, #2106, #1679, #4954, #9089, #13239, #7399, #1072, #16878, #12628, #11827, #18890, #17392, #10384, #12733, #6758, #13014, #15526, #9932, #1039, #17574, #17239, #6348, #18551, #4037, #12177, #5342, #20301, #20089, #7390, #13489, #7473, #1771, #1467, #11066, #1993, #17917, #5876, #14940, #14064, #6631, #18863, #20611, #4543, #2520, #15182, #19280, #13921, #4055, #17145, #1432, #15559, #5995, #4799, #6542, #15432, #5046, #8820, #1458, #9462, #10216, #7145, #19465, #9049, #6918, #917, #1662, #17407, #1231, #3829, #17124, #13508, #1464, #16621, #18736, #8159, #8562, #3287, #3750, #11109, #1552, #3163, #1053 ) ) ;
#17447=ORIENTED_EDGE ( 'NONE', *, *, #16824, .F. ) ;
#17449=EDGE_LOOP ( 'NONE', ( #20357, #18771, #19176, #16556 ) ) ;
#17452=ADVANCED_FACE ( 'NONE', ( #13868 ), #7284, .T. ) ;
#17463=ORIENTED_EDGE ( 'NONE', *, *, #8074, .F. ) ;
#17464=AXIS2_PLACEMENT_3D ( 'NONE', #10527, #4048, #11614 ) ;
#17468=DIRECTION ( 'NONE',  ( 0.000000000000000000, 0.000000000000000000, 1.000000000000000000 ) ) ;
#17472=ORIENTED_EDGE ( 'NONE', *, *, #15767, .T. ) ;
#17474=CARTESIAN_POINT ( 'NONE',  ( 19.99999999999999645, 15.58726123847851142, 62.93731870009410301 ) ) ;
#17475=EDGE_CURVE ( 'NONE', #14868, #14556, #7609, .T. ) ;
#17483=ADVANCED_FACE ( 'NONE', ( #20219 ), #4332, .T. ) ;
#17484=AXIS2_PLACEMENT_3D ( 'NONE', #12352, #4062, #10333 ) ;
#17485=AXIS2_PLACEMENT_3D ( 'NONE', #19047, #3139, #7802 ) ;
#17487=CYLINDRICAL_SURFACE ( 'NONE', #348, 7.500000000000000000 ) ;
#17488=VERTEX_POINT ( 'NONE', #1047 ) ;
#17494=DIRECTION ( 'NONE',  ( -1.000000000000000000, 0.000000000000000000, 0.000000000000000000 ) ) ;
#17498=DIRECTION ( 'NONE',  ( 0.000000000000000000, -0.7308359642781300236, 0.6825531432186476843 ) ) ;
#17500=ORIENTED_EDGE ( 'NONE', *, *, #6369, .T. ) ;
#17501=ORIENTED_EDGE ( 'NONE', *, *, #16620, .F. ) ;
#17502=DIRECTION ( 'NONE',  ( -1.000000000000000000, -0.000000000000000000, 0.000000000000000000 ) ) ;
#17503=VECTOR ( 'NONE', #7887, 1000.000000000000000 ) ;
#17506=DIRECTION ( 'NONE',  ( -1.000000000000000000, 0.000000000000000000, 0.000000000000000000 ) ) ;
#17512=AXIS2_PLACEMENT_3D ( 'NONE', #15115, #10234, #18510 ) ;
#17513=EDGE_CURVE ( 'NONE', #18559, #7632, #19676, .T. ) ;
#17516=DIRECTION ( 'NONE',  ( -1.000000000000000000, 0.000000000000000000, -0.000000000000000000 ) ) ;
#17517=VECTOR ( 'NONE', #15446, 1000.000000000000000 ) ;
#17518=VERTEX_POINT ( 'NONE', #20435 ) ;
#17519=VECTOR ( 'NONE', #12899, 1000.000000000000000 ) ;
#17521=ORIENTED_EDGE ( 'NONE', *, *, #272, .F. ) ;
#17525=ORIENTED_EDGE ( 'NONE', *, *, #1632, .T. ) ;
#17529=LINE ( 'NONE', #15918, #10181 ) ;
#17534=CARTESIAN_POINT ( 'NONE',  ( 19.99999999999999645, 0.000000000000000000, 0.000000000000000000 ) ) ;
#17536=CARTESIAN_POINT ( 'NONE',  ( 19.99999999999999645, -20.60847369613026103, 61.90898814327709943 ) ) ;
#17537=EDGE_CURVE ( 'NONE', #20260, #1747, #9199, .T. ) ;
#17538=AXIS2_PLACEMENT_3D ( 'NONE', #10944, #14235, #15714 ) ;
#17541=EDGE_CURVE ( 'NONE', #659, #16270, #8189, .T. ) ;
#17542=CARTESIAN_POINT ( 'NONE',  ( 0.000000000000000000, 0.000000000000000000, 0.000000000000000000 ) ) ;
#17547=ORIENTED_EDGE ( 'NONE', *, *, #16424, .F. ) ;
#17549=LINE ( 'NONE', #9474, #797 ) ;
#17551=ORIENTED_EDGE ( 'NONE', *, *, #9379, .T. ) ;
#17552=AXIS2_PLACEMENT_3D ( 'NONE', #8817, #18168, #18265 ) ;
#17555=CARTESIAN_POINT ( 'NONE',  ( 19.99999999999999645, 58.26603306961962403, 42.29739224042491941 ) ) ;
#17556=EDGE_LOOP ( 'NONE', ( #8814, #20147, #20802, #19988 ) ) ;
#17558=ORIENTED_EDGE ( 'NONE', *, *, #20171, .T. ) ;
#17560=ORIENTED_EDGE ( 'NONE', *, *, #17653, .T. ) ;
#17565=ORIENTED_EDGE ( 'NONE', *, *, #8702, .T. ) ;
#17567=CARTESIAN_POINT ( 'NONE',  ( 0.000000000000000000, 60.40676135667438729, 23.56039007469059143 ) ) ;
#17572=ORIENTED_EDGE ( 'NONE', *, *, #10127, .F. ) ;
#17574=ADVANCED_FACE ( 'NONE', ( #14404 ), #12818, .T. ) ;
#17584=DIRECTION ( 'NONE',  ( 0.000000000000000000, 0.000000000000000000, 1.000000000000000000 ) ) ;
#17589=DIRECTION ( 'NONE',  ( 0.000000000000000000, 0.6310879443260485333, 0.7757112907044232397 ) ) ;
#17593=ADVANCED_FACE ( 'NONE', ( #475 ), #18169, .T. ) ;
#17596=DIRECTION ( 'NONE',  ( 0.000000000000000000, 0.000000000000000000, 1.000000000000000000 ) ) ;
#17598=CARTESIAN_POINT ( 'NONE',  ( 19.99999999999999645, 0.000000000000000000, 0.000000000000000000 ) ) ;
#17600=CARTESIAN_POINT ( 'NONE',  ( 19.99999999999999645, 24.01204443665187327, 60.22865198596132785 ) ) ;
#17602=ORIENTED_EDGE ( 'NONE', *, *, #17513, .F. ) ;
#17603=ORIENTED_EDGE ( 'NONE', *, *, #13394, .F. ) ;
#17604=CARTESIAN_POINT ( 'NONE',  ( 19.99999999999999645, 27.62776854598856602, 58.65812137499012380 ) ) ;
#17605=AXIS2_PLACEMENT_3D ( 'NONE', #4932, #367, #8516 ) ;
#17606=CYLINDRICAL_SURFACE ( 'NONE', #16690, 27.60000000002759535 ) ;
#17611=DIRECTION ( 'NONE',  ( -1.000000000000000000, 0.000000000000000000, -0.000000000000000000 ) ) ;
#17612=CARTESIAN_POINT ( 'NONE',  ( 19.99999999999999645, 28.84646472442454979, 58.52617768068444093 ) ) ;
#17613=ORIENTED_EDGE ( 'NONE', *, *, #5186, .F. ) ;
#17617=LINE ( 'NONE', #9039, #836 ) ;
#17620=VERTEX_POINT ( 'NONE', #3638 ) ;
#17622=DIRECTION ( 'NONE',  ( 0.000000000000000000, 0.000000000000000000, 1.000000000000000000 ) ) ;
#17625=CARTESIAN_POINT ( 'NONE',  ( 19.99999999999999645, 0.000000000000000000, 0.000000000000000000 ) ) ;
#17627=EDGE_CURVE ( 'NONE', #14303, #12727, #4803, .T. ) ;
#17629=DIRECTION ( 'NONE',  ( 0.000000000000000000, 0.000000000000000000, 1.000000000000000000 ) ) ;
#17632=EDGE_CURVE ( 'NONE', #9751, #5132, #7162, .T. ) ;
#17644=DIRECTION ( 'NONE',  ( 0.000000000000000000, 8.881784197001252323E-16, 1.000000000000000000 ) ) ;
#17645=CARTESIAN_POINT ( 'NONE',  ( 0.000000000000000000, -38.69327817041812523, 52.53819777490620169 ) ) ;
#17646=ORIENTED_EDGE ( 'NONE', *, *, #12715, .F. ) ;
#17650=FACE_OUTER_BOUND ( 'NONE', #17024, .T. ) ;
#17651=ORIENTED_EDGE ( 'NONE', *, *, #16344, .F. ) ;
#17652=EDGE_CURVE ( 'NONE', #18871, #833, #4202, .T. ) ;
#17653=EDGE_CURVE ( 'NONE', #8626, #10526, #13535, .T. ) ;
#17654=CIRCLE ( 'NONE', #13243, 27.60000000002759890 ) ;
#17661=CARTESIAN_POINT ( 'NONE',  ( 19.99999999999999645, -15.58726123847893774, 62.93731870009398932 ) ) ;
#17663=VERTEX_POINT ( 'NONE', #17138 ) ;
#17667=CIRCLE ( 'NONE', #11553, 65.24900000006525147 ) ;
#17671=EDGE_CURVE ( 'NONE', #20728, #2251, #1029, .T. ) ;
#17676=ORIENTED_EDGE ( 'NONE', *, *, #15296, .F. ) ;
#17678=CARTESIAN_POINT ( 'NONE',  ( 0.000000000000000000, 0.000000000000000000, 0.000000000000000000 ) ) ;
#17681=VERTEX_POINT ( 'NONE', #7056 ) ;
#17685=CARTESIAN_POINT ( 'NONE',  ( 19.99999999999999645, 44.69367065308721720, -56.44887778834701919 ) ) ;
#17690=LINE ( 'NONE', #3161, #4314 ) ;
#17692=DIRECTION ( 'NONE',  ( -1.000000000000000000, -0.000000000000000000, -0.000000000000000000 ) ) ;
#17693=CIRCLE ( 'NONE', #8528, 27.60000000002760601 ) ;
#17694=CIRCLE ( 'NONE', #20026, 72.00000000007199219 ) ;
#17699=CARTESIAN_POINT ( 'NONE',  ( 9.999999999999998224, 53.26727847779537228, 48.44168704307649875 ) ) ;
#17708=ORIENTED_EDGE ( 'NONE', *, *, #1907, .F. ) ;
#17710=DIRECTION ( 'NONE',  ( 0.000000000000000000, -0.9422609221188237294, 0.3348796121709771700 ) ) ;
#17711=AXIS2_PLACEMENT_3D ( 'NONE', #14906, #19664, #18292 ) ;
#17713=EDGE_CURVE ( 'NONE', #1684, #6196, #18962, .T. ) ;
#17716=AXIS2_PLACEMENT_3D ( 'NONE', #2388, #10553, #10341 ) ;
#17718=DIRECTION ( 'NONE',  ( -1.000000000000000000, 0.000000000000000000, 0.000000000000000000 ) ) ;
#17720=DIRECTION ( 'NONE',  ( 0.000000000000000000, -0.9976687691905384847, -0.06824241336468166164 ) ) ;
#17722=EDGE_LOOP ( 'NONE', ( #2939, #8591, #402, #19245 ) ) ;
#17728=VERTEX_POINT ( 'NONE', #8859 ) ;
#17730=LINE ( 'NONE', #17933, #20440 ) ;
#17731=VERTEX_POINT ( 'NONE', #13746 ) ;
#17736=CARTESIAN_POINT ( 'NONE',  ( 19.99999999999999645, -43.56693332842751687, -48.57318520917550586 ) ) ;
#17737=DIRECTION ( 'NONE',  ( -1.000000000000000000, 0.000000000000000000, -0.000000000000000000 ) ) ;
#17739=AXIS2_PLACEMENT_3D ( 'NONE', #10376, #4104, #11852 ) ;
#17748=DIRECTION ( 'NONE',  ( 0.000000000000000000, -0.1361666490962538945, 0.9906859460363297565 ) ) ;
#17749=DIRECTION ( 'NONE',  ( -1.000000000000000000, 0.000000000000000000, -0.000000000000000000 ) ) ;
#17752=CARTESIAN_POINT ( 'NONE',  ( 19.99999999999999645, 0.000000000000000000, 0.000000000000000000 ) ) ;
#17753=DIRECTION ( 'NONE',  ( -1.000000000000000000, 0.000000000000000000, 0.000000000000000000 ) ) ;
#17755=CIRCLE ( 'NONE', #827, 27.60000000002759890 ) ;
#17758=VERTEX_POINT ( 'NONE', #20522 ) ;
#17759=DIRECTION ( 'NONE',  ( 0.000000000000000000, 0.000000000000000000, 1.000000000000000000 ) ) ;
#17761=CIRCLE ( 'NONE', #8597, 27.60000000002760245 ) ;
#17762=EDGE_CURVE ( 'NONE', #7264, #14245, #15557, .T. ) ;
#17764=DIRECTION ( 'NONE',  ( -1.000000000000000000, 0.000000000000000000, 0.000000000000000000 ) ) ;
#17770=VERTEX_POINT ( 'NONE', #10875 ) ;
#17771=CARTESIAN_POINT ( 'NONE',  ( -10.00000000000000000, 0.000000000000000000, 0.000000000000000000 ) ) ;
#17773=AXIS2_PLACEMENT_3D ( 'NONE', #16570, #19554, #11493 ) ;
#17774=EDGE_CURVE ( 'NONE', #17728, #12535, #12804, .T. ) ;
#17777=DIRECTION ( 'NONE',  ( -1.000000000000000000, -0.000000000000000000, -0.000000000000000000 ) ) ;
#17781=EDGE_CURVE ( 'NONE', #7039, #7171, #20287, .T. ) ;
#17782=ORIENTED_EDGE ( 'NONE', *, *, #18256, .T. ) ;
#17783=PRODUCT_DEFINITION ( 'UNKNOWN', '', #6270, #13665 ) ;
#17784=FACE_OUTER_BOUND ( 'NONE', #20620, .T. ) ;
#17785=CARTESIAN_POINT ( 'NONE',  ( 0.000000000000000000, 31.17893654894229982, 57.31758819669181548 ) ) ;
#17787=EDGE_LOOP ( 'NONE', ( #10765, #11171, #8052, #3677 ) ) ;
#17789=AXIS2_PLACEMENT_3D ( 'NONE', #12994, #9800, #2169 ) ;
#17796=DIRECTION ( 'NONE',  ( -1.000000000000000000, -0.000000000000000000, 0.000000000000000000 ) ) ;
#17799=ADVANCED_FACE ( 'NONE', ( #486 ), #12997, .T. ) ;
#17801=CIRCLE ( 'NONE', #6945, 27.60000000002760245 ) ;
#17803=VERTEX_POINT ( 'NONE', #8316 ) ;
#17804=CARTESIAN_POINT ( 'NONE',  ( 0.000000000000000000, 63.17103598352149874, -16.33561182745074447 ) ) ;
#17806=FACE_OUTER_BOUND ( 'NONE', #14452, .T. ) ;
#17808=CYLINDRICAL_SURFACE ( 'NONE', #8534, 72.00000000007199219 ) ;
#17813=EDGE_LOOP ( 'NONE', ( #20471, #18393 ) ) ;
#17814=DIRECTION ( 'NONE',  ( -1.000000000000000000, -0.000000000000000000, -0.000000000000000000 ) ) ;
#17830=DIRECTION ( 'NONE',  ( 0.000000000000000000, 0.000000000000000000, -1.000000000000000000 ) ) ;
#17831=CIRCLE ( 'NONE', #11719, 65.24900000006525147 ) ;
#17837=ORIENTED_EDGE ( 'NONE', *, *, #18699, .F. ) ;
#17841=ADVANCED_FACE ( 'NONE', ( #9907 ), #10121, .T. ) ;
#17855=CARTESIAN_POINT ( 'NONE',  ( 19.99999999999999645, 0.000000000000000000, 0.000000000000000000 ) ) ;
#17862=ORIENTED_EDGE ( 'NONE', *, *, #3571, .F. ) ;
#17863=CYLINDRICAL_SURFACE ( 'NONE', #11613, 27.60000000002759890 ) ;
#17867=VECTOR ( 'NONE', #15013, 1000.000000000000000 ) ;
#17873=CIRCLE ( 'NONE', #7661, 27.60000000002760245 ) ;
#17878=DIRECTION ( 'NONE',  ( -1.000000000000000000, 0.000000000000000000, -0.000000000000000000 ) ) ;
#17879=AXIS2_PLACEMENT_3D ( 'NONE', #13023, #11735, #4957 ) ;
#17881=CARTESIAN_POINT ( 'NONE',  ( 0.000000000000000000, -8.857208570070312703, 71.45313048675083678 ) ) ;
#17882=CARTESIAN_POINT ( 'NONE',  ( 0.000000000000000000, 0.000000000000000000, 0.000000000000000000 ) ) ;
#17883=VERTEX_POINT ( 'NONE', #8214 ) ;
#17884=FACE_OUTER_BOUND ( 'NONE', #12956, .T. ) ;
#17886=ORIENTED_EDGE ( 'NONE', *, *, #18415, .F. ) ;
#17888=CARTESIAN_POINT ( 'NONE',  ( 19.99999999999999645, -67.51707036274432028, 25.00890260772354878 ) ) ;
#17900=DIRECTION ( 'NONE',  ( -1.000000000000000000, -0.000000000000000000, 0.000000000000000000 ) ) ;
#17902=CYLINDRICAL_SURFACE ( 'NONE', #20391, 72.00000000007199219 ) ;
#17909=EDGE_CURVE ( 'NONE', #10293, #16773, #3702, .T. ) ;
#17910=DIRECTION ( 'NONE',  ( -1.000000000000000000, 0.000000000000000000, 0.000000000000000000 ) ) ;
#17913=CARTESIAN_POINT ( 'NONE',  ( 19.99999999999999645, 64.79224928664392280, -2.456263514197840614 ) ) ;
#17916=DIRECTION ( 'NONE',  ( 0.000000000000000000, -0.8878852184023794392, 0.4600650377311439887 ) ) ;
#17917=ADVANCED_FACE ( 'NONE', ( #6515 ), #14891, .T. ) ;
#17918=EDGE_CURVE ( 'NONE', #2235, #9794, #859, .T. ) ;
#17921=DIRECTION ( 'NONE',  ( 0.000000000000000000, 0.9976687691905394839, -0.06824241336466768670 ) ) ;
#17927=EDGE_LOOP ( 'NONE', ( #15276, #1700, #8622, #14377 ) ) ;
#17931=ORIENTED_EDGE ( 'NONE', *, *, #2742, .F. ) ;
#17933=CARTESIAN_POINT ( 'NONE',  ( 19.99999999999999645, -63.85430960833482317, 16.34407078397855528 ) ) ;
#17935=DIRECTION ( 'NONE',  ( -1.000000000000000000, -0.000000000000000000, -0.000000000000000000 ) ) ;
#17937=EDGE_LOOP ( 'NONE', ( #6982, #13545, #12162, #3375 ) ) ;
#17941=DIRECTION ( 'NONE',  ( -1.000000000000000000, -0.000000000000000000, -0.000000000000000000 ) ) ;
#17944=CYLINDRICAL_SURFACE ( 'NONE', #3235, 27.60000000002759890 ) ;
#17948=ORIENTED_EDGE ( 'NONE', *, *, #601, .T. ) ;
#17951=DIRECTION ( 'NONE',  ( 0.000000000000000000, 0.2697967711570248284, -0.9629172873477992445 ) ) ;
#17954=EDGE_LOOP ( 'NONE', ( #15643, #4965, #13369, #18087 ) ) ;
#17956=ORIENTED_EDGE ( 'NONE', *, *, #1587, .F. ) ;
#17962=CIRCLE ( 'NONE', #10867, 72.00000000007199219 ) ;
#17964=EDGE_CURVE ( 'NONE', #17979, #714, #8118, .T. ) ;
#17967=EDGE_CURVE ( 'NONE', #8219, #9551, #5730, .T. ) ;
#17971=EDGE_LOOP ( 'NONE', ( #10241, #19795, #19924, #19505 ) ) ;
#17973=AXIS2_PLACEMENT_3D ( 'NONE', #11905, #5543, #5241 ) ;
#17975=DIRECTION ( 'NONE',  ( 0.000000000000000000, -0.9422609221188166240, -0.3348796121709969320 ) ) ;
#17976=ORIENTED_EDGE ( 'NONE', *, *, #20074, .T. ) ;
#17978=AXIS2_PLACEMENT_3D ( 'NONE', #1389, #4560, #9327 ) ;
#17979=VERTEX_POINT ( 'NONE', #12348 ) ;
#17981=ORIENTED_EDGE ( 'NONE', *, *, #9228, .T. ) ;
#17987=ORIENTED_EDGE ( 'NONE', *, *, #4414, .F. ) ;
#17990=CARTESIAN_POINT ( 'NONE',  ( 19.99999999999999645, -60.35829202194859278, -24.78524934717612282 ) ) ;
#17994=ORIENTED_EDGE ( 'NONE', *, *, #12746, .T. ) ;
#18000=DIRECTION ( 'NONE',  ( -1.000000000000000000, 0.000000000000000000, 0.000000000000000000 ) ) ;
#18002=ORIENTED_EDGE ( 'NONE', *, *, #12338, .F. ) ;
#18003=CARTESIAN_POINT ( 'NONE',  ( 19.99999999999999645, 56.63599015375715595, -31.56633360682406675 ) ) ;
#18007=ORIENTED_EDGE ( 'NONE', *, *, #14519, .T. ) ;
#18008=CARTESIAN_POINT ( 'NONE',  ( 19.99999999999999645, 63.85430960833475211, 11.25592921604948948 ) ) ;
#18010=FACE_OUTER_BOUND ( 'NONE', #9526, .T. ) ;
#18011=DIRECTION ( 'NONE',  ( 0.000000000000000000, -0.6310879443260434263, -0.7757112907044274586 ) ) ;
#18014=VECTOR ( 'NONE', #11957, 1000.000000000000000 ) ;
#18021=VERTEX_POINT ( 'NONE', #20600 ) ;
#18025=CARTESIAN_POINT ( 'NONE',  ( 0.000000000000000000, 14.55863677812212131, -63.60407295269091321 ) ) ;
#18031=CARTESIAN_POINT ( 'NONE',  ( 19.99999999999999645, 63.85430960833475211, 11.25592921604948948 ) ) ;
#18035=FACE_OUTER_BOUND ( 'NONE', #2387, .T. ) ;
#18036=AXIS2_PLACEMENT_3D ( 'NONE', #20081, #7050, #7469 ) ;
#18037=CIRCLE ( 'NONE', #8886, 72.00000000007199219 ) ;
#18038=AXIS2_PLACEMENT_3D ( 'NONE', #13246, #19698, #17921 ) ;
#18040=FACE_OUTER_BOUND ( 'NONE', #19565, .T. ) ;
#18044=EDGE_CURVE ( 'NONE', #3604, #17345, #7991, .T. ) ;
#18047=DIRECTION ( 'NONE',  ( -1.000000000000000000, -0.000000000000000000, -0.000000000000000000 ) ) ;
#18054=EDGE_CURVE ( 'NONE', #4546, #10611, #7575, .T. ) ;
#18060=ORIENTED_EDGE ( 'NONE', *, *, #976, .T. ) ;
#18066=CIRCLE ( 'NONE', #3487, 27.60000000002759890 ) ;
#18067=DIRECTION ( 'NONE',  ( 0.000000000000000000, 0.000000000000000000, 1.000000000000000000 ) ) ;
#18069=VECTOR ( 'NONE', #15599, 1000.000000000000000 ) ;
#18073=CARTESIAN_POINT ( 'NONE',  ( 9.999999999999998224, 63.48283426024899256, -33.96954156735303343 ) ) ;
#18075=ORIENTED_EDGE ( 'NONE', *, *, #12046, .F. ) ;
#18076=CIRCLE ( 'NONE', #10967, 27.60000000002759890 ) ;
#18079=VERTEX_POINT ( 'NONE', #19230 ) ;
#18080=DIRECTION ( 'NONE',  ( 0.000000000000000000, -0.6310879443260434263, -0.7757112907044274586 ) ) ;
#18081=CARTESIAN_POINT ( 'NONE',  ( 19.99999999999999645, 0.000000000000000000, 0.000000000000000000 ) ) ;
#18082=CARTESIAN_POINT ( 'NONE',  ( 19.99999999999999645, 0.000000000000000000, 0.000000000000000000 ) ) ;
#18083=CIRCLE ( 'NONE', #8937, 4.000000000000000000 ) ;
#18086=DIRECTION ( 'NONE',  ( 0.000000000000000000, -0.5195839500354404450, 0.8544194045464843512 ) ) ;
#18087=ORIENTED_EDGE ( 'NONE', *, *, #7843, .T. ) ;
#18090=AXIS2_PLACEMENT_3D ( 'NONE', #12770, #19221, #11159 ) ;
#18091=ORIENTED_EDGE ( 'NONE', *, *, #16065, .F. ) ;
#18099=DIRECTION ( 'NONE',  ( 0.000000000000000000, 0.000000000000000000, 1.000000000000000000 ) ) ;
#18103=EDGE_LOOP ( 'NONE', ( #17249, #10547, #14929, #19848 ) ) ;
#18115=CARTESIAN_POINT ( 'NONE',  ( 19.99999999999999645, 60.35829202194909016, -24.78524934717487227 ) ) ;
#18116=CARTESIAN_POINT ( 'NONE',  ( 0.000000000000000000, 0.000000000000000000, 0.000000000000000000 ) ) ;
#18119=DIRECTION ( 'NONE',  ( -1.000000000000000000, 0.000000000000000000, 0.000000000000000000 ) ) ;
#18120=EDGE_CURVE ( 'NONE', #9908, #7786, #6878, .T. ) ;
#18121=CARTESIAN_POINT ( 'NONE',  ( 0.000000000000000000, -70.68211945903179583, -13.71269443944282607 ) ) ;
#18127=LINE ( 'NONE', #15154, #16774 ) ;
#18128=ORIENTED_EDGE ( 'NONE', *, *, #2503, .F. ) ;
#18129=CARTESIAN_POINT ( 'NONE',  ( 9.999999999999998224, 0.9548212943375489203, -71.99366858485714715 ) ) ;
#18134=ORIENTED_EDGE ( 'NONE', *, *, #2780, .F. ) ;
#18135=CARTESIAN_POINT ( 'NONE',  ( 0.000000000000000000, 0.000000000000000000, 0.000000000000000000 ) ) ;
#18138=ORIENTED_EDGE ( 'NONE', *, *, #7506, .F. ) ;
#18140=CARTESIAN_POINT ( 'NONE',  ( 0.000000000000000000, 0.000000000000000000, 0.000000000000000000 ) ) ;
#18141=CARTESIAN_POINT ( 'NONE',  ( 0.000000000000000000, 35.35772184876879720, 54.34979580218204376 ) ) ;
#18143=EDGE_CURVE ( 'NONE', #6196, #10244, #19419, .T. ) ;
#18148=EDGE_CURVE ( 'NONE', #10026, #13763, #471, .T. ) ;
#18149=DIRECTION ( 'NONE',  ( 1.000000000000000000, 0.000000000000000000, 0.000000000000000000 ) ) ;
#18156=ORIENTED_EDGE ( 'NONE', *, *, #14218, .F. ) ;
#18161=VERTEX_POINT ( 'NONE', #5874 ) ;
#18163=DIRECTION ( 'NONE',  ( 0.000000000000000000, -7.039457583666959814E-15, 1.000000000000000000 ) ) ;
#18168=DIRECTION ( 'NONE',  ( 1.000000000000000000, 0.000000000000000000, 0.000000000000000000 ) ) ;
#18169=CYLINDRICAL_SURFACE ( 'NONE', #5466, 72.00000000007199219 ) ;
#18179=CARTESIAN_POINT ( 'NONE',  ( 19.99999999999999645, 64.44931368725519860, 10.18420179740629727 ) ) ;
#18180=VERTEX_POINT ( 'NONE', #3413 ) ;
#18187=DIRECTION ( 'NONE',  ( -1.000000000000000000, -0.000000000000000000, -0.000000000000000000 ) ) ;
#18193=EDGE_CURVE ( 'NONE', #1859, #16021, #19440, .T. ) ;
#18195=ORIENTED_EDGE ( 'NONE', *, *, #14885, .F. ) ;
#18196=DIRECTION ( 'NONE',  ( 0.000000000000000000, -0.9422609221188166240, -0.3348796121709969320 ) ) ;
#18202=AXIS2_PLACEMENT_3D ( 'NONE', #20854, #1281, #12605 ) ;
#18203=EDGE_LOOP ( 'NONE', ( #9098, #17602 ) ) ;
#18205=DIRECTION ( 'NONE',  ( -1.000000000000000000, -0.000000000000000000, -0.000000000000000000 ) ) ;
#18208=DIRECTION ( 'NONE',  ( -1.000000000000000000, 0.000000000000000000, 0.000000000000000000 ) ) ;
#18210=EDGE_LOOP ( 'NONE', ( #12472, #11156, #15809, #4201 ) ) ;
#18216=CYLINDRICAL_SURFACE ( 'NONE', #13258, 65.24900000006525147 ) ;
#18218=EDGE_LOOP ( 'NONE', ( #18340, #1923, #9040, #8956 ) ) ;
#18219=ORIENTED_EDGE ( 'NONE', *, *, #15312, .T. ) ;
#18220=FACE_OUTER_BOUND ( 'NONE', #13733, .T. ) ;
#18221=DIRECTION ( 'NONE',  ( 0.000000000000000000, 0.000000000000000000, 1.000000000000000000 ) ) ;
#18225=CARTESIAN_POINT ( 'NONE',  ( 19.99999999999999645, 0.9548212943375593564, -71.99366858485714715 ) ) ;
#18227=EDGE_CURVE ( 'NONE', #16021, #5613, #3857, .T. ) ;
#18229=EDGE_CURVE ( 'NONE', #10611, #7712, #9784, .T. ) ;
#18231=FACE_OUTER_BOUND ( 'NONE', #13202, .T. ) ;
#18233=DIRECTION ( 'NONE',  ( -1.000000000000000000, -0.000000000000000000, 0.000000000000000000 ) ) ;
#18235=CARTESIAN_POINT ( 'NONE',  ( 19.99999999999999645, 0.000000000000000000, 0.000000000000000000 ) ) ;
#18236=ORIENTED_EDGE ( 'NONE', *, *, #11662, .F. ) ;
#18238=ORIENTED_EDGE ( 'NONE', *, *, #11250, .T. ) ;
#18243=CARTESIAN_POINT ( 'NONE',  ( 19.99999999999999645, 20.34307325858786086, 69.06634035770315450 ) ) ;
#18246=DIRECTION ( 'NONE',  ( 0.000000000000000000, 0.000000000000000000, 1.000000000000000000 ) ) ;
#18248=DIRECTION ( 'NONE',  ( 0.000000000000000000, 0.000000000000000000, 1.000000000000000000 ) ) ;
#18250=DIRECTION ( 'NONE',  ( -1.000000000000000000, 0.000000000000000000, 0.000000000000000000 ) ) ;
#18252=CARTESIAN_POINT ( 'NONE',  ( 19.99999999999999645, -36.59093685910670501, 62.00889726308018624 ) ) ;
#18253=ORIENTED_EDGE ( 'NONE', *, *, #6726, .F. ) ;
#18256=EDGE_CURVE ( 'NONE', #12996, #5196, #7592, .T. ) ;
#18258=EDGE_CURVE ( 'NONE', #12350, #7632, #8487, .T. ) ;
#18259=DIRECTION ( 'NONE',  ( 0.000000000000000000, 0.1361666490962400722, 0.9906859460363316439 ) ) ;
#18260=EDGE_LOOP ( 'NONE', ( #3364, #7388, #14442, #8010 ) ) ;
#18264=ORIENTED_EDGE ( 'NONE', *, *, #9637, .F. ) ;
#18265=DIRECTION ( 'NONE',  ( 0.000000000000000000, 0.000000000000000000, -1.000000000000000000 ) ) ;
#18268=EDGE_CURVE ( 'NONE', #16309, #2973, #6567, .T. ) ;
#18271=EDGE_LOOP ( 'NONE', ( #3488, #17026, #7615, #12574 ) ) ;
#18274=ORIENTED_EDGE ( 'NONE', *, *, #5468, .T. ) ;
#18278=DIRECTION ( 'NONE',  ( -1.000000000000000000, 0.000000000000000000, -0.000000000000000000 ) ) ;
#18282=EDGE_CURVE ( 'NONE', #9123, #15726, #10094, .T. ) ;
#18284=DIRECTION ( 'NONE',  ( -1.000000000000000000, 0.000000000000000000, 0.000000000000000000 ) ) ;
#18287=EDGE_CURVE ( 'NONE', #9780, #18021, #17761, .T. ) ;
#18288=VECTOR ( 'NONE', #11487, 1000.000000000000000 ) ;
#18289=ORIENTED_EDGE ( 'NONE', *, *, #4511, .T. ) ;
#18292=DIRECTION ( 'NONE',  ( 0.000000000000000000, 0.000000000000000000, 1.000000000000000000 ) ) ;
#18295=CIRCLE ( 'NONE', #2732, 27.60000000002759535 ) ;
#18296=CYLINDRICAL_SURFACE ( 'NONE', #17371, 65.24900000006525147 ) ;
#18298=EDGE_CURVE ( 'NONE', #11336, #14260, #13278, .T. ) ;
#18310=VERTEX_POINT ( 'NONE', #15074 ) ;
#18317=DIRECTION ( 'NONE',  ( -1.000000000000000000, -0.000000000000000000, -0.000000000000000000 ) ) ;
#18325=CIRCLE ( 'NONE', #3431, 27.60000000002759535 ) ;
#18327=CARTESIAN_POINT ( 'NONE',  ( 19.99999999999999645, 68.15657073222435258, 23.20952102120304517 ) ) ;
#18328=CARTESIAN_POINT ( 'NONE',  ( 9.999999999999998224, 63.48283426024851650, 33.96954156735390740 ) ) ;
#18331=ORIENTED_EDGE ( 'NONE', *, *, #1858, .F. ) ;
#18337=DIRECTION ( 'NONE',  ( 0.000000000000000000, 0.000000000000000000, -1.000000000000000000 ) ) ;
#18340=ORIENTED_EDGE ( 'NONE', *, *, #15985, .T. ) ;
#18342=DIRECTION ( 'NONE',  ( 0.000000000000000000, 0.000000000000000000, 1.000000000000000000 ) ) ;
#18343=EDGE_CURVE ( 'NONE', #11771, #12132, #16655, .T. ) ;
#18345=CARTESIAN_POINT ( 'NONE',  ( 19.99999999999999645, -56.63599015375651646, -31.56633360682521072 ) ) ;
#18349=AXIS2_PLACEMENT_3D ( 'NONE', #853, #1067, #9012 ) ;
#18352=CARTESIAN_POINT ( 'NONE',  ( 0.000000000000000000, 60.35829202194909016, -24.78524934717487227 ) ) ;
#18356=VERTEX_POINT ( 'NONE', #12200 ) ;
#18358=CARTESIAN_POINT ( 'NONE',  ( 19.99999999999999645, 61.72688495901586947, 19.84591825364119089 ) ) ;
#18360=VERTEX_POINT ( 'NONE', #5515 ) ;
#18361=CIRCLE ( 'NONE', #11598, 27.60000000002759890 ) ;
#18362=DIRECTION ( 'NONE',  ( -1.000000000000000000, -0.000000000000000000, 0.000000000000000000 ) ) ;
#18370=AXIS2_PLACEMENT_3D ( 'NONE', #14271, #15533, #4310 ) ;
#18376=CIRCLE ( 'NONE', #11924, 65.24900000006526568 ) ;
#18380=PRESENTATION_STYLE_ASSIGNMENT (( #13930 ) ) ;
#18382=EDGE_LOOP ( 'NONE', ( #13684, #10902, #11044, #14231 ) ) ;
#18384=ORIENTED_EDGE ( 'NONE', *, *, #8570, .F. ) ;
#18387=CARTESIAN_POINT ( 'NONE',  ( 0.000000000000000000, -51.96384592647235934, 49.83732252579597599 ) ) ;
#18388=CIRCLE ( 'NONE', #6208, 27.60000000002760245 ) ;
#18390=DIRECTION ( 'NONE',  ( -1.000000000000000000, 0.000000000000000000, -0.000000000000000000 ) ) ;
#18391=EDGE_LOOP ( 'NONE', ( #9803, #1339, #3347, #3105 ) ) ;
#18393=ORIENTED_EDGE ( 'NONE', *, *, #5026, .T. ) ;
#18396=AXIS2_PLACEMENT_3D ( 'NONE', #10635, #2781, #2576 ) ;
#18397=VERTEX_POINT ( 'NONE', #7010 ) ;
#18399=CARTESIAN_POINT ( 'NONE',  ( 0.000000000000000000, 0.000000000000000000, 0.000000000000000000 ) ) ;
#18401=AXIS2_PLACEMENT_3D ( 'NONE', #19533, #11170, #9576 ) ;
#18403=AXIS2_PLACEMENT_3D ( 'NONE', #11539, #1902, #18011 ) ;
#18405=EDGE_LOOP ( 'NONE', ( #7607, #19879, #15077, #5004 ) ) ;
#18408=DIRECTION ( 'NONE',  ( 1.000000000000000000, 0.000000000000000000, 0.000000000000000000 ) ) ;
#18413=DIRECTION ( 'NONE',  ( -1.000000000000000000, -0.000000000000000000, -0.000000000000000000 ) ) ;
#18415=EDGE_CURVE ( 'NONE', #10139, #10694, #7212, .T. ) ;
#18418=DIRECTION ( 'NONE',  ( 0.000000000000000000, 0.000000000000000000, -1.000000000000000000 ) ) ;
#18422=ORIENTED_EDGE ( 'NONE', *, *, #16366, .T. ) ;
#18425=ORIENTED_EDGE ( 'NONE', *, *, #4005, .F. ) ;
#18427=LINE ( 'NONE', #948, #2934 ) ;
#18429=CIRCLE ( 'NONE', #20456, 27.60000000002759890 ) ;
#18431=DIRECTION ( 'NONE',  ( -1.000000000000000000, 0.000000000000000000, 0.000000000000000000 ) ) ;
#18432=CARTESIAN_POINT ( 'NONE',  ( 0.000000000000000000, -58.26603306961936113, -42.29739224042532442 ) ) ;
#18440=AXIS2_PLACEMENT_3D ( 'NONE', #17661, #3236, #3131 ) ;
#18441=VERTEX_POINT ( 'NONE', #2452 ) ;
#18442=CARTESIAN_POINT ( 'NONE',  ( 19.99999999999999645, -20.34307325858833693, 69.06634035770301239 ) ) ;
#18447=VERTEX_POINT ( 'NONE', #11786 ) ;
#18448=FACE_OUTER_BOUND ( 'NONE', #18405, .T. ) ;
#18449=DIRECTION ( 'NONE',  ( 1.000000000000000000, 0.000000000000000000, 0.000000000000000000 ) ) ;
#18450=ORIENTED_EDGE ( 'NONE', *, *, #7668, .T. ) ;
#18451=ORIENTED_EDGE ( 'NONE', *, *, #16576, .T. ) ;
#18455=DIRECTION ( 'NONE',  ( 0.000000000000000000, 0.000000000000000000, 1.000000000000000000 ) ) ;
#18456=CARTESIAN_POINT ( 'NONE',  ( 0.000000000000000000, 61.72688495901586947, 19.84591825364119089 ) ) ;
#18459=DIRECTION ( 'NONE',  ( 0.000000000000000000, -0.9976687691905398170, 0.06824241336466072005 ) ) ;
#18462=ORIENTED_EDGE ( 'NONE', *, *, #11283, .F. ) ;
#18463=EDGE_CURVE ( 'NONE', #19105, #1793, #12106, .T. ) ;
#18466=ORIENTED_EDGE ( 'NONE', *, *, #799, .F. ) ;
#18471=ORIENTED_EDGE ( 'NONE', *, *, #15763, .T. ) ;
#18478=CARTESIAN_POINT ( 'NONE',  ( 0.000000000000000000, 49.77519642624007901, 42.18840861821802690 ) ) ;
#18480=DIRECTION ( 'NONE',  ( 0.000000000000000000, 0.000000000000000000, 1.000000000000000000 ) ) ;
#18482=CIRCLE ( 'NONE', #5280, 27.60000000002759890 ) ;
#18483=CARTESIAN_POINT ( 'NONE',  ( 0.000000000000000000, -11.98658579560543025, -64.13855129306480762 ) ) ;
#18486=CIRCLE ( 'NONE', #17484, 27.60000000002760245 ) ;
#18489=CYLINDRICAL_SURFACE ( 'NONE', #27, 27.60000000002760245 ) ;
#18490=ORIENTED_EDGE ( 'NONE', *, *, #15465, .F. ) ;
#18492=ORIENTED_EDGE ( 'NONE', *, *, #12467, .T. ) ;
#18495=AXIS2_PLACEMENT_3D ( 'NONE', #18031, #8276, #16237 ) ;
#18497=FACE_OUTER_BOUND ( 'NONE', #9960, .T. ) ;
#18498=VERTEX_POINT ( 'NONE', #6263 ) ;
#18499=CARTESIAN_POINT ( 'NONE',  ( 19.99999999999999645, 0.000000000000000000, 0.000000000000000000 ) ) ;
#18505=ORIENTED_EDGE ( 'NONE', *, *, #17909, .T. ) ;
#18510=DIRECTION ( 'NONE',  ( 0.000000000000000000, -0.7308359642781161458, -0.6825531432186624503 ) ) ;
#18514=VERTEX_POINT ( 'NONE', #12641 ) ;
#18515=AXIS2_PLACEMENT_3D ( 'NONE', #10891, #17366, #2728 ) ;
#18521=AXIS2_PLACEMENT_3D ( 'NONE', #16944, #14944, #2219 ) ;
#18522=CARTESIAN_POINT ( 'NONE',  ( 0.000000000000000000, 20.60847369613070867, -61.90898814327694311 ) ) ;
#18523=ORIENTED_EDGE ( 'NONE', *, *, #19316, .F. ) ;
#18527=ORIENTED_EDGE ( 'NONE', *, *, #18268, .F. ) ;
#18528=EDGE_CURVE ( 'NONE', #17518, #9946, #20354, .T. ) ;
#18533=CIRCLE ( 'NONE', #2967, 65.24900000006525147 ) ;
#18536=ORIENTED_EDGE ( 'NONE', *, *, #14459, .T. ) ;
#18537=CARTESIAN_POINT ( 'NONE',  ( 19.99999999999999645, 64.80702306891106446, -7.581672767545749814 ) ) ;
#18539=AXIS2_PLACEMENT_3D ( 'NONE', #12557, #11173, #3017 ) ;
#18540=CARTESIAN_POINT ( 'NONE',  ( 0.000000000000000000, 29.55812890831981932, 65.65300461859698089 ) ) ;
#18542=EDGE_CURVE ( 'NONE', #18441, #7455, #12501, .T. ) ;
#18545=FACE_OUTER_BOUND ( 'NONE', #11285, .T. ) ;
#18549=AXIS2_PLACEMENT_3D ( 'NONE', #18116, #5071, #12659 ) ;
#18550=CARTESIAN_POINT ( 'NONE',  ( 19.99999999999999645, 19.38316218894295417, -61.87375713200968619 ) ) ;
#18551=ADVANCED_FACE ( 'NONE', ( #1403 ), #15805, .T. ) ;
#18558=DIRECTION ( 'NONE',  ( -1.000000000000000000, -0.000000000000000000, -0.000000000000000000 ) ) ;
#18559=VERTEX_POINT ( 'NONE', #10827 ) ;
#18560=CARTESIAN_POINT ( 'NONE',  ( 0.000000000000000000, 39.37110852956887186, -51.51683813304829584 ) ) ;
#18565=DIRECTION ( 'NONE',  ( 0.000000000000000000, -0.9976687691905398170, 0.06824241336466078944 ) ) ;
#18571=EDGE_CURVE ( 'NONE', #12561, #1182, #20782, .T. ) ;
#18572=CARTESIAN_POINT ( 'NONE',  ( 150.0000507999999968, 3.872983346207417021, -1.000000000000000000 ) ) ;
#18577=CARTESIAN_POINT ( 'NONE',  ( 0.000000000000000000, 63.17103598352126426, 16.33561182745161844 ) ) ;
#18581=ORIENTED_EDGE ( 'NONE', *, *, #12903, .F. ) ;
#18582=CARTESIAN_POINT ( 'NONE',  ( 0.000000000000000000, 71.89099403602354244, -3.960426305689042970 ) ) ;
#18584=DIRECTION ( 'NONE',  ( -1.000000000000000000, 0.000000000000000000, 0.000000000000000000 ) ) ;
#18586=ADVANCED_FACE ( 'NONE', ( #2876 ), #11036, .T. ) ;
#18587=VERTEX_POINT ( 'NONE', #11141 ) ;
#18588=LINE ( 'NONE', #4271, #11365 ) ;
#18589=CARTESIAN_POINT ( 'NONE',  ( 0.000000000000000000, 46.01927912072591198, -45.67597560296339765 ) ) ;
#18596=DIRECTION ( 'NONE',  ( 0.000000000000000000, 0.8878852184023731109, 0.4600650377311559791 ) ) ;
#18597=VERTEX_POINT ( 'NONE', #9032 ) ;
#18603=ORIENTED_EDGE ( 'NONE', *, *, #3533, .F. ) ;
#18607=EDGE_LOOP ( 'NONE', ( #15484, #13650, #6695, #19146 ) ) ;
#18611=EDGE_CURVE ( 'NONE', #18597, #3682, #8007, .T. ) ;
#18616=DIRECTION ( 'NONE',  ( -1.000000000000000000, 0.000000000000000000, 0.000000000000000000 ) ) ;
#18618=DIRECTION ( 'NONE',  ( 0.000000000000000000, -0.3984010898462485573, 0.9172113015054500496 ) ) ;
#18620=DIRECTION ( 'NONE',  ( 0.000000000000000000, -0.2697967711570313232, 0.9629172873477972461 ) ) ;
#18621=VERTEX_POINT ( 'NONE', #13906 ) ;
#18626=ORIENTED_EDGE ( 'NONE', *, *, #8396, .T. ) ;
#18631=CARTESIAN_POINT ( 'NONE',  ( 0.000000000000000000, 62.46228066917787203, 18.86519267363478036 ) ) ;
#18632=CARTESIAN_POINT ( 'NONE',  ( 19.99999999999999645, -51.81019761368295207, -38.98425606966110735 ) ) ;
#18636=CARTESIAN_POINT ( 'NONE',  ( 19.99999999999999645, -0.9548212943370493200, 71.99366858485714715 ) ) ;
#18637=DIRECTION ( 'NONE',  ( 0.000000000000000000, 0.000000000000000000, -1.000000000000000000 ) ) ;
#18638=DIRECTION ( 'NONE',  ( 0.000000000000000000, 0.000000000000000000, -1.000000000000000000 ) ) ;
#18640=CIRCLE ( 'NONE', #19318, 65.24900000006526568 ) ;
#18653=VERTEX_POINT ( 'NONE', #16225 ) ;
#18654=DIRECTION ( 'NONE',  ( -1.000000000000000000, 0.000000000000000000, -0.000000000000000000 ) ) ;
#18661=LINE ( 'NONE', #10502, #7895 ) ;
#18662=LINE ( 'NONE', #9026, #7230 ) ;
#18669=DIRECTION ( 'NONE',  ( 0.000000000000000000, 0.000000000000000000, 1.000000000000000000 ) ) ;
#18674=ORIENTED_EDGE ( 'NONE', *, *, #10901, .F. ) ;
#18678=EDGE_CURVE ( 'NONE', #11750, #6239, #15881, .T. ) ;
#18679=AXIS2_PLACEMENT_3D ( 'NONE', #15491, #4252, #5724 ) ;
#18680=ORIENTED_EDGE ( 'NONE', *, *, #18825, .T. ) ;
#18681=CARTESIAN_POINT ( 'NONE',  ( -10.00000000000000000, 0.000000000000000000, 0.000000000000000000 ) ) ;
#18684=CYLINDRICAL_SURFACE ( 'NONE', #19875, 65.24900000006525147 ) ;
#18689=AXIS2_PLACEMENT_3D ( 'NONE', #2551, #14000, #12512 ) ;
#18694=EDGE_CURVE ( 'NONE', #7455, #9587, #2544, .T. ) ;
#18698=DIRECTION ( 'NONE',  ( 0.000000000000000000, 0.3984010898462424510, -0.9172113015054526031 ) ) ;
#18699=EDGE_CURVE ( 'NONE', #6196, #12585, #13154, .T. ) ;
#18702=AXIS2_PLACEMENT_3D ( 'NONE', #12820, #12911, #15772 ) ;
#18704=VECTOR ( 'NONE', #5393, 1000.000000000000000 ) ;
#18705=ORIENTED_EDGE ( 'NONE', *, *, #175, .T. ) ;
#18708=CIRCLE ( 'NONE', #5833, 27.60000000002759890 ) ;
#18711=ORIENTED_EDGE ( 'NONE', *, *, #19521, .F. ) ;
#18712=LINE ( 'NONE', #2606, #5850 ) ;
#18713=ORIENTED_EDGE ( 'NONE', *, *, #5690, .T. ) ;
#18718=CIRCLE ( 'NONE', #19373, 65.24900000006525147 ) ;
#18726=ORIENTED_EDGE ( 'NONE', *, *, #2227, .T. ) ;
#18732=CARTESIAN_POINT ( 'NONE',  ( 85.00002539999999840, 5.400000000000000355, 1.000000000000000000 ) ) ;
#18733=AXIS2_PLACEMENT_3D ( 'NONE', #2925, #5235, #6505 ) ;
#18735=ORIENTED_EDGE ( 'NONE', *, *, #18229, .F. ) ;
#18736=ADVANCED_FACE ( 'NONE', ( #7966 ), #14540, .T. ) ;
#18737=FACE_OUTER_BOUND ( 'NONE', #17335, .T. ) ;
#18742=ORIENTED_EDGE ( 'NONE', *, *, #20724, .T. ) ;
#18746=CIRCLE ( 'NONE', #18401, 27.60000000002760245 ) ;
#18757=AXIS2_PLACEMENT_3D ( 'NONE', #9041, #9142, #5851 ) ;
#18760=FACE_OUTER_BOUND ( 'NONE', #16357, .T. ) ;
#18771=ORIENTED_EDGE ( 'NONE', *, *, #3259, .T. ) ;
#18776=VERTEX_POINT ( 'NONE', #6367 ) ;
#18777=DIRECTION ( 'NONE',  ( 0.000000000000000000, 0.000000000000000000, -1.000000000000000000 ) ) ;
#18779=CARTESIAN_POINT ( 'NONE',  ( 19.99999999999999645, 0.000000000000000000, 0.000000000000000000 ) ) ;
#18784=CARTESIAN_POINT ( 'NONE',  ( 9.999999999999998224, -44.69367065308685483, 56.44887778834731051 ) ) ;
#18787=DIRECTION ( 'NONE',  ( 0.000000000000000000, 0.000000000000000000, 1.000000000000000000 ) ) ;
#18788=ORIENTED_EDGE ( 'NONE', *, *, #6257, .F. ) ;
#18793=CARTESIAN_POINT ( 'NONE',  ( 19.99999999999999645, -67.51707036274396501, -25.00890260772446894 ) ) ;
#18794=ORIENTED_EDGE ( 'NONE', *, *, #5630, .F. ) ;
#18796=DIRECTION ( 'NONE',  ( 0.000000000000000000, 0.000000000000000000, 1.000000000000000000 ) ) ;
#18804=CARTESIAN_POINT ( 'NONE',  ( 19.99999999999999645, 62.46228066917814203, -18.86519267363391350 ) ) ;
#18805=DIRECTION ( 'NONE',  ( -1.000000000000000000, 0.000000000000000000, 0.000000000000000000 ) ) ;
#18807=ADVANCED_FACE ( 'NONE', ( #2191 ), #13223, .T. ) ;
#18808=ORIENTED_EDGE ( 'NONE', *, *, #10506, .T. ) ;
#18809=CARTESIAN_POINT ( 'NONE',  ( -65.00002539999999840, 0.000000000000000000, 0.000000000000000000 ) ) ;
#18810=DIRECTION ( 'NONE',  ( 0.000000000000000000, 0.000000000000000000, 1.000000000000000000 ) ) ;
#18814=AXIS2_PLACEMENT_3D ( 'NONE', #16045, #6285, #15728 ) ;
#18817=CARTESIAN_POINT ( 'NONE',  ( 0.000000000000000000, 24.01204443665271882, -60.22865198596099390 ) ) ;
#18818=DIRECTION ( 'NONE',  ( 0.000000000000000000, -0.2697967711570314897, 0.9629172873477973571 ) ) ;
#18820=EDGE_CURVE ( 'NONE', #17488, #12110, #242, .T. ) ;
#18825=EDGE_CURVE ( 'NONE', #19645, #7455, #3795, .T. ) ;
#18826=VECTOR ( 'NONE', #6629, 1000.000000000000000 ) ;
#18830=ADVANCED_FACE ( 'NONE', ( #19911 ), #5491, .T. ) ;
#18834=VERTEX_POINT ( 'NONE', #12080 ) ;
#18839=AXIS2_PLACEMENT_3D ( 'NONE', #126, #13268, #10086 ) ;
#18840=CARTESIAN_POINT ( 'NONE',  ( 19.99999999999999645, 65.23577793412344761, 1.313498510941937036 ) ) ;
#18842=EDGE_CURVE ( 'NONE', #13708, #9945, #8361, .T. ) ;
#18843=AXIS2_PLACEMENT_3D ( 'NONE', #5136, #13002, #64 ) ;
#18844=ORIENTED_EDGE ( 'NONE', *, *, #8845, .T. ) ;
#18846=DIRECTION ( 'NONE',  ( -1.000000000000000000, -0.000000000000000000, 0.000000000000000000 ) ) ;
#18851=EDGE_CURVE ( 'NONE', #18161, #14303, #20891, .T. ) ;
#18852=AXIS2_PLACEMENT_3D ( 'NONE', #666, #13706, #7117 ) ;
#18855=AXIS2_PLACEMENT_3D ( 'NONE', #20221, #16934, #10584 ) ;
#18863=ADVANCED_FACE ( 'NONE', ( #10277 ), #634, .T. ) ;
#18866=ORIENTED_EDGE ( 'NONE', *, *, #2902, .F. ) ;
#18869=AXIS2_PLACEMENT_3D ( 'NONE', #1064, #9116, #15570 ) ;
#18871=VERTEX_POINT ( 'NONE', #13782 ) ;
#18876=ORIENTED_EDGE ( 'NONE', *, *, #20717, .F. ) ;
#18881=CARTESIAN_POINT ( 'NONE',  ( 19.99999999999999645, 0.000000000000000000, 0.000000000000000000 ) ) ;
#18882=CIRCLE ( 'NONE', #598, 72.00000000007199219 ) ;
#18883=ORIENTED_EDGE ( 'NONE', *, *, #14170, .T. ) ;
#18884=ORIENTED_EDGE ( 'NONE', *, *, #16401, .T. ) ;
#18885=FACE_OUTER_BOUND ( 'NONE', #17927, .T. ) ;
#18890=ADVANCED_FACE ( 'NONE', ( #20006 ), #3593, .T. ) ;
#18893=AXIS2_PLACEMENT_3D ( 'NONE', #6642, #10246, #18099 ) ;
#18895=DIRECTION ( 'NONE',  ( -1.000000000000000000, 0.000000000000000000, -0.000000000000000000 ) ) ;
#18897=LINE ( 'NONE', #14125, #15099 ) ;
#18898=EDGE_LOOP ( 'NONE', ( #2174, #18505, #11977, #10424 ) ) ;
#18900=VERTEX_POINT ( 'NONE', #18327 ) ;
#18904=FACE_OUTER_BOUND ( 'NONE', #5888, .T. ) ;
#18905=ORIENTED_EDGE ( 'NONE', *, *, #20348, .T. ) ;
#18909=ORIENTED_EDGE ( 'NONE', *, *, #19855, .F. ) ;
#18911=CARTESIAN_POINT ( 'NONE',  ( 19.99999999999999645, -39.37110852956777762, -51.51683813304910586 ) ) ;
#18916=DIRECTION ( 'NONE',  ( -1.000000000000000000, 0.000000000000000000, 0.000000000000000000 ) ) ;
#18917=DIRECTION ( 'NONE',  ( 0.000000000000000000, 0.000000000000000000, 1.000000000000000000 ) ) ;
#18920=CARTESIAN_POINT ( 'NONE',  ( 0.000000000000000000, 15.58726123847851142, 62.93731870009410301 ) ) ;
#18921=CYLINDRICAL_SURFACE ( 'NONE', #12658, 65.24900000006525147 ) ;
#18922=EDGE_CURVE ( 'NONE', #4998, #9154, #13794, .T. ) ;
#18923=ORIENTED_EDGE ( 'NONE', *, *, #12269, .F. ) ;
#18927=ORIENTED_EDGE ( 'NONE', *, *, #18282, .T. ) ;
#18928=CARTESIAN_POINT ( 'NONE',  ( 19.99999999999999645, 0.000000000000000000, 0.000000000000000000 ) ) ;
#18930=CARTESIAN_POINT ( 'NONE',  ( 19.99999999999999645, -56.63599015375694989, 31.56633360682443268 ) ) ;
#18937=DIRECTION ( 'NONE',  ( -1.000000000000000000, 0.000000000000000000, 0.000000000000000000 ) ) ;
#18938=ORIENTED_EDGE ( 'NONE', *, *, #1555, .T. ) ;
#18944=CARTESIAN_POINT ( 'NONE',  ( 9.999999999999998224, 68.15657073222436679, 23.20952102120305227 ) ) ;
#18947=CARTESIAN_POINT ( 'NONE',  ( 19.99999999999999645, 62.46228066917814203, -18.86519267363391350 ) ) ;
#18949=VERTEX_POINT ( 'NONE', #8778 ) ;
#18953=ORIENTED_EDGE ( 'NONE', *, *, #2597, .F. ) ;
#18954=LINE ( 'NONE', #4640, #11420 ) ;
#18955=DIRECTION ( 'NONE',  ( 0.000000000000000000, 0.000000000000000000, 1.000000000000000000 ) ) ;
#18957=DIRECTION ( 'NONE',  ( 0.000000000000000000, 0.000000000000000000, -1.000000000000000000 ) ) ;
#18959=EDGE_CURVE ( 'NONE', #15567, #9945, #15248, .T. ) ;
#18962=CIRCLE ( 'NONE', #10144, 65.24900000006525147 ) ;
#18973=DIRECTION ( 'NONE',  ( -1.000000000000000000, 0.000000000000000000, -0.000000000000000000 ) ) ;
#18974=ORIENTED_EDGE ( 'NONE', *, *, #17398, .T. ) ;
#18978=CYLINDRICAL_SURFACE ( 'NONE', #9382, 27.60000000002759535 ) ;
#18983=AXIS2_PLACEMENT_3D ( 'NONE', #8799, #20252, #20353 ) ;
#18984=CARTESIAN_POINT ( 'NONE',  ( 19.99999999999999645, -6.872116855663586321, 64.47358224882414390 ) ) ;
#18997=ORIENTED_EDGE ( 'NONE', *, *, #15200, .T. ) ;
#18998=DIRECTION ( 'NONE',  ( 0.000000000000000000, 0.000000000000000000, 1.000000000000000000 ) ) ;
#19001=CARTESIAN_POINT ( 'NONE',  ( 0.000000000000000000, -43.56693332842820610, 48.57318520917490190 ) ) ;
#19006=DIRECTION ( 'NONE',  ( 0.000000000000000000, 0.000000000000000000, 1.000000000000000000 ) ) ;
#19009=VECTOR ( 'NONE', #7058, 1000.000000000000000 ) ;
#19010=CARTESIAN_POINT ( 'NONE',  ( 0.000000000000000000, -61.72688495901628869, 19.84591825363989415 ) ) ;
#19014=CARTESIAN_POINT ( 'NONE',  ( 19.99999999999999645, 0.000000000000000000, 0.000000000000000000 ) ) ;
#19015=EDGE_LOOP ( 'NONE', ( #19767, #20679, #4664, #17976 ) ) ;
#19016=AXIS2_PLACEMENT_3D ( 'NONE', #18632, #8990, #4426 ) ;
#19018=DIRECTION ( 'NONE',  ( 0.000000000000000000, 0.2697967711570248284, -0.9629172873477992445 ) ) ;
#19022=CARTESIAN_POINT ( 'NONE',  ( 0.000000000000000000, 36.54710069451126486, -54.05313526368077248 ) ) ;
#19025=ORIENTED_EDGE ( 'NONE', *, *, #3610, .F. ) ;
#19026=CARTESIAN_POINT ( 'NONE',  ( 0.000000000000000000, 18.50424539729845108, 69.58155576219121485 ) ) ;
#19027=ORIENTED_EDGE ( 'NONE', *, *, #14431, .F. ) ;
#19029=ADVANCED_FACE ( 'NONE', ( #10810 ), #963, .F. ) ;
#19037=CIRCLE ( 'NONE', #75, 27.60000000002759890 ) ;
#19041=DIRECTION ( 'NONE',  ( -1.000000000000000000, 0.000000000000000000, 0.000000000000000000 ) ) ;
#19042=AXIS2_PLACEMENT_3D ( 'NONE', #9646, #6657, #4758 ) ;
#19043=EDGE_LOOP ( 'NONE', ( #98, #5066, #10224, #4620 ) ) ;
#19046=DIRECTION ( 'NONE',  ( 0.000000000000000000, 0.3984010898462361228, 0.9172113015054554896 ) ) ;
#19047=CARTESIAN_POINT ( 'NONE',  ( -10.00000000000000000, 0.000000000000000000, 0.000000000000000000 ) ) ;
#19052=DIRECTION ( 'NONE',  ( -1.000000000000000000, -0.000000000000000000, -0.000000000000000000 ) ) ;
#19053=AXIS2_PLACEMENT_3D ( 'NONE', #7686, #2809, #20816 ) ;
#19058=DIRECTION ( 'NONE',  ( 0.000000000000000000, 0.3984010898462361228, 0.9172113015054552676 ) ) ;
#19060=CYLINDRICAL_SURFACE ( 'NONE', #16975, 27.60000000002760245 ) ;
#19072=AXIS2_PLACEMENT_3D ( 'NONE', #18681, #11048, #9352 ) ;
#19075=ORIENTED_EDGE ( 'NONE', *, *, #13385, .F. ) ;
#19076=DIRECTION ( 'NONE',  ( 1.000000000000000000, 0.000000000000000000, -0.000000000000000000 ) ) ;
#19077=CARTESIAN_POINT ( 'NONE',  ( 0.000000000000000000, -42.42902769288503606, -49.02903636734241388 ) ) ;
#19078=DIRECTION ( 'NONE',  ( -1.000000000000000000, 0.000000000000000000, -0.000000000000000000 ) ) ;
#19080=VERTEX_POINT ( 'NONE', #9608 ) ;
#19082=CARTESIAN_POINT ( 'NONE',  ( 19.99999999999999645, 0.000000000000000000, 0.000000000000000000 ) ) ;
#19087=ORIENTED_EDGE ( 'NONE', *, *, #15835, .T. ) ;
#19090=CIRCLE ( 'NONE', #16710, 27.60000000002759890 ) ;
#19092=EDGE_CURVE ( 'NONE', #10684, #6520, #20936, .T. ) ;
#19094=DIRECTION ( 'NONE',  ( -1.000000000000000000, 0.000000000000000000, 0.000000000000000000 ) ) ;
#19095=EDGE_CURVE ( 'NONE', #15450, #17187, #1670, .T. ) ;
#19098=CIRCLE ( 'NONE', #9937, 27.60000000002759535 ) ;
#19101=CARTESIAN_POINT ( 'NONE',  ( 19.99999999999999645, 8.857208570070797649, -71.45313048675075152 ) ) ;
#19102=CARTESIAN_POINT ( 'NONE',  ( 0.000000000000000000, -51.81019761368295207, -38.98425606966110735 ) ) ;
#19105=VERTEX_POINT ( 'NONE', #5926 ) ;
#19109=DIRECTION ( 'NONE',  ( -1.000000000000000000, 0.000000000000000000, 0.000000000000000000 ) ) ;
#19110=VERTEX_POINT ( 'NONE', #14589 ) ;
#19111=EDGE_CURVE ( 'NONE', #10293, #19589, #63, .T. ) ;
#19116=DIRECTION ( 'NONE',  ( -1.000000000000000000, 0.000000000000000000, -0.000000000000000000 ) ) ;
#19121=CYLINDRICAL_SURFACE ( 'NONE', #5205, 27.60000000002759890 ) ;
#19122=CIRCLE ( 'NONE', #6247, 72.00000000007199219 ) ;
#19124=ORIENTED_EDGE ( 'NONE', *, *, #16401, .F. ) ;
#19134=CYLINDRICAL_SURFACE ( 'NONE', #11427, 4.000000000000000000 ) ;
#19136=ORIENTED_EDGE ( 'NONE', *, *, #12968, .F. ) ;
#19140=LINE ( 'NONE', #15628, #1437 ) ;
#19141=ORIENTED_EDGE ( 'NONE', *, *, #13374, .T. ) ;
#19143=DIRECTION ( 'NONE',  ( -1.000000000000000000, 0.000000000000000000, -0.000000000000000000 ) ) ;
#19146=ORIENTED_EDGE ( 'NONE', *, *, #19438, .T. ) ;
#19148=ADVANCED_FACE ( 'NONE', ( #10019 ), #8631, .T. ) ;
#19150=ORIENTED_EDGE ( 'NONE', *, *, #12460, .F. ) ;
#19153=CARTESIAN_POINT ( 'NONE',  ( -65.00002539999999840, 0.000000000000000000, 0.000000000000000000 ) ) ;
#19155=VECTOR ( 'NONE', #9048, 1000.000000000000000 ) ;
#19162=ORIENTED_EDGE ( 'NONE', *, *, #20769, .T. ) ;
#19163=DIRECTION ( 'NONE',  ( 0.000000000000000000, 0.5195839500354288987, 0.8544194045464914566 ) ) ;
#19164=CYLINDRICAL_SURFACE ( 'NONE', #1117, 27.60000000002759535 ) ;
#19167=AXIS2_PLACEMENT_3D ( 'NONE', #6582, #24, #9972 ) ;
#19170=DIRECTION ( 'NONE',  ( -1.000000000000000000, 0.000000000000000000, -0.000000000000000000 ) ) ;
#19174=DIRECTION ( 'NONE',  ( 0.000000000000000000, 0.000000000000000000, 1.000000000000000000 ) ) ;
#19175=EDGE_CURVE ( 'NONE', #18021, #8383, #18882, .T. ) ;
#19176=ORIENTED_EDGE ( 'NONE', *, *, #20743, .T. ) ;
#19179=CIRCLE ( 'NONE', #12062, 27.60000000002760245 ) ;
#19184=AXIS2_PLACEMENT_3D ( 'NONE', #4878, #11536, #13148 ) ;
#19186=DIRECTION ( 'NONE',  ( -1.000000000000000000, 0.000000000000000000, 0.000000000000000000 ) ) ;
#19191=EDGE_LOOP ( 'NONE', ( #1151, #5933, #7754, #2928 ) ) ;
#19194=CARTESIAN_POINT ( 'NONE',  ( 0.000000000000000000, 70.68211945903188109, 13.71269443944231980 ) ) ;
#19199=AXIS2_PLACEMENT_3D ( 'NONE', #6221, #20637, #19163 ) ;
#19203=EDGE_CURVE ( 'NONE', #15210, #5576, #2177, .T. ) ;
#19206=PLANE ( 'NONE',  #16650 ) ;
#19208=VERTEX_POINT ( 'NONE', #17881 ) ;
#19212=DIRECTION ( 'NONE',  ( 0.000000000000000000, 0.000000000000000000, 1.000000000000000000 ) ) ;
#19213=ORIENTED_EDGE ( 'NONE', *, *, #17398, .F. ) ;
#19216=EDGE_CURVE ( 'NONE', #5326, #6733, #16452, .T. ) ;
#19217=ORIENTED_EDGE ( 'NONE', *, *, #7803, .F. ) ;
#19218=CARTESIAN_POINT ( 'NONE',  ( 19.99999999999999645, -3.141410481201533322, 65.17333458706184501 ) ) ;
#19221=DIRECTION ( 'NONE',  ( 1.000000000000000000, 0.000000000000000000, 0.000000000000000000 ) ) ;
#19224=EDGE_CURVE ( 'NONE', #5705, #13762, #5348, .T. ) ;
#19226=EDGE_CURVE ( 'NONE', #3060, #5677, #13751, .T. ) ;
#19227=DIRECTION ( 'NONE',  ( -1.000000000000000000, 0.000000000000000000, 0.000000000000000000 ) ) ;
#19228=DIRECTION ( 'NONE',  ( 0.000000000000000000, 0.000000000000000000, 1.000000000000000000 ) ) ;
#19229=ORIENTED_EDGE ( 'NONE', *, *, #14716, .F. ) ;
#19230=CARTESIAN_POINT ( 'NONE',  ( 19.99999999999999645, -62.46228066917801414, 18.86519267363435048 ) ) ;
#19231=DIRECTION ( 'NONE',  ( 0.000000000000000000, 0.000000000000000000, 1.000000000000000000 ) ) ;
#19235=DIRECTION ( 'NONE',  ( -1.000000000000000000, 0.000000000000000000, 0.000000000000000000 ) ) ;
#19237=ORIENTED_EDGE ( 'NONE', *, *, #3492, .F. ) ;
#19238=DIRECTION ( 'NONE',  ( -1.000000000000000000, 0.000000000000000000, 0.000000000000000000 ) ) ;
#19245=ORIENTED_EDGE ( 'NONE', *, *, #5186, .T. ) ;
#19251=FACE_OUTER_BOUND ( 'NONE', #9492, .T. ) ;
#19254=CARTESIAN_POINT ( 'NONE',  ( 0.000000000000000000, 0.000000000000000000, 0.000000000000000000 ) ) ;
#19256=ORIENTED_EDGE ( 'NONE', *, *, #19226, .T. ) ;
#19260=EDGE_CURVE ( 'NONE', #10658, #1607, #8652, .T. ) ;
#19268=DIRECTION ( 'NONE',  ( -1.000000000000000000, 0.000000000000000000, 0.000000000000000000 ) ) ;
#19271=ORIENTED_EDGE ( 'NONE', *, *, #5565, .F. ) ;
#19272=DIRECTION ( 'NONE',  ( -1.000000000000000000, -0.000000000000000000, -0.000000000000000000 ) ) ;
#19276=DIRECTION ( 'NONE',  ( -1.000000000000000000, 0.000000000000000000, 0.000000000000000000 ) ) ;
#19278=CYLINDRICAL_SURFACE ( 'NONE', #4102, 27.60000000002759890 ) ;
#19279=DIRECTION ( 'NONE',  ( 0.000000000000000000, 0.000000000000000000, -1.000000000000000000 ) ) ;
#19280=ADVANCED_FACE ( 'NONE', ( #16578 ), #3546, .T. ) ;
#19283=LINE ( 'NONE', #11025, #220 ) ;
#19291=CARTESIAN_POINT ( 'NONE',  ( 19.99999999999999645, 31.98952867950403345, -56.39803944231551469 ) ) ;
#19295=ORIENTED_EDGE ( 'NONE', *, *, #20901, .F. ) ;
#19296=AXIS2_PLACEMENT_3D ( 'NONE', #3817, #16761, #14760 ) ;
#19298=DIRECTION ( 'NONE',  ( -1.000000000000000000, 0.000000000000000000, -0.000000000000000000 ) ) ;
#19300=CARTESIAN_POINT ( 'NONE',  ( 0.000000000000000000, -60.35829202194891252, 24.78524934717529504 ) ) ;
#19304=ORIENTED_EDGE ( 'NONE', *, *, #7144, .T. ) ;
#19307=DIRECTION ( 'NONE',  ( -1.000000000000000000, 0.000000000000000000, 0.000000000000000000 ) ) ;
#19313=CARTESIAN_POINT ( 'NONE',  ( 19.99999999999999645, 0.000000000000000000, 0.000000000000000000 ) ) ;
#19315=DIRECTION ( 'NONE',  ( -1.000000000000000000, 0.000000000000000000, 0.000000000000000000 ) ) ;
#19316=EDGE_CURVE ( 'NONE', #8735, #10739, #7313, .T. ) ;
#19318=AXIS2_PLACEMENT_3D ( 'NONE', #11695, #12983, #147 ) ;
#19320=DIRECTION ( 'NONE',  ( 1.000000000000000000, -0.000000000000000000, 0.000000000000000000 ) ) ;
#19322=VERTEX_POINT ( 'NONE', #5441 ) ;
#19323=DIRECTION ( 'NONE',  ( -1.000000000000000000, 0.000000000000000000, 0.000000000000000000 ) ) ;
#19324=CARTESIAN_POINT ( 'NONE',  ( -10.00000000000000000, 0.000000000000000000, 0.000000000000000000 ) ) ;
#19326=VERTEX_POINT ( 'NONE', #12026 ) ;
#19331=ORIENTED_EDGE ( 'NONE', *, *, #20717, .T. ) ;
#19333=AXIS2_PLACEMENT_3D ( 'NONE', #9607, #16272, #16074 ) ;
#19335=CARTESIAN_POINT ( 'NONE',  ( 19.99999999999999645, 0.000000000000000000, 0.000000000000000000 ) ) ;
#19337=CARTESIAN_POINT ( 'NONE',  ( 19.99999999999999645, 60.35829202194909016, -24.78524934717487227 ) ) ;
#19340=ORIENTED_EDGE ( 'NONE', *, *, #6120, .T. ) ;
#19341=CARTESIAN_POINT ( 'NONE',  ( 19.99999999999999645, -39.37110852956848817, 51.51683813304857296 ) ) ;
#19343=CARTESIAN_POINT ( 'NONE',  ( 19.99999999999999645, -42.42902769288568976, 49.02903636734183124 ) ) ;
#19348=FACE_OUTER_BOUND ( 'NONE', #11311, .T. ) ;
#19349=AXIS2_PLACEMENT_3D ( 'NONE', #13862, #10887, #20309 ) ;
#19352=ORIENTED_EDGE ( 'NONE', *, *, #18287, .F. ) ;
#19355=ORIENTED_EDGE ( 'NONE', *, *, #17127, .T. ) ;
#19360=ORIENTED_EDGE ( 'NONE', *, *, #7843, .F. ) ;
#19361=CYLINDRICAL_SURFACE ( 'NONE', #10388, 27.60000000002759890 ) ;
#19366=VERTEX_POINT ( 'NONE', #5661 ) ;
#19367=FACE_BOUND ( 'NONE', #15896, .T. ) ;
#19368=DIRECTION ( 'NONE',  ( 0.000000000000000000, -1.000000000000000000, 0.000000000000000000 ) ) ;
#19370=EDGE_CURVE ( 'NONE', #8470, #1628, #18486, .T. ) ;
#19373=AXIS2_PLACEMENT_3D ( 'NONE', #7138, #19584, #3464 ) ;
#19375=CYLINDRICAL_SURFACE ( 'NONE', #17018, 27.60000000002760245 ) ;
#19376=LINE ( 'NONE', #8349, #8342 ) ;
#19378=AXIS2_PLACEMENT_3D ( 'NONE', #3678, #10363, #8449 ) ;
#19379=VERTEX_POINT ( 'NONE', #2281 ) ;
#19380=CARTESIAN_POINT ( 'NONE',  ( 19.99999999999999645, 5.762283366691162811, 64.99406197038673838 ) ) ;
#19385=AXIS2_PLACEMENT_3D ( 'NONE', #16594, #2398, #10140 ) ;
#19386=ORIENTED_EDGE ( 'NONE', *, *, #19438, .F. ) ;
#19387=DIRECTION ( 'NONE',  ( -1.000000000000000000, 0.000000000000000000, -0.000000000000000000 ) ) ;
#19388=DIRECTION ( 'NONE',  ( 0.000000000000000000, 0.000000000000000000, 1.000000000000000000 ) ) ;
#19397=VECTOR ( 'NONE', #20336, 1000.000000000000000 ) ;
#19399=DIRECTION ( 'NONE',  ( -1.000000000000000000, -0.000000000000000000, -0.000000000000000000 ) ) ;
#19403=ORIENTED_EDGE ( 'NONE', *, *, #10701, .T. ) ;
#19409=DIRECTION ( 'NONE',  ( -1.000000000000000000, 0.000000000000000000, 0.000000000000000000 ) ) ;
#19412=CARTESIAN_POINT ( 'NONE',  ( 19.99999999999999645, -70.68211945903198057, 13.71269443944183841 ) ) ;
#19415=LINE ( 'NONE', #441, #10023 ) ;
#19417=DIRECTION ( 'NONE',  ( -1.000000000000000000, 0.000000000000000000, 0.000000000000000000 ) ) ;
#19419=CIRCLE ( 'NONE', #10280, 27.60000000002759890 ) ;
#19420=CARTESIAN_POINT ( 'NONE',  ( 19.99999999999999645, 53.26727847779537228, 48.44168704307649875 ) ) ;
#19421=CIRCLE ( 'NONE', #16364, 65.24900000006525147 ) ;
#19423=ORIENTED_EDGE ( 'NONE', *, *, #19776, .F. ) ;
#19434=EDGE_CURVE ( 'NONE', #15450, #18079, #10029, .T. ) ;
#19435=FACE_OUTER_BOUND ( 'NONE', #11382, .T. ) ;
#19438=EDGE_CURVE ( 'NONE', #9449, #5396, #7653, .T. ) ;
#19440=CIRCLE ( 'NONE', #2858, 27.60000000002759890 ) ;
#19442=EDGE_CURVE ( 'NONE', #6220, #1870, #11049, .T. ) ;
#19444=DIRECTION ( 'NONE',  ( 0.000000000000000000, 0.2697967711570248839, -0.9629172873477991335 ) ) ;
#19446=VERTEX_POINT ( 'NONE', #20067 ) ;
#19452=AXIS2_PLACEMENT_3D ( 'NONE', #2058, #4280, #18698 ) ;
#19454=DIRECTION ( 'NONE',  ( -1.000000000000000000, 0.000000000000000000, -0.000000000000000000 ) ) ;
#19458=EDGE_CURVE ( 'NONE', #14269, #5705, #897, .T. ) ;
#19462=DIRECTION ( 'NONE',  ( -1.000000000000000000, 0.000000000000000000, 0.000000000000000000 ) ) ;
#19463=DIRECTION ( 'NONE',  ( -1.000000000000000000, 0.000000000000000000, -0.000000000000000000 ) ) ;
#19465=ADVANCED_FACE ( 'NONE', ( #2699 ), #9165, .T. ) ;
#19474=CARTESIAN_POINT ( 'NONE',  ( 0.000000000000000000, 0.000000000000000000, 0.000000000000000000 ) ) ;
#19480=ORIENTED_EDGE ( 'NONE', *, *, #10644, .F. ) ;
#19481=CARTESIAN_POINT ( 'NONE',  ( 0.000000000000000000, -19.38316218894168586, -61.87375713201008409 ) ) ;
#19482=EDGE_CURVE ( 'NONE', #13947, #15185, #3587, .T. ) ;
#19484=DIRECTION ( 'NONE',  ( 0.000000000000000000, 0.000000000000000000, 1.000000000000000000 ) ) ;
#19485=VERTEX_POINT ( 'NONE', #19022 ) ;
#19487=ORIENTED_EDGE ( 'NONE', *, *, #12344, .F. ) ;
#19491=VERTEX_POINT ( 'NONE', #20813 ) ;
#19493=CIRCLE ( 'NONE', #16447, 27.60000000002759890 ) ;
#19496=CARTESIAN_POINT ( 'NONE',  ( 9.999999999999998224, 10.74906464462217137, -71.19310085447958159 ) ) ;
#19497=AXIS2_PLACEMENT_3D ( 'NONE', #7134, #17005, #13618 ) ;
#19501=CIRCLE ( 'NONE', #2291, 65.24900000006525147 ) ;
#19503=DIRECTION ( 'NONE',  ( -1.000000000000000000, 0.000000000000000000, 0.000000000000000000 ) ) ;
#19504=AXIS2_PLACEMENT_3D ( 'NONE', #18589, #9149, #13825 ) ;
#19505=ORIENTED_EDGE ( 'NONE', *, *, #6924, .T. ) ;
#19506=DIRECTION ( 'NONE',  ( -1.000000000000000000, 0.000000000000000000, -0.000000000000000000 ) ) ;
#19508=DIRECTION ( 'NONE',  ( 0.000000000000000000, 0.000000000000000000, 1.000000000000000000 ) ) ;
#19509=ORIENTED_EDGE ( 'NONE', *, *, #13897, .T. ) ;
#19510=CARTESIAN_POINT ( 'NONE',  ( 19.99999999999999645, -70.29359119158473845, -15.58239511117358944 ) ) ;
#19518=ORIENTED_EDGE ( 'NONE', *, *, #17128, .T. ) ;
#19519=DIRECTION ( 'NONE',  ( -1.000000000000000000, -0.000000000000000000, -0.000000000000000000 ) ) ;
#19520=ADVANCED_FACE ( 'NONE', ( #14368 ), #19134, .F. ) ;
#19521=EDGE_CURVE ( 'NONE', #10081, #2829, #20855, .T. ) ;
#19523=DIRECTION ( 'NONE',  ( -1.000000000000000000, 0.000000000000000000, -0.000000000000000000 ) ) ;
#19524=AXIS2_PLACEMENT_3D ( 'NONE', #15143, #17048, #12276 ) ;
#19526=DIRECTION ( 'NONE',  ( 0.000000000000000000, 0.6310879443260485333, 0.7757112907044232397 ) ) ;
#19528=VECTOR ( 'NONE', #2632, 1000.000000000000000 ) ;
#19533=CARTESIAN_POINT ( 'NONE',  ( 0.000000000000000000, -58.44960523466261293, 28.06621538408569805 ) ) ;
#19535=LINE ( 'NONE', #16253, #10876 ) ;
#19539=AXIS2_PLACEMENT_3D ( 'NONE', #11124, #7945, #19484 ) ;
#19542=ORIENTED_EDGE ( 'NONE', *, *, #20878, .F. ) ;
#19543=CARTESIAN_POINT ( 'NONE',  ( 19.99999999999999645, 0.000000000000000000, 0.000000000000000000 ) ) ;
#19552=EDGE_CURVE ( 'NONE', #14177, #17518, #561, .T. ) ;
#19554=DIRECTION ( 'NONE',  ( -1.000000000000000000, 0.000000000000000000, 0.000000000000000000 ) ) ;
#19556=DIRECTION ( 'NONE',  ( -1.000000000000000000, -0.000000000000000000, -0.000000000000000000 ) ) ;
#19558=CARTESIAN_POINT ( 'NONE',  ( -10.00000000000000000, 0.000000000000000000, 0.000000000000000000 ) ) ;
#19560=DIRECTION ( 'NONE',  ( -1.000000000000000000, 0.000000000000000000, -0.000000000000000000 ) ) ;
#19562=EDGE_CURVE ( 'NONE', #2697, #11465, #12413, .T. ) ;
#19565=EDGE_LOOP ( 'NONE', ( #6392, #283, #17122, #13813 ) ) ;
#19567=DIRECTION ( 'NONE',  ( 0.000000000000000000, 0.000000000000000000, -1.000000000000000000 ) ) ;
#19569=ORIENTED_EDGE ( 'NONE', *, *, #1484, .F. ) ;
#19576=EDGE_CURVE ( 'NONE', #10139, #9276, #13426, .T. ) ;
#19580=DIRECTION ( 'NONE',  ( -1.000000000000000000, 0.000000000000000000, 0.000000000000000000 ) ) ;
#19584=DIRECTION ( 'NONE',  ( -1.000000000000000000, 0.000000000000000000, 0.000000000000000000 ) ) ;
#19589=VERTEX_POINT ( 'NONE', #3113 ) ;
#19593=EDGE_CURVE ( 'NONE', #1684, #1429, #9383, .T. ) ;
#19599=CARTESIAN_POINT ( 'NONE',  ( 19.99999999999999645, -63.85430960833482317, 16.34407078397855528 ) ) ;
#19600=ADVANCED_FACE ( 'NONE', ( #20604 ), #16052, .T. ) ;
#19601=CARTESIAN_POINT ( 'NONE',  ( 19.99999999999999645, 71.76067541710858677, -5.865617076723870227 ) ) ;
#19606=ORIENTED_EDGE ( 'NONE', *, *, #2981, .F. ) ;
#19612=EDGE_LOOP ( 'NONE', ( #6495, #8351, #3703, #15932 ) ) ;
#19614=DIRECTION ( 'NONE',  ( 1.000000000000000000, -0.000000000000000000, 0.000000000000000000 ) ) ;
#19619=CARTESIAN_POINT ( 'NONE',  ( 19.99999999999999645, 20.34307325858883431, -69.06634035770284186 ) ) ;
#19624=CARTESIAN_POINT ( 'NONE',  ( 19.99999999999999645, 35.35772184876955038, -54.34979580218157480 ) ) ;
#19633=CIRCLE ( 'NONE', #18983, 27.60000000002759535 ) ;
#19634=VERTEX_POINT ( 'NONE', #20503 ) ;
#19635=CARTESIAN_POINT ( 'NONE',  ( 19.99999999999999645, -63.85430960833482317, -11.25592921604904539 ) ) ;
#19640=AXIS2_PLACEMENT_3D ( 'NONE', #14048, #4282, #18917 ) ;
#19643=AXIS2_PLACEMENT_3D ( 'NONE', #2260, #13596, #2155 ) ;
#19645=VERTEX_POINT ( 'NONE', #5983 ) ;
#19647=DIRECTION ( 'NONE',  ( 0.000000000000000000, 0.000000000000000000, 1.000000000000000000 ) ) ;
#19650=ORIENTED_EDGE ( 'NONE', *, *, #5630, .T. ) ;
#19657=AXIS2_PLACEMENT_3D ( 'NONE', #5823, #20656, #2756 ) ;
#19658=ORIENTED_EDGE ( 'NONE', *, *, #1368, .T. ) ;
#19660=DIRECTION ( 'NONE',  ( -1.000000000000000000, 0.000000000000000000, -0.000000000000000000 ) ) ;
#19662=ORIENTED_EDGE ( 'NONE', *, *, #9877, .T. ) ;
#19663=CARTESIAN_POINT ( 'NONE',  ( 19.99999999999999645, 51.96384592647198986, 49.83732252579632416 ) ) ;
#19664=DIRECTION ( 'NONE',  ( -1.000000000000000000, -0.000000000000000000, -0.000000000000000000 ) ) ;
#19674=ORIENTED_EDGE ( 'NONE', *, *, #2403, .F. ) ;
#19676=CIRCLE ( 'NONE', #7147, 7.500000000000000000 ) ;
#19680=EDGE_LOOP ( 'NONE', ( #17167, #1731, #1207, #1093, #11024, #12555, #6707, #11634, #7894, #17181, #15060, #17447, #18923, #12232, #19271, #13060, #18138, #3967, #20170, #13731, #19386, #6594, #9007, #18466, #9247, #18264, #4261, #2127, #12664, #3804, #7307, #9061, #9330, #14474, #3941, #9886, #5971, #6548, #9573, #576, #12645, #19842, #10771, #18331, #13069, #2676, #17603, #491, #14665, #6345, #3011, #18527, #8277, #19674, #15543, #17521, #11890, #10866, #3425, #1329, #19972, #20559, #2656, #2859, #16304, #18075, #8737, #1019, #20599, #6213, #10536, #772, #20636, #3959, #2171, #11390, #12295, #10288, #42, #4243, #13522, #3555, #7281, #11252, #15996, #3973, #4286, #5691, #7568, #11951, #13861, #17862, #941, #14786, #10233, #8323, #535, #4237, #1199, #749, #3853, #625, #4189, #8402, #2202, #12959, #7235, #19213, #14591, #73, #13471, #12927, #12302, #2181, #6404, #10325, #9771, #11125, #11906, #596, #3389, #18425, #7670, #8142, #1890, #4516, #15659, #15812, #14049, #17708, #14985, #16047, #16149, #3932, #14771, #14108, #14711, #10157, #16741, #6293, #13192, #4860, #18523, #9178, #6473, #12030, #5301, #20873, #13830, #1004, #10206, #18156, #2810, #4115, #2867, #20699, #3312, #12450, #13914, #18581, #460, #20099, #9169, #7328, #3625, #4496, #15372, #20548, #9736, #7622, #14339, #15527, #144, #20292, #15712, #4830, #18603, #11469, #14075, #2990, #20085, #18236, #6462, #10261, #9941, #17572, #1576, #11846, #16720 ) ) ;
#19682=EDGE_CURVE ( 'NONE', #645, #12045, #3521, .T. ) ;
#19683=CARTESIAN_POINT ( 'NONE',  ( 0.000000000000000000, -56.42118728228177105, 32.77318456705422278 ) ) ;
#19684=CIRCLE ( 'NONE', #5457, 27.60000000002759890 ) ;
#19686=CYLINDRICAL_SURFACE ( 'NONE', #741, 27.60000000002759890 ) ;
#19688=EDGE_CURVE ( 'NONE', #2782, #18871, #1258, .T. ) ;
#19690=CIRCLE ( 'NONE', #8857, 65.24900000006525147 ) ;
#19695=EDGE_CURVE ( 'NONE', #6425, #16884, #251, .T. ) ;
#19698=DIRECTION ( 'NONE',  ( -1.000000000000000000, 0.000000000000000000, -0.000000000000000000 ) ) ;
#19700=AXIS2_PLACEMENT_3D ( 'NONE', #20222, #18431, #12277 ) ;
#19705=DIRECTION ( 'NONE',  ( 0.000000000000000000, 0.8169698930104432044, -0.5766803221148655290 ) ) ;
#19706=EDGE_CURVE ( 'NONE', #2775, #7789, #14115, .T. ) ;
#19707=ORIENTED_EDGE ( 'NONE', *, *, #11217, .T. ) ;
#19708=CARTESIAN_POINT ( 'NONE',  ( 19.99999999999999645, 0.000000000000000000, 0.000000000000000000 ) ) ;
#19711=CIRCLE ( 'NONE', #19385, 72.00000000007199219 ) ;
#19714=DIRECTION ( 'NONE',  ( -1.000000000000000000, -0.000000000000000000, -0.000000000000000000 ) ) ;
#19715=VERTEX_POINT ( 'NONE', #9991 ) ;
#19719=ORIENTED_EDGE ( 'NONE', *, *, #8185, .T. ) ;
#19725=AXIS2_PLACEMENT_3D ( 'NONE', #8155, #4986, #11649 ) ;
#19726=CIRCLE ( 'NONE', #10597, 65.24900000006526568 ) ;
#19728=DIRECTION ( 'NONE',  ( -1.000000000000000000, -0.000000000000000000, -0.000000000000000000 ) ) ;
#19737=CIRCLE ( 'NONE', #20057, 27.60000000002759890 ) ;
#19739=ORIENTED_EDGE ( 'NONE', *, *, #9798, .F. ) ;
#19744=VERTEX_POINT ( 'NONE', #15677 ) ;
#19746=ORIENTED_EDGE ( 'NONE', *, *, #14533, .T. ) ;
#19747=LINE ( 'NONE', #11389, #18288 ) ;
#19748=DIRECTION ( 'NONE',  ( -1.000000000000000000, -0.000000000000000000, 0.000000000000000000 ) ) ;
#19749=ORIENTED_EDGE ( 'NONE', *, *, #11217, .F. ) ;
#19752=DIRECTION ( 'NONE',  ( 0.000000000000000000, 0.000000000000000000, 1.000000000000000000 ) ) ;
#19761=AXIS2_PLACEMENT_3D ( 'NONE', #5897, #16176, #8013 ) ;
#19764=CARTESIAN_POINT ( 'NONE',  ( 9.999999999999998224, -0.9548212943360466776, -71.99366858485717557 ) ) ;
#19767=ORIENTED_EDGE ( 'NONE', *, *, #17762, .F. ) ;
#19770=ORIENTED_EDGE ( 'NONE', *, *, #19370, .F. ) ;
#19772=VECTOR ( 'NONE', #8387, 1000.000000000000000 ) ;
#19773=ORIENTED_EDGE ( 'NONE', *, *, #8438, .F. ) ;
#19776=EDGE_CURVE ( 'NONE', #10364, #4710, #915, .T. ) ;
#19780=VERTEX_POINT ( 'NONE', #4235 ) ;
#19782=CARTESIAN_POINT ( 'NONE',  ( 0.000000000000000000, -8.857208570069305509, -71.45313048675095047 ) ) ;
#19783=CARTESIAN_POINT ( 'NONE',  ( 19.99999999999999645, 71.89099403602354244, -3.960426305689046522 ) ) ;
#19787=CARTESIAN_POINT ( 'NONE',  ( 0.000000000000000000, 56.42118728228155788, 32.77318456705461358 ) ) ;
#19792=CARTESIAN_POINT ( 'NONE',  ( 85.00002539999999840, 0.000000000000000000, 0.000000000000000000 ) ) ;
#19794=ADVANCED_BREP_SHAPE_REPRESENTATION ( '', ( #10511, #12461 ), #5631 ) ;
#19795=ORIENTED_EDGE ( 'NONE', *, *, #6479, .F. ) ;
#19802=UNCERTAINTY_MEASURE_WITH_UNIT (LENGTH_MEASURE( 1.000000000000000082E-05 ), #20023, 'distance_accuracy_value', 'NONE');
#19803=CARTESIAN_POINT ( 'NONE',  ( 0.000000000000000000, 44.69367065308645692, 56.44887778834763026 ) ) ;
#19809=EDGE_CURVE ( 'NONE', #6701, #16060, #6972, .T. ) ;
#19810=DIRECTION ( 'NONE',  ( -1.000000000000000000, -0.000000000000000000, -0.000000000000000000 ) ) ;
#19813=CARTESIAN_POINT ( 'NONE',  ( 19.99999999999999645, 35.35772184876955038, -54.34979580218157480 ) ) ;
#19815=FACE_OUTER_BOUND ( 'NONE', #13527, .T. ) ;
#19816=EDGE_CURVE ( 'NONE', #12431, #13947, #19376, .T. ) ;
#19817=ORIENTED_EDGE ( 'NONE', *, *, #18528, .F. ) ;
#19819=CARTESIAN_POINT ( 'NONE',  ( 0.000000000000000000, 43.56693332842786504, 48.57318520917521454 ) ) ;
#19825=ORIENTED_EDGE ( 'NONE', *, *, #9637, .T. ) ;
#19828=CARTESIAN_POINT ( 'NONE',  ( 9.999999999999998224, -44.69367065308607323, -56.44887778834792158 ) ) ;
#19829=CARTESIAN_POINT ( 'NONE',  ( 0.000000000000000000, 0.000000000000000000, 0.000000000000000000 ) ) ;
#19832=DIRECTION ( 'NONE',  ( -1.000000000000000000, 0.000000000000000000, -0.000000000000000000 ) ) ;
#19833=AXIS2_PLACEMENT_3D ( 'NONE', #2339, #550, #18342 ) ;
#19838=AXIS2_PLACEMENT_3D ( 'NONE', #19324, #6189, #15844 ) ;
#19839=CIRCLE ( 'NONE', #15779, 65.24900000006525147 ) ;
#19840=ORIENTED_EDGE ( 'NONE', *, *, #16065, .T. ) ;
#19842=ORIENTED_EDGE ( 'NONE', *, *, #16847, .F. ) ;
#19844=CARTESIAN_POINT ( 'NONE',  ( 19.99999999999999645, -28.84646472442415543, -58.52617768068463278 ) ) ;
#19848=ORIENTED_EDGE ( 'NONE', *, *, #673, .F. ) ;
#19849=CARTESIAN_POINT ( 'NONE',  ( 19.99999999999999645, -59.31169354540756444, 27.19476070466835438 ) ) ;
#19853=VECTOR ( 'NONE', #17214, 1000.000000000000000 ) ;
#19854=AXIS2_PLACEMENT_3D ( 'NONE', #10264, #2208, #19995 ) ;
#19855=EDGE_CURVE ( 'NONE', #10231, #18587, #3171, .T. ) ;
#19860=CIRCLE ( 'NONE', #10735, 72.00000000007199219 ) ;
#19866=DIRECTION ( 'NONE',  ( -1.000000000000000000, 0.000000000000000000, -0.000000000000000000 ) ) ;
#19869=CARTESIAN_POINT ( 'NONE',  ( 19.99999999999999645, 0.000000000000000000, 0.000000000000000000 ) ) ;
#19875=AXIS2_PLACEMENT_3D ( 'NONE', #4156, #2580, #20369 ) ;
#19879=ORIENTED_EDGE ( 'NONE', *, *, #1481, .T. ) ;
#19881=VECTOR ( 'NONE', #4322, 1000.000000000000000 ) ;
#19888=AXIS2_PLACEMENT_3D ( 'NONE', #14915, #18205, #16292 ) ;
#19891=CARTESIAN_POINT ( 'NONE',  ( 0.000000000000000000, 31.17893654894306721, -57.31758819669140337 ) ) ;
#19893=DIRECTION ( 'NONE',  ( 0.000000000000000000, 0.000000000000000000, 1.000000000000000000 ) ) ;
#19898=DIRECTION ( 'NONE',  ( 0.000000000000000000, 0.000000000000000000, -1.000000000000000000 ) ) ;
#19899=ORIENTED_EDGE ( 'NONE', *, *, #5210, .T. ) ;
#19900=CARTESIAN_POINT ( 'NONE',  ( 19.99999999999999645, 0.000000000000000000, 0.000000000000000000 ) ) ;
#19906=FACE_OUTER_BOUND ( 'NONE', #17722, .T. ) ;
#19911=FACE_OUTER_BOUND ( 'NONE', #5346, .T. ) ;
#19921=CYLINDRICAL_SURFACE ( 'NONE', #19999, 27.60000000002759890 ) ;
#19922=DIRECTION ( 'NONE',  ( 0.000000000000000000, 0.8878852184023763305, -0.4600650377311499839 ) ) ;
#19923=EDGE_LOOP ( 'NONE', ( #20210, #4578, #14641, #4670 ) ) ;
#19924=ORIENTED_EDGE ( 'NONE', *, *, #272, .T. ) ;
#19928=DIRECTION ( 'NONE',  ( -1.000000000000000000, -0.000000000000000000, 0.000000000000000000 ) ) ;
#19929=DIRECTION ( 'NONE',  ( -1.000000000000000000, 0.000000000000000000, 0.000000000000000000 ) ) ;
#19931=CARTESIAN_POINT ( 'NONE',  ( 19.99999999999999645, -15.58726123847893774, 62.93731870009398932 ) ) ;
#19932=CARTESIAN_POINT ( 'NONE',  ( 19.99999999999999645, 65.23577793412344761, -1.313498510941930153 ) ) ;
#19937=EDGE_LOOP ( 'NONE', ( #6638, #6215, #9829, #5573 ) ) ;
#19940=EDGE_LOOP ( 'NONE', ( #9011, #1497, #9097, #7045 ) ) ;
#19942=EDGE_LOOP ( 'NONE', ( #3579, #12656, #5458, #1344 ) ) ;
#19944=CYLINDRICAL_SURFACE ( 'NONE', #15105, 65.24900000006525147 ) ;
#19945=EDGE_LOOP ( 'NONE', ( #1867, #5187, #19606, #15580 ) ) ;
#19946=ADVANCED_FACE ( 'NONE', ( #13445 ), #10359, .T. ) ;
#19948=DIRECTION ( 'NONE',  ( 0.000000000000000000, 0.000000000000000000, 1.000000000000000000 ) ) ;
#19952=EDGE_CURVE ( 'NONE', #10498, #3661, #20187, .T. ) ;
#19954=EDGE_CURVE ( 'NONE', #12290, #17620, #511, .T. ) ;
#19964=ORIENTED_EDGE ( 'NONE', *, *, #8127, .T. ) ;
#19966=ORIENTED_EDGE ( 'NONE', *, *, #11799, .F. ) ;
#19968=AXIS2_PLACEMENT_3D ( 'NONE', #5976, #9267, #12449 ) ;
#19969=ORIENTED_EDGE ( 'NONE', *, *, #16069, .F. ) ;
#19971=EDGE_CURVE ( 'NONE', #6180, #10026, #9714, .T. ) ;
#19972=ORIENTED_EDGE ( 'NONE', *, *, #15706, .F. ) ;
#19973=DIRECTION ( 'NONE',  ( -1.000000000000000000, -0.000000000000000000, 0.000000000000000000 ) ) ;
#19977=ORIENTED_EDGE ( 'NONE', *, *, #1328, .T. ) ;
#19978=CIRCLE ( 'NONE', #10865, 72.00000000007199219 ) ;
#19979=DIRECTION ( 'NONE',  ( -1.000000000000000000, -0.000000000000000000, 0.000000000000000000 ) ) ;
#19982=DIRECTION ( 'NONE',  ( 0.000000000000000000, 0.000000000000000000, 1.000000000000000000 ) ) ;
#19983=AXIS2_PLACEMENT_3D ( 'NONE', #19543, #8405, #3424 ) ;
#19985=ORIENTED_EDGE ( 'NONE', *, *, #5468, .F. ) ;
#19988=ORIENTED_EDGE ( 'NONE', *, *, #4192, .T. ) ;
#19991=FACE_OUTER_BOUND ( 'NONE', #6554, .T. ) ;
#19993=ORIENTED_EDGE ( 'NONE', *, *, #1587, .T. ) ;
#19995=DIRECTION ( 'NONE',  ( 0.000000000000000000, 0.000000000000000000, 1.000000000000000000 ) ) ;
#19998=DIRECTION ( 'NONE',  ( -1.000000000000000000, -0.000000000000000000, 0.000000000000000000 ) ) ;
#19999=AXIS2_PLACEMENT_3D ( 'NONE', #5609, #18654, #8691 ) ;
#20003=DIRECTION ( 'NONE',  ( 0.000000000000000000, 0.000000000000000000, 1.000000000000000000 ) ) ;
#20006=FACE_OUTER_BOUND ( 'NONE', #4258, .T. ) ;
#20007=CIRCLE ( 'NONE', #13954, 72.00000000007199219 ) ;
#20009=EDGE_LOOP ( 'NONE', ( #7139, #15513, #8590, #17501 ) ) ;
#20012=CARTESIAN_POINT ( 'NONE',  ( 0.000000000000000000, -38.69327817041740047, -52.53819777490674880 ) ) ;
#20014=VERTEX_POINT ( 'NONE', #19787 ) ;
#20021=ORIENTED_EDGE ( 'NONE', *, *, #17513, .T. ) ;
#20022=FACE_OUTER_BOUND ( 'NONE', #9674, .T. ) ;
#20023=( LENGTH_UNIT ( ) NAMED_UNIT ( * ) SI_UNIT ( .MILLI., .METRE. ) );
#20024=FACE_OUTER_BOUND ( 'NONE', #18391, .T. ) ;
#20026=AXIS2_PLACEMENT_3D ( 'NONE', #5706, #965, #2854 ) ;
#20033=CARTESIAN_POINT ( 'NONE',  ( 19.99999999999999645, 23.08379033237351052, 61.02926039941442582 ) ) ;
#20034=VERTEX_POINT ( 'NONE', #16715 ) ;
#20039=AXIS2_PLACEMENT_3D ( 'NONE', #3664, #5145, #13017 ) ;
#20041=AXIS2_PLACEMENT_3D ( 'NONE', #7829, #16104, #3272 ) ;
#20044=CARTESIAN_POINT ( 'NONE',  ( 19.99999999999999645, 29.55812890831981932, 65.65300461859696668 ) ) ;
#20045=DIRECTION ( 'NONE',  ( 0.000000000000000000, 0.7308359642781206977, 0.6825531432186578984 ) ) ;
#20047=CIRCLE ( 'NONE', #10927, 27.60000000002759890 ) ;
#20049=DIRECTION ( 'NONE',  ( 0.000000000000000000, 0.000000000000000000, 1.000000000000000000 ) ) ;
#20057=AXIS2_PLACEMENT_3D ( 'NONE', #3936, #2153, #18259 ) ;
#20059=DIRECTION ( 'NONE',  ( 0.000000000000000000, 0.000000000000000000, 1.000000000000000000 ) ) ;
#20061=VERTEX_POINT ( 'NONE', #10569 ) ;
#20064=ORIENTED_EDGE ( 'NONE', *, *, #20904, .F. ) ;
#20067=CARTESIAN_POINT ( 'NONE',  ( 19.99999999999999645, -55.05624179292004072, 35.01774179823764399 ) ) ;
#20071=FACE_OUTER_BOUND ( 'NONE', #16177, .T. ) ;
#20074=EDGE_CURVE ( 'NONE', #1607, #14245, #17250, .T. ) ;
#20079=ORIENTED_EDGE ( 'NONE', *, *, #1368, .F. ) ;
#20081=CARTESIAN_POINT ( 'NONE',  ( 0.000000000000000000, -63.85430960833482317, -11.25592921604904539 ) ) ;
#20083=CIRCLE ( 'NONE', #13326, 72.00000000007199219 ) ;
#20084=EDGE_CURVE ( 'NONE', #14491, #20014, #1362, .T. ) ;
#20085=ORIENTED_EDGE ( 'NONE', *, *, #6486, .F. ) ;
#20086=DIRECTION ( 'NONE',  ( 1.000000000000000000, 0.000000000000000000, 0.000000000000000000 ) ) ;
#20089=ADVANCED_FACE ( 'NONE', ( #2720 ), #9188, .T. ) ;
#20092=ADVANCED_FACE ( 'NONE', ( #18737 ), #2522, .T. ) ;
#20096=DIRECTION ( 'NONE',  ( -1.000000000000000000, 0.000000000000000000, 0.000000000000000000 ) ) ;
#20097=DIRECTION ( 'NONE',  ( -1.000000000000000000, 0.000000000000000000, 0.000000000000000000 ) ) ;
#20098=AXIS2_PLACEMENT_3D ( 'NONE', #16440, #19417, #6787 ) ;
#20099=ORIENTED_EDGE ( 'NONE', *, *, #19260, .F. ) ;
#20102=CARTESIAN_POINT ( 'NONE',  ( -10.00000000000000000, 0.000000000000000000, 0.000000000000000000 ) ) ;
#20107=AXIS2_PLACEMENT_3D ( 'NONE', #11462, #19298, #6375 ) ;
#20117=CARTESIAN_POINT ( 'NONE',  ( 0.000000000000000000, 5.762283366691162811, 64.99406197038673838 ) ) ;
#20119=EDGE_CURVE ( 'NONE', #10244, #13762, #14126, .T. ) ;
#20120=DIRECTION ( 'NONE',  ( -1.000000000000000000, -0.000000000000000000, -0.000000000000000000 ) ) ;
#20125=DIRECTION ( 'NONE',  ( -1.000000000000000000, 0.000000000000000000, 0.000000000000000000 ) ) ;
#20132=ORIENTED_EDGE ( 'NONE', *, *, #3890, .T. ) ;
#20133=CARTESIAN_POINT ( 'NONE',  ( 19.99999999999999645, 0.000000000000000000, 0.000000000000000000 ) ) ;
#20134=CARTESIAN_POINT ( 'NONE',  ( 19.99999999999999645, -55.05624179291956466, -35.01774179823839717 ) ) ;
#20135=CIRCLE ( 'NONE', #863, 65.24900000006525147 ) ;
#20147=ORIENTED_EDGE ( 'NONE', *, *, #3026, .F. ) ;
#20148=ADVANCED_FACE ( 'NONE', ( #4525 ), #10789, .T. ) ;
#20154=DIRECTION ( 'NONE',  ( -1.000000000000000000, -0.000000000000000000, -0.000000000000000000 ) ) ;
#20155=EDGE_CURVE ( 'NONE', #14998, #15789, #10989, .T. ) ;
#20158=CARTESIAN_POINT ( 'NONE',  ( 0.000000000000000000, 0.000000000000000000, 0.000000000000000000 ) ) ;
#20169=CARTESIAN_POINT ( 'NONE',  ( 19.99999999999999645, 55.05624179291979914, 35.01774179823801347 ) ) ;
#20170=ORIENTED_EDGE ( 'NONE', *, *, #8053, .F. ) ;
#20171=EDGE_CURVE ( 'NONE', #1772, #3060, #936, .T. ) ;
#20176=DIRECTION ( 'NONE',  ( 0.000000000000000000, 0.7308359642781208088, 0.6825531432186576763 ) ) ;
#20178=ORIENTED_EDGE ( 'NONE', *, *, #2330, .T. ) ;
#20179=DIRECTION ( 'NONE',  ( 1.000000000000000000, 0.000000000000000000, -0.000000000000000000 ) ) ;
#20185=ORIENTED_EDGE ( 'NONE', *, *, #20628, .T. ) ;
#20186=DIRECTION ( 'NONE',  ( -1.000000000000000000, 0.000000000000000000, -0.000000000000000000 ) ) ;
#20187=CIRCLE ( 'NONE', #4629, 65.24900000006526568 ) ;
#20189=CARTESIAN_POINT ( 'NONE',  ( 0.000000000000000000, -36.59093685910671212, 62.00889726308019334 ) ) ;
#20191=AXIS2_PLACEMENT_3D ( 'NONE', #20657, #11129, #7415 ) ;
#20196=AXIS2_PLACEMENT_3D ( 'NONE', #16697, #19973, #11923 ) ;
#20200=DIRECTION ( 'NONE',  ( -1.000000000000000000, -0.000000000000000000, 0.000000000000000000 ) ) ;
#20205=CARTESIAN_POINT ( 'NONE',  ( -10.00000000000000000, 0.000000000000000000, 0.000000000000000000 ) ) ;
#20207=CIRCLE ( 'NONE', #16161, 65.24900000006526568 ) ;
#20210=ORIENTED_EDGE ( 'NONE', *, *, #11371, .F. ) ;
#20211=CARTESIAN_POINT ( 'NONE',  ( -10.00000000000000000, 0.000000000000000000, 0.000000000000000000 ) ) ;
#20215=VERTEX_POINT ( 'NONE', #1766 ) ;
#20219=FACE_OUTER_BOUND ( 'NONE', #12183, .T. ) ;
#20221=CARTESIAN_POINT ( 'NONE',  ( 19.99999999999999645, -27.62776854598816101, -58.65812137499030854 ) ) ;
#20222=CARTESIAN_POINT ( 'NONE',  ( 19.99999999999999645, -63.85430960833482317, -11.25592921604904539 ) ) ;
#20225=DIRECTION ( 'NONE',  ( 0.000000000000000000, 0.000000000000000000, 1.000000000000000000 ) ) ;
#20226=EDGE_CURVE ( 'NONE', #11557, #16083, #16821, .T. ) ;
#20228=EDGE_CURVE ( 'NONE', #11622, #7171, #20837, .T. ) ;
#20229=DIRECTION ( 'NONE',  ( -1.000000000000000000, -0.000000000000000000, -0.000000000000000000 ) ) ;
#20231=CIRCLE ( 'NONE', #19504, 27.60000000002760245 ) ;
#20233=ORIENTED_EDGE ( 'NONE', *, *, #17632, .T. ) ;
#20238=ORIENTED_EDGE ( 'NONE', *, *, #565, .F. ) ;
#20240=CYLINDRICAL_SURFACE ( 'NONE', #11570, 72.00000000007199219 ) ;
#20242=CYLINDRICAL_SURFACE ( 'NONE', #8168, 27.60000000002759890 ) ;
#20244=ORIENTED_EDGE ( 'NONE', *, *, #978, .T. ) ;
#20250=DIRECTION ( 'NONE',  ( -1.000000000000000000, -0.000000000000000000, -0.000000000000000000 ) ) ;
#20252=DIRECTION ( 'NONE',  ( -1.000000000000000000, -0.000000000000000000, 0.000000000000000000 ) ) ;
#20255=ORIENTED_EDGE ( 'NONE', *, *, #6446, .F. ) ;
#20260=VERTEX_POINT ( 'NONE', #12809 ) ;
#20261=CARTESIAN_POINT ( 'NONE',  ( -10.00000000000000000, 0.000000000000000000, 0.000000000000000000 ) ) ;
#20262=ORIENTED_EDGE ( 'NONE', *, *, #6924, .F. ) ;
#20270=DIRECTION ( 'NONE',  ( -1.000000000000000000, -0.000000000000000000, -0.000000000000000000 ) ) ;
#20271=DIRECTION ( 'NONE',  ( -1.000000000000000000, 0.000000000000000000, 0.000000000000000000 ) ) ;
#20275=CARTESIAN_POINT ( 'NONE',  ( -10.00000000000000000, 0.000000000000000000, 0.000000000000000000 ) ) ;
#20287=CIRCLE ( 'NONE', #14563, 27.60000000002759890 ) ;
#20289=CARTESIAN_POINT ( 'NONE',  ( 20.00000000000000355, 0.000000000000000000, 7.500000000000000000 ) ) ;
#20292=ORIENTED_EDGE ( 'NONE', *, *, #978, .F. ) ;
#20293=EDGE_CURVE ( 'NONE', #3130, #4449, #11102, .T. ) ;
#20295=ORIENTED_EDGE ( 'NONE', *, *, #9237, .T. ) ;
#20299=CARTESIAN_POINT ( 'NONE',  ( 0.000000000000000000, -60.40676135667455071, 23.56039007469017221 ) ) ;
#20301=ADVANCED_FACE ( 'NONE', ( #17884 ), #16186, .T. ) ;
#20305=AXIS2_PLACEMENT_3D ( 'NONE', #13388, #18149, #3818 ) ;
#20306=ORIENTED_EDGE ( 'NONE', *, *, #4818, .F. ) ;
#20309=DIRECTION ( 'NONE',  ( 0.000000000000000000, -0.8878852184023702243, -0.4600650377311618633 ) ) ;
#20313=CARTESIAN_POINT ( 'NONE',  ( 19.99999999999999645, 39.37110852956814000, 51.51683813304883586 ) ) ;
#20314=CARTESIAN_POINT ( 'NONE',  ( 0.000000000000000000, 0.000000000000000000, 0.000000000000000000 ) ) ;
#20315=CIRCLE ( 'NONE', #13902, 72.00000000007199219 ) ;
#20321=VECTOR ( 'NONE', #19, 1000.000000000000000 ) ;
#20325=CARTESIAN_POINT ( 'NONE',  ( 9.999999999999998224, -27.80658314415180499, -66.41380830714152239 ) ) ;
#20331=CARTESIAN_POINT ( 'NONE',  ( 0.000000000000000000, 56.42118728228200553, -32.77318456705383198 ) ) ;
#20332=ORIENTED_EDGE ( 'NONE', *, *, #16263, .F. ) ;
#20336=DIRECTION ( 'NONE',  ( 1.000000000000000000, -0.000000000000000000, 0.000000000000000000 ) ) ;
#20344=DIRECTION ( 'NONE',  ( -1.000000000000000000, 0.000000000000000000, -0.000000000000000000 ) ) ;
#20345=CYLINDRICAL_SURFACE ( 'NONE', #11225, 27.60000000002759890 ) ;
#20348=EDGE_CURVE ( 'NONE', #19645, #8741, #19860, .T. ) ;
#20349=AXIS2_PLACEMENT_3D ( 'NONE', #8757, #706, #19982 ) ;
#20351=LINE ( 'NONE', #7424, #9868 ) ;
#20353=DIRECTION ( 'NONE',  ( 0.000000000000000000, -0.9422609221188167350, -0.3348796121709969875 ) ) ;
#20354=LINE ( 'NONE', #18784, #9173 ) ;
#20356=ADVANCED_FACE ( 'NONE', ( #5250 ), #373, .T. ) ;
#20357=ORIENTED_EDGE ( 'NONE', *, *, #17151, .T. ) ;
#20358=DIRECTION ( 'NONE',  ( 0.000000000000000000, 0.000000000000000000, 1.000000000000000000 ) ) ;
#20359=ADVANCED_FACE ( 'NONE', ( #10745 ), #7439, .T. ) ;
#20360=ORIENTED_EDGE ( 'NONE', *, *, #15915, .F. ) ;
#20364=VERTEX_POINT ( 'NONE', #13820 ) ;
#20369=DIRECTION ( 'NONE',  ( 0.000000000000000000, 0.000000000000000000, 1.000000000000000000 ) ) ;
#20374=CIRCLE ( 'NONE', #1439, 72.00000000007199219 ) ;
#20384=FACE_OUTER_BOUND ( 'NONE', #13167, .T. ) ;
#20386=VECTOR ( 'NONE', #11320, 1000.000000000000000 ) ;
#20388=CARTESIAN_POINT ( 'NONE',  ( 19.99999999999999645, 3.141410481201071914, 65.17333458706188765 ) ) ;
#20391=AXIS2_PLACEMENT_3D ( 'NONE', #8136, #17692, #16201 ) ;
#20393=ADVANCED_FACE ( 'NONE', ( #16980 ), #18684, .T. ) ;
#20397=ORIENTED_EDGE ( 'NONE', *, *, #1665, .T. ) ;
#20398=DIRECTION ( 'NONE',  ( 0.000000000000000000, 0.6310879443260538624, -0.7757112907044189098 ) ) ;
#20401=ORIENTED_EDGE ( 'NONE', *, *, #17918, .T. ) ;
#20405=CIRCLE ( 'NONE', #8545, 27.60000000002760601 ) ;
#20410=CYLINDRICAL_SURFACE ( 'NONE', #19761, 72.00000000007199219 ) ;
#20414=VECTOR ( 'NONE', #2239, 1000.000000000000000 ) ;
#20416=DIRECTION ( 'NONE',  ( 0.000000000000000000, 0.8169698930104393186, 0.5766803221148710801 ) ) ;
#20417=DIRECTION ( 'NONE',  ( -1.000000000000000000, 0.000000000000000000, 0.000000000000000000 ) ) ;
#20419=CIRCLE ( 'NONE', #17378, 27.60000000002759535 ) ;
#20422=FACE_OUTER_BOUND ( 'NONE', #4064, .T. ) ;
#20424=ORIENTED_EDGE ( 'NONE', *, *, #6716, .F. ) ;
#20426=EDGE_CURVE ( 'NONE', #2965, #20728, #5664, .T. ) ;
#20429=EDGE_CURVE ( 'NONE', #3338, #5717, #16493, .T. ) ;
#20435=CARTESIAN_POINT ( 'NONE',  ( 0.000000000000000000, -44.69367065308685483, 56.44887778834731762 ) ) ;
#20436=CARTESIAN_POINT ( 'NONE',  ( 19.99999999999999645, 0.000000000000000000, 0.000000000000000000 ) ) ;
#20437=CYLINDRICAL_SURFACE ( 'NONE', #3128, 27.60000000002759890 ) ;
#20440=VECTOR ( 'NONE', #19409, 1000.000000000000000 ) ;
#20449=ORIENTED_EDGE ( 'NONE', *, *, #8624, .T. ) ;
#20450=DIRECTION ( 'NONE',  ( -1.000000000000000000, 0.000000000000000000, 0.000000000000000000 ) ) ;
#20456=AXIS2_PLACEMENT_3D ( 'NONE', #18358, #2256, #462 ) ;
#20457=CARTESIAN_POINT ( 'NONE',  ( 0.000000000000000000, -64.36139404985944168, -32.27399814043941007 ) ) ;
#20458=CARTESIAN_POINT ( 'NONE',  ( 0.000000000000000000, -31.98952867950285395, -56.39803944231618971 ) ) ;
#20460=ORIENTED_EDGE ( 'NONE', *, *, #19434, .T. ) ;
#20462=CARTESIAN_POINT ( 'NONE',  ( 19.99999999999999645, -38.69327817041739337, -52.53819777490673459 ) ) ;
#20467=CARTESIAN_POINT ( 'NONE',  ( 19.99999999999999645, 51.43306257653197378, -40.15061736769512635 ) ) ;
#20471=ORIENTED_EDGE ( 'NONE', *, *, #20226, .T. ) ;
#20472=LINE ( 'NONE', #16129, #12250 ) ;
#20479=ORIENTED_EDGE ( 'NONE', *, *, #4725, .T. ) ;
#20481=CARTESIAN_POINT ( 'NONE',  ( 9.999999999999998224, -8.857208570069305509, -71.45313048675095047 ) ) ;
#20484=CARTESIAN_POINT ( 'NONE',  ( 0.000000000000000000, 64.36139404986010959, -32.27399814043809556 ) ) ;
#20485=CIRCLE ( 'NONE', #18814, 27.60000000002759890 ) ;
#20486=CARTESIAN_POINT ( 'NONE',  ( 0.000000000000000000, -38.22257254261782577, 61.01667762370126269 ) ) ;
#20494=VECTOR ( 'NONE', #14507, 1000.000000000000000 ) ;
#20496=CARTESIAN_POINT ( 'NONE',  ( 9.999999999999998224, -67.51707036274430607, 25.00890260772354878 ) ) ;
#20503=CARTESIAN_POINT ( 'NONE',  ( 19.99999999999999645, -11.98658579560543025, -64.13855129306480762 ) ) ;
#20505=ORIENTED_EDGE ( 'NONE', *, *, #16627, .F. ) ;
#20506=DIRECTION ( 'NONE',  ( -1.000000000000000000, 0.000000000000000000, 0.000000000000000000 ) ) ;
#20509=EDGE_CURVE ( 'NONE', #6520, #17663, #12444, .T. ) ;
#20510=EDGE_LOOP ( 'NONE', ( #18492, #18674, #7744, #19719 ) ) ;
#20511=EDGE_CURVE ( 'NONE', #5396, #9946, #20908, .T. ) ;
#20514=CIRCLE ( 'NONE', #7639, 27.60000000002759890 ) ;
#20516=CARTESIAN_POINT ( 'NONE',  ( 19.99999999999999645, -14.55863677812078016, -63.60407295269120453 ) ) ;
#20520=CARTESIAN_POINT ( 'NONE',  ( 0.000000000000000000, -51.81019761368347787, 38.98425606966041101 ) ) ;
#20522=CARTESIAN_POINT ( 'NONE',  ( 0.000000000000000000, -10.74906464462068456, -71.19310085447979475 ) ) ;
#20528=AXIS2_PLACEMENT_3D ( 'NONE', #13854, #5783, #19705 ) ;
#20529=ORIENTED_EDGE ( 'NONE', *, *, #1609, .F. ) ;
#20530=DIRECTION ( 'NONE',  ( 0.000000000000000000, 0.000000000000000000, 1.000000000000000000 ) ) ;
#20536=VECTOR ( 'NONE', #19614, 1000.000000000000000 ) ;
#20540=DIRECTION ( 'NONE',  ( -1.000000000000000000, 0.000000000000000000, 0.000000000000000000 ) ) ;
#20541=VECTOR ( 'NONE', #1897, 1000.000000000000000 ) ;
#20543=DIRECTION ( 'NONE',  ( -1.000000000000000000, 0.000000000000000000, 0.000000000000000000 ) ) ;
#20546=AXIS2_PLACEMENT_3D ( 'NONE', #10883, #4086, #20530 ) ;
#20548=ORIENTED_EDGE ( 'NONE', *, *, #2912, .F. ) ;
#20551=ADVANCED_FACE ( 'NONE', ( #11153 ), #6063, .T. ) ;
#20552=CIRCLE ( 'NONE', #20882, 72.00000000007199219 ) ;
#20554=VERTEX_POINT ( 'NONE', #19001 ) ;
#20556=AXIS2_PLACEMENT_3D ( 'NONE', #20313, #10696, #5795 ) ;
#20559=ORIENTED_EDGE ( 'NONE', *, *, #20685, .F. ) ;
#20560=DIRECTION ( 'NONE',  ( 0.000000000000000000, -0.5195839500354229035, -0.8544194045464950094 ) ) ;
#20561=AXIS2_PLACEMENT_3D ( 'NONE', #2744, #1172, #17055 ) ;
#20562=ORIENTED_EDGE ( 'NONE', *, *, #14173, .T. ) ;
#20564=DIRECTION ( 'NONE',  ( -1.000000000000000000, 0.000000000000000000, 0.000000000000000000 ) ) ;
#20565=AXIS2_PLACEMENT_3D ( 'NONE', #5135, #11607, #11815 ) ;
#20569=CIRCLE ( 'NONE', #11434, 72.00000000007199219 ) ;
#20572=AXIS2_PLACEMENT_3D ( 'NONE', #153, #6606, #9592 ) ;
#20579=DIRECTION ( 'NONE',  ( 1.000000000000000000, -0.000000000000000000, -0.000000000000000000 ) ) ;
#20584=EDGE_CURVE ( 'NONE', #17275, #16282, #1415, .T. ) ;
#20585=DIRECTION ( 'NONE',  ( -1.000000000000000000, -0.000000000000000000, -0.000000000000000000 ) ) ;
#20588=CARTESIAN_POINT ( 'NONE',  ( 19.99999999999999645, 54.08351995568756365, -35.76369202524444546 ) ) ;
#20589=CARTESIAN_POINT ( 'NONE',  ( 0.000000000000000000, 60.40676135667469282, -23.56039007468977431 ) ) ;
#20591=LINE ( 'NONE', #17736, #6607 ) ;
#20592=DIRECTION ( 'NONE',  ( -1.000000000000000000, 0.000000000000000000, 0.000000000000000000 ) ) ;
#20598=DIRECTION ( 'NONE',  ( -1.000000000000000000, -0.000000000000000000, -0.000000000000000000 ) ) ;
#20599=ORIENTED_EDGE ( 'NONE', *, *, #7668, .F. ) ;
#20600=CARTESIAN_POINT ( 'NONE',  ( 0.000000000000000000, -0.9548212943370493200, 71.99366858485716136 ) ) ;
#20602=VERTEX_POINT ( 'NONE', #20117 ) ;
#20604=FACE_OUTER_BOUND ( 'NONE', #7081, .T. ) ;
#20609=VERTEX_POINT ( 'NONE', #5924 ) ;
#20611=ADVANCED_FACE ( 'NONE', ( #18760 ), #16941, .T. ) ;
#20615=DIRECTION ( 'NONE',  ( -1.000000000000000000, 0.000000000000000000, 0.000000000000000000 ) ) ;
#20617=ORIENTED_EDGE ( 'NONE', *, *, #15957, .T. ) ;
#20620=EDGE_LOOP ( 'NONE', ( #11117, #10939, #3763, #16921 ) ) ;
#20625=CARTESIAN_POINT ( 'NONE',  ( 85.00002539999999840, 0.000000000000000000, 7.500000000000000000 ) ) ;
#20627=EDGE_LOOP ( 'NONE', ( #6010, #17393, #7459, #10153 ) ) ;
#20628=EDGE_CURVE ( 'NONE', #8629, #8808, #6675, .T. ) ;
#20629=CARTESIAN_POINT ( 'NONE',  ( 19.99999999999999645, 56.42118728228154367, 32.77318456705460648 ) ) ;
#20636=ORIENTED_EDGE ( 'NONE', *, *, #13641, .F. ) ;
#20637=DIRECTION ( 'NONE',  ( -1.000000000000000000, 0.000000000000000000, 0.000000000000000000 ) ) ;
#20639=CARTESIAN_POINT ( 'NONE',  ( 0.000000000000000000, -63.05226888949902531, 15.11556105343437828 ) ) ;
#20640=DIRECTION ( 'NONE',  ( -1.000000000000000000, 0.000000000000000000, 0.000000000000000000 ) ) ;
#20645=CYLINDRICAL_SURFACE ( 'NONE', #16167, 27.60000000002759890 ) ;
#20649=ORIENTED_EDGE ( 'NONE', *, *, #14545, .F. ) ;
#20650=LINE ( 'NONE', #11436, #1120 ) ;
#20652=LINE ( 'NONE', #15678, #5998 ) ;
#20656=DIRECTION ( 'NONE',  ( -1.000000000000000000, 0.000000000000000000, -0.000000000000000000 ) ) ;
#20657=CARTESIAN_POINT ( 'NONE',  ( 19.99999999999999645, 60.40676135667469282, -23.56039007468977431 ) ) ;
#20658=AXIS2_PLACEMENT_3D ( 'NONE', #9375, #10759, #18596 ) ;
#20663=CIRCLE ( 'NONE', #19643, 27.60000000002759890 ) ;
#20664=DIRECTION ( 'NONE',  ( -1.000000000000000000, 0.000000000000000000, -0.000000000000000000 ) ) ;
#20670=CARTESIAN_POINT ( 'NONE',  ( 19.99999999999999645, -71.76067541710854414, 5.865617076724380041 ) ) ;
#20671=ORIENTED_EDGE ( 'NONE', *, *, #13374, .F. ) ;
#20672=CYLINDRICAL_SURFACE ( 'NONE', #6820, 72.00000000007199219 ) ;
#20676=AXIS2_PLACEMENT_3D ( 'NONE', #2863, #1070, #14319 ) ;
#20678=DIRECTION ( 'NONE',  ( 0.000000000000000000, -0.3984010898462297390, -0.9172113015054581542 ) ) ;
#20679=ORIENTED_EDGE ( 'NONE', *, *, #5367, .F. ) ;
#20681=CARTESIAN_POINT ( 'NONE',  ( 19.99999999999999645, 0.000000000000000000, 0.000000000000000000 ) ) ;
#20683=ORIENTED_EDGE ( 'NONE', *, *, #17781, .T. ) ;
#20685=EDGE_CURVE ( 'NONE', #20728, #10182, #1292, .T. ) ;
#20686=CYLINDRICAL_SURFACE ( 'NONE', #10371, 27.60000000002759535 ) ;
#20689=CIRCLE ( 'NONE', #4098, 65.24900000006525147 ) ;
#20692=EDGE_LOOP ( 'NONE', ( #974, #1531, #8426, #5541 ) ) ;
#20699=ORIENTED_EDGE ( 'NONE', *, *, #14351, .F. ) ;
#20702=CARTESIAN_POINT ( 'NONE',  ( 19.99999999999999645, -63.85430960833497949, 11.25592921604817676 ) ) ;
#20705=AXIS2_PLACEMENT_3D ( 'NONE', #11685, #2148, #3624 ) ;
#20706=DIRECTION ( 'NONE',  ( 0.000000000000000000, 0.9790840876823220240, 0.2034560130526375243 ) ) ;
#20708=LINE ( 'NONE', #12562, #10558 ) ;
#20709=VECTOR ( 'NONE', #14107, 1000.000000000000000 ) ;
#20714=EDGE_CURVE ( 'NONE', #8788, #6733, #7502, .T. ) ;
#20717=EDGE_CURVE ( 'NONE', #13680, #1822, #10380, .T. ) ;
#20719=CIRCLE ( 'NONE', #775, 72.00000000007199219 ) ;
#20722=CARTESIAN_POINT ( 'NONE',  ( 19.99999999999999645, 0.000000000000000000, 0.000000000000000000 ) ) ;
#20724=EDGE_CURVE ( 'NONE', #14260, #19105, #15246, .T. ) ;
#20727=CARTESIAN_POINT ( 'NONE',  ( 19.99999999999999645, 64.79224928664386596, 2.456263514198732345 ) ) ;
#20728=VERTEX_POINT ( 'NONE', #9734 ) ;
#20729=DIRECTION ( 'NONE',  ( 0.000000000000000000, 0.000000000000000000, 1.000000000000000000 ) ) ;
#20732=AXIS2_PLACEMENT_3D ( 'NONE', #3479, #6456, #5179 ) ;
#20735=ORIENTED_EDGE ( 'NONE', *, *, #10920, .T. ) ;
#20736=CARTESIAN_POINT ( 'NONE',  ( 0.000000000000000000, 71.89099403602354244, 3.960426305689042970 ) ) ;
#20737=EDGE_CURVE ( 'NONE', #11443, #15314, #15882, .T. ) ;
#20738=DIRECTION ( 'NONE',  ( -1.000000000000000000, 0.000000000000000000, -0.000000000000000000 ) ) ;
#20743=EDGE_CURVE ( 'NONE', #1553, #10695, #11118, .T. ) ;
#20744=EDGE_CURVE ( 'NONE', #2973, #16343, #6340, .T. ) ;
#20750=CARTESIAN_POINT ( 'NONE',  ( 85.00002539999999840, 0.000000000000000000, 0.000000000000000000 ) ) ;
#20753=DIRECTION ( 'NONE',  ( 0.000000000000000000, 0.000000000000000000, 1.000000000000000000 ) ) ;
#20755=DIRECTION ( 'NONE',  ( 0.000000000000000000, -0.2697967711570115057, -0.9629172873478027972 ) ) ;
#20763=ORIENTED_EDGE ( 'NONE', *, *, #15161, .F. ) ;
#20765=ORIENTED_EDGE ( 'NONE', *, *, #17541, .T. ) ;
#20769=EDGE_CURVE ( 'NONE', #16945, #14269, #12718, .T. ) ;
#20770=EDGE_CURVE ( 'NONE', #11465, #19379, #8039, .T. ) ;
#20774=EDGE_CURVE ( 'NONE', #15895, #13680, #2972, .T. ) ;
#20781=VECTOR ( 'NONE', #5509, 1000.000000000000000 ) ;
#20782=LINE ( 'NONE', #7854, #10791 ) ;
#20785=DIRECTION ( 'NONE',  ( 0.000000000000000000, 0.000000000000000000, 1.000000000000000000 ) ) ;
#20786=ORIENTED_EDGE ( 'NONE', *, *, #934, .F. ) ;
#20797=DIRECTION ( 'NONE',  ( 0.000000000000000000, 0.1361666490962468723, -0.9906859460363306447 ) ) ;
#20802=ORIENTED_EDGE ( 'NONE', *, *, #6712, .T. ) ;
#20804=LINE ( 'NONE', #12971, #9152 ) ;
#20813=CARTESIAN_POINT ( 'NONE',  ( -65.00002539999999840, 4.898587196589412829E-16, -4.000000000000000000 ) ) ;
#20814=CYLINDRICAL_SURFACE ( 'NONE', #9633, 65.24900000006525147 ) ;
#20815=EDGE_LOOP ( 'NONE', ( #17547, #5106, #15401, #7577 ) ) ;
#20816=DIRECTION ( 'NONE',  ( 0.000000000000000000, 0.2697967711570183891, 0.9629172873478009098 ) ) ;
#20817=ORIENTED_EDGE ( 'NONE', *, *, #11069, .T. ) ;
#20818=CIRCLE ( 'NONE', #15403, 27.60000000002759535 ) ;
#20823=CARTESIAN_POINT ( 'NONE',  ( 9.999999999999998224, 10.74906464462118016, 71.19310085447973790 ) ) ;
#20826=ORIENTED_EDGE ( 'NONE', *, *, #88, .F. ) ;
#20828=FACE_OUTER_BOUND ( 'NONE', #9869, .T. ) ;
#20832=EDGE_CURVE ( 'NONE', #15515, #2965, #13804, .T. ) ;
#20836=CIRCLE ( 'NONE', #8649, 27.60000000002760245 ) ;
#20837=LINE ( 'NONE', #16080, #7345 ) ;
#20838=CARTESIAN_POINT ( 'NONE',  ( 19.99999999999999645, -58.44960523466261293, 28.06621538408569805 ) ) ;
#20840=ADVANCED_FACE ( 'NONE', ( #15984, #1487 ), #2849, .T. ) ;
#20842=VECTOR ( 'NONE', #1089, 1000.000000000000000 ) ;
#20847=CARTESIAN_POINT ( 'NONE',  ( 19.99999999999999645, 10.77748419466781726, -63.93680186330462334 ) ) ;
#20851=ADVANCED_FACE ( 'NONE', ( #12824 ), #20645, .T. ) ;
#20854=CARTESIAN_POINT ( 'NONE',  ( 85.00002539999999840, 0.000000000000000000, 0.000000000000000000 ) ) ;
#20855=CIRCLE ( 'NONE', #2288, 72.00000000007199219 ) ;
#20859=ORIENTED_EDGE ( 'NONE', *, *, #18571, .F. ) ;
#20860=CYLINDRICAL_SURFACE ( 'NONE', #5156, 27.60000000002759535 ) ;
#20863=ORIENTED_EDGE ( 'NONE', *, *, #12465, .T. ) ;
#20864=EDGE_CURVE ( 'NONE', #17301, #6711, #17690, .T. ) ;
#20868=DIRECTION ( 'NONE',  ( -1.000000000000000000, 0.000000000000000000, -0.000000000000000000 ) ) ;
#20870=CIRCLE ( 'NONE', #5296, 65.24900000006525147 ) ;
#20872=ORIENTED_EDGE ( 'NONE', *, *, #14649, .T. ) ;
#20873=ORIENTED_EDGE ( 'NONE', *, *, #12572, .F. ) ;
#20876=MECHANICAL_DESIGN_GEOMETRIC_PRESENTATION_REPRESENTATION('',(#1610),#14469);
#20878=EDGE_CURVE ( 'NONE', #5163, #12115, #16851, .T. ) ;
#20879=DIRECTION ( 'NONE',  ( -1.000000000000000000, 0.000000000000000000, -0.000000000000000000 ) ) ;
#20882=AXIS2_PLACEMENT_3D ( 'NONE', #2225, #8686, #15159 ) ;
#20886=ADVANCED_FACE ( 'NONE', ( #3764 ), #291, .T. ) ;
#20888=CARTESIAN_POINT ( 'NONE',  ( 19.99999999999999645, -63.05226888949902531, 15.11556105343437828 ) ) ;
#20891=CIRCLE ( 'NONE', #18521, 65.24900000006525147 ) ;
#20897=CARTESIAN_POINT ( 'NONE',  ( 0.000000000000000000, -39.37110852956777762, -51.51683813304910586 ) ) ;
#20898=ORIENTED_EDGE ( 'NONE', *, *, #5309, .F. ) ;
#20901=EDGE_CURVE ( 'NONE', #2530, #8201, #11442, .T. ) ;
#20903=DIRECTION ( 'NONE',  ( -1.000000000000000000, 0.000000000000000000, 0.000000000000000000 ) ) ;
#20904=EDGE_CURVE ( 'NONE', #5132, #4779, #6539, .T. ) ;
#20905=AXIS2_PLACEMENT_3D ( 'NONE', #3945, #15090, #2052 ) ;
#20907=DIRECTION ( 'NONE',  ( 0.000000000000000000, 0.8169698930104430934, -0.5766803221148656400 ) ) ;
#20908=CIRCLE ( 'NONE', #3301, 72.00000000007199219 ) ;
#20910=VERTEX_POINT ( 'NONE', #19891 ) ;
#20913=ORIENTED_EDGE ( 'NONE', *, *, #8496, .T. ) ;
#20914=DIRECTION ( 'NONE',  ( -1.000000000000000000, 0.000000000000000000, 0.000000000000000000 ) ) ;
#20915=DIRECTION ( 'NONE',  ( -1.000000000000000000, 0.000000000000000000, -0.000000000000000000 ) ) ;
#20917=VERTEX_POINT ( 'NONE', #1990 ) ;
#20920=CYLINDRICAL_SURFACE ( 'NONE', #15373, 27.60000000002760245 ) ;
#20921=EDGE_LOOP ( 'NONE', ( #18471, #3742, #20671, #15065 ) ) ;
#20924=CYLINDRICAL_SURFACE ( 'NONE', #1758, 72.00000000007199219 ) ;
#20925=ORIENTED_EDGE ( 'NONE', *, *, #16035, .T. ) ;
#20928=DIRECTION ( 'NONE',  ( -1.000000000000000000, 0.000000000000000000, 0.000000000000000000 ) ) ;
#20930=ORIENTED_EDGE ( 'NONE', *, *, #5309, .T. ) ;
#20934=DIRECTION ( 'NONE',  ( 0.000000000000000000, -0.7308359642781301346, 0.6825531432186475733 ) ) ;
#20936=LINE ( 'NONE', #17060, #10398 ) ;
#20941=ORIENTED_EDGE ( 'NONE', *, *, #5451, .F. ) ;
#20942=CYLINDRICAL_SURFACE ( 'NONE', #11261, 65.24900000006525147 ) ;
#20943=DIRECTION ( 'NONE',  ( 0.000000000000000000, -0.9790840876823249106, 0.2034560130526240629 ) ) ;
ENDSEC;
END-ISO-10303-21;
